ISO-10303-21;
HEADER;
FILE_DESCRIPTION (('STEP AP214'),
    '1' );
FILE_NAME ('slow gear_ISO - Spur gear 2M 80T 20PA 12FW ---S80A75H50L38.0N.step',
    '2026-10-08T09:53:37',
    ( '' ),
    ( '' ),
    'SwSTEP 2.0',
    'SolidWorks 2026',
    '' );
FILE_SCHEMA (( 'AUTOMOTIVE_DESIGN' ));
ENDSEC;

DATA;
#11=CYLINDRICAL_SURFACE ( 'NONE', #11189, 82.00000000000000000 ) ;
#13=DIRECTION ( 'NONE',  ( 0.000000000000000000, 0.8660254037844421493, 0.4999999999999938938 ) ) ;
#20=CYLINDRICAL_SURFACE ( 'NONE', #64875, 31.99999999999998579 ) ;
#26=ADVANCED_FACE ( 'NONE', ( #50299 ), #9718, .T. ) ;
#30=DIRECTION ( 'NONE',  ( 0.000000000000000000, 0.3090169943749410675, 0.9510565162951556406 ) ) ;
#38=ORIENTED_EDGE ( 'NONE', *, *, #69676, .T. ) ;
#41=ORIENTED_EDGE ( 'NONE', *, *, #37857, .F. ) ;
#45=VERTEX_POINT ( 'NONE', #4470 ) ;
#46=DIRECTION ( 'NONE',  ( -1.000000000000000000, 0.000000000000000000, 0.000000000000000000 ) ) ;
#48=ORIENTED_EDGE ( 'NONE', *, *, #42717, .F. ) ;
#63=EDGE_LOOP ( 'NONE', ( #58419, #58729, #9713, #39288 ) ) ;
#81=EDGE_CURVE ( 'NONE', #13281, #10925, #26630, .T. ) ;
#83=DIRECTION ( 'NONE',  ( -1.000000000000000000, 0.000000000000000000, 0.000000000000000000 ) ) ;
#84=ORIENTED_EDGE ( 'NONE', *, *, #17370, .T. ) ;
#94=CARTESIAN_POINT ( 'NONE',  ( 11.99999999999999822, 66.50666863322000211, 39.78640506895628448 ) ) ;
#97=VECTOR ( 'NONE', #25254, 1000.000000000000114 ) ;
#116=DIRECTION ( 'NONE',  ( 1.000000000000000000, -0.000000000000000000, -0.000000000000000000 ) ) ;
#117=DIRECTION ( 'NONE',  ( 1.000000000000000000, -0.000000000000000000, 0.000000000000000000 ) ) ;
#118=LINE ( 'NONE', #6814, #70143 ) ;
#119=CIRCLE ( 'NONE', #8452, 82.00000000000000000 ) ;
#122=ADVANCED_FACE ( 'NONE', ( #44690 ), #3363, .T. ) ;
#127=CARTESIAN_POINT ( 'NONE',  ( -10.00000000000000000, 0.000000000000000000, 0.000000000000000000 ) ) ;
#132=CARTESIAN_POINT ( 'NONE',  ( 11.99999999999999822, 41.76106447765580043, -62.50884508063379741 ) ) ;
#143=VERTEX_POINT ( 'NONE', #61975 ) ;
#147=ORIENTED_EDGE ( 'NONE', *, *, #29982, .T. ) ;
#150=CYLINDRICAL_SURFACE ( 'NONE', #8414, 77.49899999999999523 ) ;
#151=ADVANCED_FACE ( 'NONE', ( #45053 ), #32637, .T. ) ;
#154=ORIENTED_EDGE ( 'NONE', *, *, #63199, .F. ) ;
#158=ORIENTED_EDGE ( 'NONE', *, *, #43110, .F. ) ;
#162=CARTESIAN_POINT ( 'NONE',  ( 12.00000000000000355, 0.000000000000000000, 21.00000000000000000 ) ) ;
#173=ORIENTED_EDGE ( 'NONE', *, *, #55746, .F. ) ;
#176=CARTESIAN_POINT ( 'NONE',  ( 12.00000000000000000, -3.948201729842355068, -23.21447184625292692 ) ) ;
#181=AXIS2_PLACEMENT_3D ( 'NONE', #994, #13333, #11843 ) ;
#186=EDGE_LOOP ( 'NONE', ( #8690, #64007, #52251, #61322 ) ) ;
#192=CARTESIAN_POINT ( 'NONE',  ( 11.99999999999999822, -69.42325613327415113, -34.44570377933671779 ) ) ;
#196=VECTOR ( 'NONE', #2843, 1000.000000000000000 ) ;
#212=CARTESIAN_POINT ( 'NONE',  ( 11.99999999999999822, -65.64334221924937651, 41.19522573413711797 ) ) ;
#229=ORIENTED_EDGE ( 'NONE', *, *, #36188, .T. ) ;
#232=VERTEX_POINT ( 'NONE', #36200 ) ;
#237=VERTEX_POINT ( 'NONE', #8375 ) ;
#244=ADVANCED_FACE ( 'NONE', ( #1303 ), #7269, .T. ) ;
#253=DIRECTION ( 'NONE',  ( 0.000000000000000000, -6.938893903907231533E-15, 1.000000000000000000 ) ) ;
#257=DIRECTION ( 'NONE',  ( 0.000000000000000000, 0.000000000000000000, 1.000000000000000000 ) ) ;
#259=ORIENTED_EDGE ( 'NONE', *, *, #14783, .T. ) ;
#262=ORIENTED_EDGE ( 'NONE', *, *, #9019, .T. ) ;
#264=PLANE ( 'NONE',  #181 ) ;
#267=CARTESIAN_POINT ( 'NONE',  ( 11.99999999999999822, -2.946379043146863719, 75.11764819372146462 ) ) ;
#282=VECTOR ( 'NONE', #8652, 999.9999999999998863 ) ;
#283=CARTESIAN_POINT ( 'NONE',  ( 11.99999999999999822, -76.66974797899830207, -11.30684508768420571 ) ) ;
#289=DIRECTION ( 'NONE',  ( -1.000000000000000000, 0.000000000000000000, 0.000000000000000000 ) ) ;
#290=CARTESIAN_POINT ( 'NONE',  ( 11.99999999999999822, 10.30890764327501863, -81.34940948281324324 ) ) ;
#296=ORIENTED_EDGE ( 'NONE', *, *, #49460, .F. ) ;
#297=CARTESIAN_POINT ( 'NONE',  ( -10.00000000000000000, 0.000000000000000000, 0.000000000000000000 ) ) ;
#299=VECTOR ( 'NONE', #69573, 1000.000000000000000 ) ;
#300=VECTOR ( 'NONE', #69732, 1000.000000000000000 ) ;
#313=ORIENTED_EDGE ( 'NONE', *, *, #65007, .T. ) ;
#315=EDGE_CURVE ( 'NONE', #4428, #26458, #9223, .T. ) ;
#319=DIRECTION ( 'NONE',  ( -1.000000000000000000, 0.000000000000000000, 0.000000000000000000 ) ) ;
#325=ORIENTED_EDGE ( 'NONE', *, *, #34194, .F. ) ;
#332=VECTOR ( 'NONE', #36378, 1000.000000000000000 ) ;
#359=VERTEX_POINT ( 'NONE', #37325 ) ;
#366=VERTEX_POINT ( 'NONE', #72607 ) ;
#368=CARTESIAN_POINT ( 'NONE',  ( -10.00000000000000000, 0.000000000000000000, 0.000000000000000000 ) ) ;
#375=LINE ( 'NONE', #57852, #26573 ) ;
#378=LINE ( 'NONE', #63140, #40444 ) ;
#385=CARTESIAN_POINT ( 'NONE',  ( -10.00000000000000000, 0.000000000000000000, 0.000000000000000000 ) ) ;
#387=AXIS2_PLACEMENT_3D ( 'NONE', #42617, #2061, #64816 ) ;
#389=EDGE_CURVE ( 'NONE', #21226, #47439, #64170, .T. ) ;
#407=DIRECTION ( 'NONE',  ( 0.000000000000000000, 0.6691306063588661202, 0.7431448254773871387 ) ) ;
#415=CARTESIAN_POINT ( 'NONE',  ( 11.99999999999999822, 66.50666863322000211, 39.78640506895628448 ) ) ;
#417=ORIENTED_EDGE ( 'NONE', *, *, #65115, .F. ) ;
#424=DIRECTION ( 'NONE',  ( 0.000000000000000000, 0.7071067811865436870, 0.7071067811865513475 ) ) ;
#425=ORIENTED_EDGE ( 'NONE', *, *, #23338, .F. ) ;
#431=CYLINDRICAL_SURFACE ( 'NONE', #39041, 82.00000000000000000 ) ;
#451=EDGE_CURVE ( 'NONE', #39502, #20436, #22152, .T. ) ;
#454=VECTOR ( 'NONE', #33806, 1000.000000000000000 ) ;
#470=CARTESIAN_POINT ( 'NONE',  ( 11.99999999999999822, -59.75363087400035056, -56.15606465355020305 ) ) ;
#477=CARTESIAN_POINT ( 'NONE',  ( 0.000000000000000000, -73.95703589263958122, -23.16143007188505010 ) ) ;
#480=AXIS2_PLACEMENT_3D ( 'NONE', #12899, #47498, #41481 ) ;
#484=ORIENTED_EDGE ( 'NONE', *, *, #61147, .T. ) ;
#488=FACE_OUTER_BOUND ( 'NONE', #49842, .T. ) ;
#498=AXIS2_PLACEMENT_3D ( 'NONE', #29163, #40843, #63777 ) ;
#501=AXIS2_PLACEMENT_3D ( 'NONE', #68859, #24108, #18089 ) ;
#507=CARTESIAN_POINT ( 'NONE',  ( 11.99999999999999822, 75.54627589209970040, -17.28742895386005785 ) ) ;
#522=PLANE ( 'NONE',  #4394 ) ;
#523=LINE ( 'NONE', #34687, #51605 ) ;
#524=DIRECTION ( 'NONE',  ( 0.000000000000000000, 0.000000000000000000, 1.000000000000000000 ) ) ;
#527=ORIENTED_EDGE ( 'NONE', *, *, #36261, .T. ) ;
#530=ORIENTED_EDGE ( 'NONE', *, *, #3696, .T. ) ;
#537=EDGE_CURVE ( 'NONE', #47446, #69197, #73750, .T. ) ;
#544=EDGE_CURVE ( 'NONE', #21721, #68051, #41359, .T. ) ;
#547=DIRECTION ( 'NONE',  ( -1.000000000000000000, -0.000000000000000000, -0.000000000000000000 ) ) ;
#553=AXIS2_PLACEMENT_3D ( 'NONE', #47964, #19379, #37052 ) ;
#560=LINE ( 'NONE', #2036, #46654 ) ;
#562=CARTESIAN_POINT ( 'NONE',  ( 0.000000000000000000, -75.16055320797043748, 18.89407956138231270 ) ) ;
#569=DIRECTION ( 'NONE',  ( 0.000000000000000000, 0.5877852522924708056, -0.8090169943749491166 ) ) ;
#581=ORIENTED_EDGE ( 'NONE', *, *, #28091, .T. ) ;
#588=VERTEX_POINT ( 'NONE', #34626 ) ;
#590=VERTEX_POINT ( 'NONE', #56835 ) ;
#594=AXIS2_PLACEMENT_3D ( 'NONE', #11700, #37618, #37250 ) ;
#595=AXIS2_PLACEMENT_3D ( 'NONE', #68160, #67039, #38481 ) ;
#599=ORIENTED_EDGE ( 'NONE', *, *, #44383, .T. ) ;
#612=EDGE_LOOP ( 'NONE', ( #17860, #45967, #2763, #45895 ) ) ;
#622=CARTESIAN_POINT ( 'NONE',  ( 0.000000000000000000, 27.74655509720780344, -77.16300072079631889 ) ) ;
#637=LINE ( 'NONE', #52844, #42561 ) ;
#649=LINE ( 'NONE', #40460, #53242 ) ;
#650=CARTESIAN_POINT ( 'NONE',  ( 15.00000000000000000, 14.60985201121703980, -18.46759930825707841 ) ) ;
#651=EDGE_CURVE ( 'NONE', #53386, #50810, #36469, .T. ) ;
#660=DIRECTION ( 'NONE',  ( -1.000000000000000000, 0.000000000000000000, 0.000000000000000000 ) ) ;
#677=ORIENTED_EDGE ( 'NONE', *, *, #18568, .T. ) ;
#682=CARTESIAN_POINT ( 'NONE',  ( 0.000000000000000000, 39.47590169984945163, -71.87247863392373404 ) ) ;
#706=CIRCLE ( 'NONE', #10260, 31.99999999999998579 ) ;
#712=CARTESIAN_POINT ( 'NONE',  ( 15.00000000000000000, 6.762365576493310826, -25.66652317338401090 ) ) ;
#714=CARTESIAN_POINT ( 'NONE',  ( 15.00000000000000000, -18.13022148937263012, -15.02647892043543898 ) ) ;
#719=VERTEX_POINT ( 'NONE', #2311 ) ;
#725=CARTESIAN_POINT ( 'NONE',  ( 0.000000000000000000, -62.50884508063395373, -41.76106447765554464 ) ) ;
#731=CARTESIAN_POINT ( 'NONE',  ( 0.000000000000000000, -74.74816331893453025, 33.71516098798714722 ) ) ;
#733=VECTOR ( 'NONE', #407, 1000.000000000000000 ) ;
#740=FACE_OUTER_BOUND ( 'NONE', #186, .T. ) ;
#741=CARTESIAN_POINT ( 'NONE',  ( 0.000000000000000000, -36.73666225445845157, -65.58780272294114866 ) ) ;
#743=EDGE_CURVE ( 'NONE', #60856, #66942, #69583, .T. ) ;
#749=DIRECTION ( 'NONE',  ( -0.000000000000000000, 0.5000000000000038858, 0.8660254037844363761 ) ) ;
#750=DIRECTION ( 'NONE',  ( 0.000000000000000000, 0.5877852522924780221, 0.8090169943749438985 ) ) ;
#751=EDGE_CURVE ( 'NONE', #28286, #68468, #38828, .T. ) ;
#759=DIRECTION ( 'NONE',  ( 0.000000000000000000, -0.7604059656000227152, -0.6494480483301934282 ) ) ;
#774=ORIENTED_EDGE ( 'NONE', *, *, #54561, .F. ) ;
#781=AXIS2_PLACEMENT_3D ( 'NONE', #6819, #24847, #19567 ) ;
#797=DIRECTION ( 'NONE',  ( 0.000000000000000000, 0.1564344650402244019, 0.9876883405951387696 ) ) ;
#798=DIRECTION ( 'NONE',  ( 0.000000000000000000, 0.000000000000000000, 1.000000000000000000 ) ) ;
#803=ORIENTED_EDGE ( 'NONE', *, *, #14680, .F. ) ;
#804=DIRECTION ( 'NONE',  ( -1.000000000000000000, 0.000000000000000000, 0.000000000000000000 ) ) ;
#813=EDGE_CURVE ( 'NONE', #67853, #69733, #42870, .T. ) ;
#817=DIRECTION ( 'NONE',  ( 1.000000000000000000, 0.000000000000000000, 0.000000000000000000 ) ) ;
#818=CARTESIAN_POINT ( 'NONE',  ( 0.000000000000000000, -81.96053171279903893, 2.543863470248101333 ) ) ;
#821=CARTESIAN_POINT ( 'NONE',  ( 0.000000000000000000, 55.20638768913760686, 51.02545421589343988 ) ) ;
#839=EDGE_CURVE ( 'NONE', #45762, #32475, #26300, .T. ) ;
#853=CARTESIAN_POINT ( 'NONE',  ( 12.00000000000000000, 20.85821328998741109, -10.92862929874522671 ) ) ;
#855=VERTEX_POINT ( 'NONE', #65800 ) ;
#861=AXIS2_PLACEMENT_3D ( 'NONE', #12106, #35045, #12475 ) ;
#866=ORIENTED_EDGE ( 'NONE', *, *, #10496, .F. ) ;
#868=EDGE_LOOP ( 'NONE', ( #22669, #43084, #16669, #61333 ) ) ;
#878=AXIS2_PLACEMENT_3D ( 'NONE', #26295, #49228, #31195 ) ;
#879=EDGE_CURVE ( 'NONE', #38728, #27488, #14836, .T. ) ;
#884=ORIENTED_EDGE ( 'NONE', *, *, #13756, .T. ) ;
#888=CARTESIAN_POINT ( 'NONE',  ( 15.00000000000000000, -26.23277895567251505, -4.042438405569750870 ) ) ;
#892=EDGE_CURVE ( 'NONE', #32115, #57513, #43257, .T. ) ;
#903=EDGE_CURVE ( 'NONE', #33655, #1337, #14284, .T. ) ;
#917=EDGE_CURVE ( 'NONE', #41826, #143, #63505, .T. ) ;
#926=AXIS2_PLACEMENT_3D ( 'NONE', #39119, #66582, #26705 ) ;
#929=DIRECTION ( 'NONE',  ( 0.000000000000000000, 0.000000000000000000, 1.000000000000000000 ) ) ;
#940=DIRECTION ( 'NONE',  ( 0.000000000000000000, 0.9510565162951536422, 0.3090169943749471182 ) ) ;
#964=DIRECTION ( 'NONE',  ( -1.000000000000000000, -0.000000000000000000, 0.000000000000000000 ) ) ;
#970=EDGE_LOOP ( 'NONE', ( #40059, #29578, #18197, #54354 ) ) ;
#972=ORIENTED_EDGE ( 'NONE', *, *, #22497, .F. ) ;
#974=LINE ( 'NONE', #40408, #37100 ) ;
#984=ORIENTED_EDGE ( 'NONE', *, *, #20979, .T. ) ;
#987=CARTESIAN_POINT ( 'NONE',  ( 0.000000000000000000, -64.81221759200379040, 50.23322058963324110 ) ) ;
#994=CARTESIAN_POINT ( 'NONE',  ( 15.00000000000000000, -19.89357724625003598, -12.59942793731059041 ) ) ;
#998=ORIENTED_EDGE ( 'NONE', *, *, #42050, .F. ) ;
#1011=VECTOR ( 'NONE', #2786, 1000.000000000000000 ) ;
#1014=DIRECTION ( 'NONE',  ( -1.000000000000000000, 0.000000000000000000, -0.000000000000000000 ) ) ;
#1016=DIRECTION ( 'NONE',  ( 1.000000000000000000, 0.000000000000000000, 0.000000000000000000 ) ) ;
#1020=DIRECTION ( 'NONE',  ( -1.000000000000000000, 0.000000000000000000, 0.000000000000000000 ) ) ;
#1022=CARTESIAN_POINT ( 'NONE',  ( 11.99999999999999822, -73.95703589263958122, -23.16143007188505010 ) ) ;
#1026=AXIS2_PLACEMENT_3D ( 'NONE', #3591, #2859, #37037 ) ;
#1027=VECTOR ( 'NONE', #57764, 1000.000000000000000 ) ;
#1029=CARTESIAN_POINT ( 'NONE',  ( 0.000000000000000000, 51.03279382321088065, 55.19960302592086521 ) ) ;
#1035=AXIS2_PLACEMENT_3D ( 'NONE', #72622, #66281, #14754 ) ;
#1044=CIRCLE ( 'NONE', #32217, 82.00000000000000000 ) ;
#1048=ORIENTED_EDGE ( 'NONE', *, *, #56690, .T. ) ;
#1049=VECTOR ( 'NONE', #6917, 1000.000000000000000 ) ;
#1055=CYLINDRICAL_SURFACE ( 'NONE', #60505, 31.99999999999998579 ) ;
#1061=VERTEX_POINT ( 'NONE', #5626 ) ;
#1062=VERTEX_POINT ( 'NONE', #51465 ) ;
#1063=ORIENTED_EDGE ( 'NONE', *, *, #64797, .T. ) ;
#1075=ADVANCED_FACE ( 'NONE', ( #57486 ), #20, .T. ) ;
#1079=VECTOR ( 'NONE', #34029, 1000.000000000000000 ) ;
#1082=EDGE_LOOP ( 'NONE', ( #30138, #24808, #4651, #72575 ) ) ;
#1097=VERTEX_POINT ( 'NONE', #7455 ) ;
#1098=ADVANCED_FACE ( 'NONE', ( #64980 ), #24013, .T. ) ;
#1113=LINE ( 'NONE', #11970, #36398 ) ;
#1116=DIRECTION ( 'NONE',  ( 1.000000000000000000, -0.000000000000000000, -0.000000000000000000 ) ) ;
#1125=CARTESIAN_POINT ( 'NONE',  ( 0.000000000000000000, -31.47745569255092235, -68.26794271651296242 ) ) ;
#1129=DIRECTION ( 'NONE',  ( 0.000000000000000000, 0.9238795325112851842, 0.3826834323650937786 ) ) ;
#1140=ORIENTED_EDGE ( 'NONE', *, *, #2156, .F. ) ;
#1141=DIRECTION ( 'NONE',  ( -1.000000000000000000, 0.000000000000000000, 0.000000000000000000 ) ) ;
#1145=LINE ( 'NONE', #24398, #36387 ) ;
#1148=AXIS2_PLACEMENT_3D ( 'NONE', #69760, #16793, #69391 ) ;
#1167=VECTOR ( 'NONE', #67110, 1000.000000000000000 ) ;
#1170=VERTEX_POINT ( 'NONE', #30001 ) ;
#1174=CARTESIAN_POINT ( 'NONE',  ( 15.00000000000000000, 0.000000000000000000, 0.000000000000000000 ) ) ;
#1175=EDGE_CURVE ( 'NONE', #61985, #23343, #58965, .T. ) ;
#1177=DIRECTION ( 'NONE',  ( -1.000000000000000000, 0.000000000000000000, -0.000000000000000000 ) ) ;
#1181=DIRECTION ( 'NONE',  ( -1.000000000000000000, 0.000000000000000000, -0.000000000000000000 ) ) ;
#1182=DIRECTION ( 'NONE',  ( -1.000000000000000000, -0.000000000000000000, -0.000000000000000000 ) ) ;
#1189=ORIENTED_EDGE ( 'NONE', *, *, #14589, .F. ) ;
#1194=CARTESIAN_POINT ( 'NONE',  ( 11.99999999999999822, 72.35432306680485226, -20.40083707022909110 ) ) ;
#1205=CARTESIAN_POINT ( 'NONE',  ( 11.99999999999999822, 0.000000000000000000, 0.000000000000000000 ) ) ;
#1214=AXIS2_PLACEMENT_3D ( 'NONE', #42287, #30244, #59569 ) ;
#1230=DIRECTION ( 'NONE',  ( 0.000000000000000000, 0.000000000000000000, 1.000000000000000000 ) ) ;
#1233=DIRECTION ( 'NONE',  ( 0.000000000000000000, -0.8090169943749401238, -0.5877852522924831291 ) ) ;
#1236=AXIS2_PLACEMENT_3D ( 'NONE', #49211, #20650, #30670 ) ;
#1251=DIRECTION ( 'NONE',  ( -1.000000000000000000, -0.000000000000000000, -0.000000000000000000 ) ) ;
#1257=VERTEX_POINT ( 'NONE', #14939 ) ;
#1258=DIRECTION ( 'NONE',  ( -1.000000000000000000, -0.000000000000000000, 0.000000000000000000 ) ) ;
#1260=CIRCLE ( 'NONE', #20423, 31.99999999999998579 ) ;
#1268=SHAPE_DEFINITION_REPRESENTATION ( #56642, #36835 ) ;
#1283=CARTESIAN_POINT ( 'NONE',  ( 15.00000000000000000, -13.04903810567675393, -19.60159698893424718 ) ) ;
#1285=DIRECTION ( 'NONE',  ( 0.000000000000000000, -0.9238795325112821866, -0.3826834323651008285 ) ) ;
#1294=ORIENTED_EDGE ( 'NONE', *, *, #18339, .T. ) ;
#1298=CARTESIAN_POINT ( 'NONE',  ( 0.000000000000000000, 33.71516098798849015, -74.74816331893393340 ) ) ;
#1301=CARTESIAN_POINT ( 'NONE',  ( 11.99999999999999822, 51.03279382321166224, -55.19960302592011914 ) ) ;
#1303=FACE_OUTER_BOUND ( 'NONE', #33672, .T. ) ;
#1305=CYLINDRICAL_SURFACE ( 'NONE', #51389, 31.99999999999998579 ) ;
#1306=DIRECTION ( 'NONE',  ( -1.000000000000000000, 0.000000000000000000, -0.000000000000000000 ) ) ;
#1308=CIRCLE ( 'NONE', #26476, 31.99999999999998934 ) ;
#1309=CARTESIAN_POINT ( 'NONE',  ( 11.99999999999999822, -40.65526001592564853, -71.21200624218839437 ) ) ;
#1311=( LENGTH_UNIT ( ) NAMED_UNIT ( * ) SI_UNIT ( .MILLI., .METRE. ) );
#1313=CYLINDRICAL_SURFACE ( 'NONE', #10823, 31.99999999999998579 ) ;
#1315=DIRECTION ( 'NONE',  ( -1.000000000000000000, -0.000000000000000000, -0.000000000000000000 ) ) ;
#1318=DIRECTION ( 'NONE',  ( 0.000000000000000000, 0.000000000000000000, 1.000000000000000000 ) ) ;
#1320=EDGE_LOOP ( 'NONE', ( #66595, #15736, #2918, #49929 ) ) ;
#1331=DIRECTION ( 'NONE',  ( -1.000000000000000000, 0.000000000000000000, -0.000000000000000000 ) ) ;
#1332=ORIENTED_EDGE ( 'NONE', *, *, #14740, .T. ) ;
#1334=CARTESIAN_POINT ( 'NONE',  ( 0.000000000000000000, 26.02418014898310261, 70.52718814184268581 ) ) ;
#1335=ORIENTED_EDGE ( 'NONE', *, *, #11023, .T. ) ;
#1337=VERTEX_POINT ( 'NONE', #25480 ) ;
#1346=DIRECTION ( 'NONE',  ( -1.000000000000000000, -0.000000000000000000, -0.000000000000000000 ) ) ;
#1353=CIRCLE ( 'NONE', #7319, 82.00000000000000000 ) ;
#1359=DIRECTION ( 'NONE',  ( 0.000000000000000000, 0.000000000000000000, -1.000000000000000000 ) ) ;
#1376=DIRECTION ( 'NONE',  ( 0.000000000000000000, 0.000000000000000000, 1.000000000000000000 ) ) ;
#1377=VECTOR ( 'NONE', #14068, 1000.000000000000000 ) ;
#1387=EDGE_CURVE ( 'NONE', #52407, #28756, #61183, .T. ) ;
#1393=CARTESIAN_POINT ( 'NONE',  ( 12.00000000000000000, 5.835314593368777558, 22.81335362449846471 ) ) ;
#1395=DIRECTION ( 'NONE',  ( 0.000000000000000000, -0.07845909572785234043, 0.9969173337331274087 ) ) ;
#1426=EDGE_CURVE ( 'NONE', #17494, #34012, #52386, .T. ) ;
#1431=CYLINDRICAL_SURFACE ( 'NONE', #22074, 77.49899999999999523 ) ;
#1446=ORIENTED_EDGE ( 'NONE', *, *, #4810, .F. ) ;
#1464=CARTESIAN_POINT ( 'NONE',  ( 11.99999999999999822, 51.02545421589402252, -55.20638768913705263 ) ) ;
#1471=ORIENTED_EDGE ( 'NONE', *, *, #12870, .F. ) ;
#1472=ADVANCED_FACE ( 'NONE', ( #38621 ), #1313, .T. ) ;
#1474=CARTESIAN_POINT ( 'NONE',  ( 11.99999999999999822, 80.55351364060588537, 15.33399622253511829 ) ) ;
#1480=AXIS2_PLACEMENT_3D ( 'NONE', #65172, #58785, #7282 ) ;
#1482=ADVANCED_FACE ( 'NONE', ( #68307 ), #67559, .T. ) ;
#1488=LINE ( 'NONE', #13456, #332 ) ;
#1491=DIRECTION ( 'NONE',  ( 0.000000000000000000, 0.000000000000000000, 1.000000000000000000 ) ) ;
#1495=EDGE_CURVE ( 'NONE', #24191, #40982, #61218, .T. ) ;
#1506=ORIENTED_EDGE ( 'NONE', *, *, #55790, .T. ) ;
#1507=ORIENTED_EDGE ( 'NONE', *, *, #8990, .T. ) ;
#1508=VECTOR ( 'NONE', #39066, 1000.000000000000000 ) ;
#1511=ORIENTED_EDGE ( 'NONE', *, *, #34886, .F. ) ;
#1512=EDGE_CURVE ( 'NONE', #7988, #58803, #65910, .T. ) ;
#1513=LINE ( 'NONE', #12735, #60580 ) ;
#1515=CARTESIAN_POINT ( 'NONE',  ( 11.99999999999999822, -35.91791733033428358, -68.67312586195033930 ) ) ;
#1523=CARTESIAN_POINT ( 'NONE',  ( 0.000000000000000000, 0.000000000000000000, 0.000000000000000000 ) ) ;
#1528=CARTESIAN_POINT ( 'NONE',  ( 11.99999999999999822, 79.10210256391367523, 21.60688246758614284 ) ) ;
#1531=ORIENTED_EDGE ( 'NONE', *, *, #3412, .F. ) ;
#1543=VERTEX_POINT ( 'NONE', #30193 ) ;
#1545=ORIENTED_EDGE ( 'NONE', *, *, #47043, .F. ) ;
#1550=CARTESIAN_POINT ( 'NONE',  ( 0.000000000000000000, -59.46389618801999433, 49.70050353004867816 ) ) ;
#1568=DIRECTION ( 'NONE',  ( 0.000000000000000000, 0.9969173337331276308, 0.07845909572784874608 ) ) ;
#1569=CARTESIAN_POINT ( 'NONE',  ( 15.00000000000000000, -22.32062822937469093, 14.36278369418830181 ) ) ;
#1576=EDGE_CURVE ( 'NONE', #33089, #21642, #34083, .T. ) ;
#1577=CARTESIAN_POINT ( 'NONE',  ( 11.99999999999999822, 68.26794271651307611, -31.47745569255064169 ) ) ;
#1589=DIRECTION ( 'NONE',  ( 0.000000000000000000, -0.9876883405951394357, 0.1564344650402205716 ) ) ;
#1597=EDGE_CURVE ( 'NONE', #29219, #39517, #2881, .T. ) ;
#1603=CARTESIAN_POINT ( 'NONE',  ( 11.99999999999999822, -24.73286445877757345, 73.44644590900053061 ) ) ;
#1606=VERTEX_POINT ( 'NONE', #36951 ) ;
#1610=AXIS2_PLACEMENT_3D ( 'NONE', #59355, #54817, #8590 ) ;
#1615=DIRECTION ( 'NONE',  ( 0.000000000000000000, 0.000000000000000000, 1.000000000000000000 ) ) ;
#1627=EDGE_LOOP ( 'NONE', ( #50321, #61394, #9092, #16789 ) ) ;
#1633=CARTESIAN_POINT ( 'NONE',  ( 0.000000000000000000, -76.69515212745996280, -29.01471420065643869 ) ) ;
#1641=ORIENTED_EDGE ( 'NONE', *, *, #28400, .F. ) ;
#1642=CARTESIAN_POINT ( 'NONE',  ( 11.99999999999999822, 76.69515212746016175, 29.01471420065590578 ) ) ;
#1643=PLANE ( 'NONE',  #55177 ) ;
#1652=DIRECTION ( 'NONE',  ( -1.000000000000000000, 0.000000000000000000, 0.000000000000000000 ) ) ;
#1654=EDGE_CURVE ( 'NONE', #23480, #37858, #64796, .T. ) ;
#1656=ADVANCED_FACE ( 'NONE', ( #14386 ), #37334, .F. ) ;
#1662=DIRECTION ( 'NONE',  ( 0.000000000000000000, -0.5000000000000038858, -0.8660254037844363761 ) ) ;
#1669=CARTESIAN_POINT ( 'NONE',  ( 0.000000000000000000, 0.000000000000000000, 0.000000000000000000 ) ) ;
#1673=SURFACE_STYLE_FILL_AREA ( #63320 ) ;
#1674=EDGE_CURVE ( 'NONE', #6114, #67241, #3500, .T. ) ;
#1675=DIRECTION ( 'NONE',  ( -0.000000000000000000, 0.6691306063588672304, 0.7431448254773862505 ) ) ;
#1681=VERTEX_POINT ( 'NONE', #39176 ) ;
#1682=CARTESIAN_POINT ( 'NONE',  ( 11.99999999999999822, -73.73191006444561424, -14.66109333815538918 ) ) ;
#1683=CARTESIAN_POINT ( 'NONE',  ( 11.99999999999999822, 54.21277698773675979, 55.38113227695801299 ) ) ;
#1685=EDGE_CURVE ( 'NONE', #50776, #855, #28066, .T. ) ;
#1688=DIRECTION ( 'NONE',  ( -1.000000000000000000, -0.000000000000000000, -0.000000000000000000 ) ) ;
#1694=CARTESIAN_POINT ( 'NONE',  ( 11.99999999999999822, 0.000000000000000000, 0.000000000000000000 ) ) ;
#1700=ORIENTED_EDGE ( 'NONE', *, *, #51808, .T. ) ;
#1713=CIRCLE ( 'NONE', #17289, 31.99999999999999289 ) ;
#1726=CIRCLE ( 'NONE', #31724, 31.99999999999998579 ) ;
#1733=ADVANCED_FACE ( 'NONE', ( #21493 ), #72618, .F. ) ;
#1734=LINE ( 'NONE', #70461, #12258 ) ;
#1751=ORIENTED_EDGE ( 'NONE', *, *, #16450, .F. ) ;
#1755=DIRECTION ( 'NONE',  ( -1.000000000000000000, 0.000000000000000000, 0.000000000000000000 ) ) ;
#1762=ADVANCED_FACE ( 'NONE', ( #3869 ), #67367, .T. ) ;
#1796=EDGE_CURVE ( 'NONE', #32190, #40071, #39551, .T. ) ;
#1803=CARTESIAN_POINT ( 'NONE',  ( 11.99999999999999822, 5.256550761632864166, 77.32052557432842832 ) ) ;
#1822=ORIENTED_EDGE ( 'NONE', *, *, #50920, .T. ) ;
#1823=CARTESIAN_POINT ( 'NONE',  ( 15.00000000000000000, 0.000000000000000000, 0.000000000000000000 ) ) ;
#1828=CYLINDRICAL_SURFACE ( 'NONE', #2605, 31.99999999999998579 ) ;
#1833=AXIS2_PLACEMENT_3D ( 'NONE', #38345, #39094, #60909 ) ;
#1841=FACE_OUTER_BOUND ( 'NONE', #23600, .T. ) ;
#1844=CARTESIAN_POINT ( 'NONE',  ( 0.000000000000000000, 62.20884554314020676, 46.21855187248652896 ) ) ;
#1845=CARTESIAN_POINT ( 'NONE',  ( 11.99999999999999822, -59.46389618801929089, -49.70050353004953081 ) ) ;
#1849=EDGE_CURVE ( 'NONE', #15455, #32135, #60896, .T. ) ;
#1850=DIRECTION ( 'NONE',  ( -1.000000000000000000, 0.000000000000000000, 0.000000000000000000 ) ) ;
#1852=EDGE_CURVE ( 'NONE', #588, #49792, #56478, .T. ) ;
#1862=DIRECTION ( 'NONE',  ( 0.000000000000000000, 0.000000000000000000, 1.000000000000000000 ) ) ;
#1863=VERTEX_POINT ( 'NONE', #4982 ) ;
#1874=ORIENTED_EDGE ( 'NONE', *, *, #17594, .F. ) ;
#1882=LINE ( 'NONE', #8596, #69536 ) ;
#1887=DIRECTION ( 'NONE',  ( 0.000000000000000000, -0.1564344650402381687, 0.9876883405951365491 ) ) ;
#1896=CARTESIAN_POINT ( 'NONE',  ( 11.99999999999999822, 77.16300072079698680, -27.74655509720590629 ) ) ;
#1902=ORIENTED_EDGE ( 'NONE', *, *, #53163, .T. ) ;
#1907=ORIENTED_EDGE ( 'NONE', *, *, #16647, .T. ) ;
#1912=CIRCLE ( 'NONE', #61934, 31.99999999999998934 ) ;
#1918=CARTESIAN_POINT ( 'NONE',  ( 11.99999999999999822, 74.65374052328648702, 8.840884882375350529 ) ) ;
#1921=FACE_OUTER_BOUND ( 'NONE', #49565, .T. ) ;
#1925=EDGE_CURVE ( 'NONE', #38652, #27167, #17350, .T. ) ;
#1933=CARTESIAN_POINT ( 'NONE',  ( 0.000000000000000000, -70.52718814184277107, 26.02418014898285037 ) ) ;
#1935=EDGE_CURVE ( 'NONE', #54478, #45, #11693, .T. ) ;
#1938=FACE_OUTER_BOUND ( 'NONE', #41703, .T. ) ;
#1943=VECTOR ( 'NONE', #31711, 1000.000000000000000 ) ;
#1949=DIRECTION ( 'NONE',  ( -1.000000000000000000, 0.000000000000000000, 0.000000000000000000 ) ) ;
#1968=DIRECTION ( 'NONE',  ( -1.000000000000000000, -0.000000000000000000, -0.000000000000000000 ) ) ;
#1971=ORIENTED_EDGE ( 'NONE', *, *, #69410, .T. ) ;
#1985=ORIENTED_EDGE ( 'NONE', *, *, #55925, .F. ) ;
#1995=CARTESIAN_POINT ( 'NONE',  ( 11.99999999999999822, 0.000000000000000000, 0.000000000000000000 ) ) ;
#1997=VECTOR ( 'NONE', #73274, 1000.000000000000000 ) ;
#1998=CARTESIAN_POINT ( 'NONE',  ( 11.99999999999999822, 0.000000000000000000, 0.000000000000000000 ) ) ;
#2002=ORIENTED_EDGE ( 'NONE', *, *, #69178, .T. ) ;
#2006=AXIS2_PLACEMENT_3D ( 'NONE', #58291, #57566, #19172 ) ;
#2008=CARTESIAN_POINT ( 'NONE',  ( 15.00000000000000000, 26.49999999999999645, 1.499999999999995781 ) ) ;
#2010=CYLINDRICAL_SURFACE ( 'NONE', #31399, 77.49899999999999523 ) ;
#2013=CARTESIAN_POINT ( 'NONE',  ( 11.99999999999999822, 8.840884882376133902, -74.65374052328640175 ) ) ;
#2028=CARTESIAN_POINT ( 'NONE',  ( 11.99999999999999822, 0.000000000000000000, 0.000000000000000000 ) ) ;
#2031=ORIENTED_EDGE ( 'NONE', *, *, #62393, .T. ) ;
#2036=CARTESIAN_POINT ( 'NONE',  ( 5.999999999999999112, 27.74655509720669500, 77.16300072079670258 ) ) ;
#2037=DIRECTION ( 'NONE',  ( 0.000000000000000000, -0.5877852522924802425, 0.8090169943749422332 ) ) ;
#2047=ORIENTED_EDGE ( 'NONE', *, *, #70798, .F. ) ;
#2051=AXIS2_PLACEMENT_3D ( 'NONE', #54225, #53109, #30897 ) ;
#2055=VERTEX_POINT ( 'NONE', #19197 ) ;
#2061=DIRECTION ( 'NONE',  ( -1.000000000000000000, -0.000000000000000000, 0.000000000000000000 ) ) ;
#2065=EDGE_CURVE ( 'NONE', #35604, #57809, #19361, .T. ) ;
#2066=AXIS2_PLACEMENT_3D ( 'NONE', #35214, #70515, #46880 ) ;
#2067=ORIENTED_EDGE ( 'NONE', *, *, #74116, .F. ) ;
#2077=FACE_OUTER_BOUND ( 'NONE', #32273, .T. ) ;
#2085=CARTESIAN_POINT ( 'NONE',  ( 11.99999999999999822, 30.41916302227216562, -71.27951684757994144 ) ) ;
#2102=VECTOR ( 'NONE', #50687, 1000.000000000000000 ) ;
#2104=VERTEX_POINT ( 'NONE', #71791 ) ;
#2105=FACE_OUTER_BOUND ( 'NONE', #23044, .T. ) ;
#2106=ADVANCED_FACE ( 'NONE', ( #27417 ), #21785, .T. ) ;
#2109=ORIENTED_EDGE ( 'NONE', *, *, #41746, .F. ) ;
#2121=DIRECTION ( 'NONE',  ( -1.000000000000000000, 0.000000000000000000, 0.000000000000000000 ) ) ;
#2125=LINE ( 'NONE', #31011, #56050 ) ;
#2127=DIRECTION ( 'NONE',  ( -1.000000000000000000, 0.000000000000000000, -0.000000000000000000 ) ) ;
#2129=CARTESIAN_POINT ( 'NONE',  ( -10.00000000000000000, 0.000000000000000000, 0.000000000000000000 ) ) ;
#2132=DIRECTION ( 'NONE',  ( 0.000000000000000000, 0.7604059656000322631, -0.6494480483301821039 ) ) ;
#2142=DIRECTION ( 'NONE',  ( -1.000000000000000000, 0.000000000000000000, 0.000000000000000000 ) ) ;
#2150=AXIS2_PLACEMENT_3D ( 'NONE', #12967, #16878, #39811 ) ;
#2154=VERTEX_POINT ( 'NONE', #43630 ) ;
#2156=EDGE_CURVE ( 'NONE', #36701, #53249, #14294, .T. ) ;
#2163=DIRECTION ( 'NONE',  ( -1.000000000000000000, 0.000000000000000000, 0.000000000000000000 ) ) ;
#2165=ORIENTED_EDGE ( 'NONE', *, *, #6174, .T. ) ;
#2171=AXIS2_PLACEMENT_3D ( 'NONE', #11912, #52889, #7400 ) ;
#2178=ORIENTED_EDGE ( 'NONE', *, *, #14660, .T. ) ;
#2183=ORIENTED_EDGE ( 'NONE', *, *, #4249, .F. ) ;
#2198=CARTESIAN_POINT ( 'NONE',  ( 11.99999999999999822, 0.000000000000000000, 0.000000000000000000 ) ) ;
#2203=AXIS2_PLACEMENT_3D ( 'NONE', #1523, #6392, #12744 ) ;
#2204=DIRECTION ( 'NONE',  ( -1.000000000000000000, -0.000000000000000000, -0.000000000000000000 ) ) ;
#2206=VECTOR ( 'NONE', #31382, 999.9999999999998863 ) ;
#2208=EDGE_LOOP ( 'NONE', ( #5662, #48384, #16356, #23020 ) ) ;
#2217=FACE_OUTER_BOUND ( 'NONE', #70885, .T. ) ;
#2227=VECTOR ( 'NONE', #22749, 1000.000000000000000 ) ;
#2228=VECTOR ( 'NONE', #24928, 1000.000000000000000 ) ;
#2230=CARTESIAN_POINT ( 'NONE',  ( 0.000000000000000000, 76.41127070299290835, -12.93880638057234123 ) ) ;
#2234=CARTESIAN_POINT ( 'NONE',  ( 0.000000000000000000, 0.000000000000000000, 0.000000000000000000 ) ) ;
#2235=LINE ( 'NONE', #48059, #42023 ) ;
#2241=ORIENTED_EDGE ( 'NONE', *, *, #11525, .T. ) ;
#2254=ORIENTED_EDGE ( 'NONE', *, *, #54247, .F. ) ;
#2255=ORIENTED_EDGE ( 'NONE', *, *, #9692, .F. ) ;
#2266=EDGE_CURVE ( 'NONE', #45880, #26872, #58477, .T. ) ;
#2274=CIRCLE ( 'NONE', #39440, 31.99999999999999289 ) ;
#2284=AXIS2_PLACEMENT_3D ( 'NONE', #18097, #62498, #69231 ) ;
#2288=AXIS2_PLACEMENT_3D ( 'NONE', #50925, #56953, #40387 ) ;
#2289=LINE ( 'NONE', #42111, #27503 ) ;
#2298=CARTESIAN_POINT ( 'NONE',  ( 12.00000000000000000, -22.32062822937469093, 14.36278369418830181 ) ) ;
#2311=CARTESIAN_POINT ( 'NONE',  ( 11.99999999999999822, 39.47590169984846398, 71.87247863392425984 ) ) ;
#2312=AXIS2_PLACEMENT_3D ( 'NONE', #69309, #7633, #6179 ) ;
#2317=CARTESIAN_POINT ( 'NONE',  ( 0.000000000000000000, 74.65374052328660071, -8.840884882374309583 ) ) ;
#2328=EDGE_CURVE ( 'NONE', #15222, #73599, #8029, .T. ) ;
#2330=VECTOR ( 'NONE', #54980, 1000.000000000000000 ) ;
#2333=VECTOR ( 'NONE', #25162, 1000.000000000000000 ) ;
#2337=DIRECTION ( 'NONE',  ( 1.000000000000000000, 0.000000000000000000, -0.000000000000000000 ) ) ;
#2365=CIRCLE ( 'NONE', #22792, 82.00000000000000000 ) ;
#2377=LINE ( 'NONE', #60234, #64876 ) ;
#2381=ORIENTED_EDGE ( 'NONE', *, *, #60782, .T. ) ;
#2391=DIRECTION ( 'NONE',  ( 1.000000000000000000, -0.000000000000000000, 0.000000000000000000 ) ) ;
#2392=FACE_OUTER_BOUND ( 'NONE', #70808, .T. ) ;
#2394=ORIENTED_EDGE ( 'NONE', *, *, #12407, .F. ) ;
#2396=VECTOR ( 'NONE', #30345, 1000.000000000000000 ) ;
#2398=CARTESIAN_POINT ( 'NONE',  ( 11.99999999999999822, -74.18225833017913828, 34.94270380257611208 ) ) ;
#2401=CARTESIAN_POINT ( 'NONE',  ( 11.99999999999999822, 0.000000000000000000, 0.000000000000000000 ) ) ;
#2402=DIRECTION ( 'NONE',  ( 0.000000000000000000, -0.8526401643540860720, -0.5224985647159590130 ) ) ;
#2404=CARTESIAN_POINT ( 'NONE',  ( 0.000000000000000000, -3.894527615417333610, -81.90746397400393164 ) ) ;
#2410=CARTESIAN_POINT ( 'NONE',  ( 11.99999999999999822, 70.52718814184294160, -26.02418014898236720 ) ) ;
#2418=EDGE_CURVE ( 'NONE', #12733, #55763, #59337, .T. ) ;
#2419=DIRECTION ( 'NONE',  ( 1.000000000000000000, -0.000000000000000000, -0.000000000000000000 ) ) ;
#2431=VECTOR ( 'NONE', #73815, 1000.000000000000114 ) ;
#2435=CARTESIAN_POINT ( 'NONE',  ( 15.00000000000000000, 5.835314593368470248, -22.81335362449854642 ) ) ;
#2436=DIRECTION ( 'NONE',  ( 0.000000000000000000, 0.000000000000000000, -1.000000000000000000 ) ) ;
#2437=CARTESIAN_POINT ( 'NONE',  ( 11.99999999999999822, -77.32052557432845674, 5.256550761632577284 ) ) ;
#2440=CYLINDRICAL_SURFACE ( 'NONE', #37531, 31.99999999999998579 ) ;
#2444=CIRCLE ( 'NONE', #39649, 82.00000000000000000 ) ;
#2460=CYLINDRICAL_SURFACE ( 'NONE', #18814, 31.99999999999998579 ) ;
#2464=DIRECTION ( 'NONE',  ( -1.000000000000000000, 0.000000000000000000, -0.000000000000000000 ) ) ;
#2477=ORIENTED_EDGE ( 'NONE', *, *, #33420, .F. ) ;
#2496=DIRECTION ( 'NONE',  ( -1.000000000000000000, 0.000000000000000000, 0.000000000000000000 ) ) ;
#2500=VECTOR ( 'NONE', #40079, 1000.000000000000000 ) ;
#2506=CYLINDRICAL_SURFACE ( 'NONE', #25732, 31.99999999999998579 ) ;
#2510=AXIS2_PLACEMENT_3D ( 'NONE', #6403, #24066, #424 ) ;
#2511=EDGE_CURVE ( 'NONE', #58816, #26361, #8429, .T. ) ;
#2513=FACE_OUTER_BOUND ( 'NONE', #69564, .T. ) ;
#2515=ADVANCED_FACE ( 'NONE', ( #69504 ), #40946, .T. ) ;
#2527=FILL_AREA_STYLE ('',( #11610 ) ) ;
#2528=ORIENTED_EDGE ( 'NONE', *, *, #51579, .T. ) ;
#2531=CIRCLE ( 'NONE', #34844, 31.99999999999998934 ) ;
#2532=CARTESIAN_POINT ( 'NONE',  ( 11.99999999999999822, -23.16143007188376757, -73.95703589263997912 ) ) ;
#2533=CIRCLE ( 'NONE', #38549, 77.49899999999999523 ) ;
#2535=EDGE_CURVE ( 'NONE', #57809, #63132, #58221, .T. ) ;
#2536=VERTEX_POINT ( 'NONE', #2230 ) ;
#2537=DIRECTION ( 'NONE',  ( 0.000000000000000000, -0.9510565162951510887, 0.3090169943749551673 ) ) ;
#2548=ORIENTED_EDGE ( 'NONE', *, *, #44102, .T. ) ;
#2551=CIRCLE ( 'NONE', #3759, 77.49899999999999523 ) ;
#2552=AXIS2_PLACEMENT_3D ( 'NONE', #71387, #31913, #19889 ) ;
#2566=LINE ( 'NONE', #17135, #41037 ) ;
#2567=DIRECTION ( 'NONE',  ( 0.000000000000000000, 0.8910065241883690090, -0.4539904997395446395 ) ) ;
#2580=VERTEX_POINT ( 'NONE', #42784 ) ;
#2586=VECTOR ( 'NONE', #71315, 1000.000000000000000 ) ;
#2594=ADVANCED_FACE ( 'NONE', ( #67193 ), #3694, .T. ) ;
#2605=AXIS2_PLACEMENT_3D ( 'NONE', #24717, #8544, #31459 ) ;
#2621=FACE_OUTER_BOUND ( 'NONE', #36232, .T. ) ;
#2628=CARTESIAN_POINT ( 'NONE',  ( 12.00000000000000000, -25.60904388321925040, -6.976881207771167048 ) ) ;
#2632=AXIS2_PLACEMENT_3D ( 'NONE', #51171, #15859, #38422 ) ;
#2633=DIRECTION ( 'NONE',  ( -1.000000000000000000, -0.000000000000000000, -0.000000000000000000 ) ) ;
#2643=ORIENTED_EDGE ( 'NONE', *, *, #20449, .F. ) ;
#2651=CIRCLE ( 'NONE', #54248, 31.99999999999998579 ) ;
#2656=CARTESIAN_POINT ( 'NONE',  ( 11.99999999999999822, 39.78640506895698792, -66.50666863321958999 ) ) ;
#2660=VERTEX_POINT ( 'NONE', #14949 ) ;
#2661=CARTESIAN_POINT ( 'NONE',  ( 11.99999999999999822, -76.66974797899844418, 11.30684508768314522 ) ) ;
#2664=CARTESIAN_POINT ( 'NONE',  ( 11.99999999999999822, 33.71516098798849015, -74.74816331893393340 ) ) ;
#2668=DIRECTION ( 'NONE',  ( -1.000000000000000000, 0.000000000000000000, 0.000000000000000000 ) ) ;
#2681=DIRECTION ( 'NONE',  ( -1.000000000000000000, -0.000000000000000000, -0.000000000000000000 ) ) ;
#2686=CIRCLE ( 'NONE', #44672, 77.49899999999998101 ) ;
#2687=CYLINDRICAL_SURFACE ( 'NONE', #59335, 31.99999999999998579 ) ;
#2691=CIRCLE ( 'NONE', #17031, 31.99999999999998579 ) ;
#2694=ADVANCED_FACE ( 'NONE', ( #32965 ), #8941, .F. ) ;
#2695=AXIS2_PLACEMENT_3D ( 'NONE', #30078, #3029, #35711 ) ;
#2697=ADVANCED_FACE ( 'NONE', ( #60457 ), #31858, .T. ) ;
#2710=CARTESIAN_POINT ( 'NONE',  ( 5.999999999999999112, 64.81221759200415988, -50.23322058963276504 ) ) ;
#2713=ORIENTED_EDGE ( 'NONE', *, *, #22413, .F. ) ;
#2719=FACE_OUTER_BOUND ( 'NONE', #6414, .T. ) ;
#2720=DIRECTION ( 'NONE',  ( 0.000000000000000000, 0.3090169943749410675, 0.9510565162951556406 ) ) ;
#2722=DIRECTION ( 'NONE',  ( -0.000000000000000000, 0.8090169943749503378, 0.5877852522924690293 ) ) ;
#2723=VERTEX_POINT ( 'NONE', #9301 ) ;
#2725=CARTESIAN_POINT ( 'NONE',  ( 0.000000000000000000, 66.50666863322055633, -39.78640506895536078 ) ) ;
#2739=CARTESIAN_POINT ( 'NONE',  ( 11.99999999999999822, 0.000000000000000000, 0.000000000000000000 ) ) ;
#2741=EDGE_CURVE ( 'NONE', #32448, #64295, #40471, .T. ) ;
#2742=DIRECTION ( 'NONE',  ( -1.000000000000000000, 0.000000000000000000, 0.000000000000000000 ) ) ;
#2748=ORIENTED_EDGE ( 'NONE', *, *, #8772, .F. ) ;
#2751=EDGE_LOOP ( 'NONE', ( #12229, #62623, #61997, #60581 ) ) ;
#2756=DIRECTION ( 'NONE',  ( 0.000000000000000000, 0.000000000000000000, 1.000000000000000000 ) ) ;
#2763=ORIENTED_EDGE ( 'NONE', *, *, #29843, .F. ) ;
#2766=DIRECTION ( 'NONE',  ( -1.000000000000000000, -0.000000000000000000, 0.000000000000000000 ) ) ;
#2772=ORIENTED_EDGE ( 'NONE', *, *, #11899, .F. ) ;
#2774=DIRECTION ( 'NONE',  ( -0.000000000000000000, 0.1045284632676569680, 0.9945218953682730678 ) ) ;
#2777=DIRECTION ( 'NONE',  ( -1.000000000000000000, -0.000000000000000000, 0.000000000000000000 ) ) ;
#2780=EDGE_CURVE ( 'NONE', #26458, #72049, #50651, .T. ) ;
#2786=DIRECTION ( 'NONE',  ( -1.000000000000000000, -0.000000000000000000, 0.000000000000000000 ) ) ;
#2790=CARTESIAN_POINT ( 'NONE',  ( 11.99999999999999822, -77.49459641780886443, -0.8261519478439277586 ) ) ;
#2791=AXIS2_PLACEMENT_3D ( 'NONE', #23869, #17485, #40412 ) ;
#2797=ORIENTED_EDGE ( 'NONE', *, *, #40085, .T. ) ;
#2803=ORIENTED_EDGE ( 'NONE', *, *, #25974, .F. ) ;
#2804=VERTEX_POINT ( 'NONE', #10414 ) ;
#2807=DIRECTION ( 'NONE',  ( 0.000000000000000000, 0.000000000000000000, 1.000000000000000000 ) ) ;
#2814=ORIENTED_EDGE ( 'NONE', *, *, #59753, .T. ) ;
#2817=FACE_OUTER_BOUND ( 'NONE', #24401, .T. ) ;
#2820=DIRECTION ( 'NONE',  ( 0.000000000000000000, -0.9969173337331287410, 0.07845909572783489605 ) ) ;
#2828=EDGE_CURVE ( 'NONE', #28379, #23563, #72941, .T. ) ;
#2829=DIRECTION ( 'NONE',  ( 0.000000000000000000, 0.07845909572783793529, 0.9969173337331285190 ) ) ;
#2830=AXIS2_PLACEMENT_3D ( 'NONE', #11877, #46474, #57763 ) ;
#2835=LINE ( 'NONE', #8064, #42152 ) ;
#2843=DIRECTION ( 'NONE',  ( -1.000000000000000000, 0.000000000000000000, -0.000000000000000000 ) ) ;
#2846=ORIENTED_EDGE ( 'NONE', *, *, #65954, .F. ) ;
#2848=DIRECTION ( 'NONE',  ( 0.000000000000000000, 0.2334453638559058908, -0.9723699203976764460 ) ) ;
#2851=DIRECTION ( 'NONE',  ( -1.000000000000000000, -0.000000000000000000, 0.000000000000000000 ) ) ;
#2852=CARTESIAN_POINT ( 'NONE',  ( 11.99999999999999822, -70.52718814184240159, -26.02418014898383802 ) ) ;
#2856=CIRCLE ( 'NONE', #36460, 31.99999999999998579 ) ;
#2858=DIRECTION ( 'NONE',  ( 0.000000000000000000, 0.8910065241883655673, 0.4539904997395510233 ) ) ;
#2859=DIRECTION ( 'NONE',  ( -1.000000000000000000, 0.000000000000000000, 0.000000000000000000 ) ) ;
#2860=CARTESIAN_POINT ( 'NONE',  ( 0.000000000000000000, 71.87247863392413194, 39.47590169984871267 ) ) ;
#2872=CARTESIAN_POINT ( 'NONE',  ( 0.000000000000000000, 81.90746397400393164, -3.894527615416979671 ) ) ;
#2876=ORIENTED_EDGE ( 'NONE', *, *, #65855, .F. ) ;
#2881=CIRCLE ( 'NONE', #62941, 82.00000000000000000 ) ;
#2893=CARTESIAN_POINT ( 'NONE',  ( 15.00000000000000000, 16.83928648764922542, -16.46020748918050458 ) ) ;
#2904=CIRCLE ( 'NONE', #66529, 77.49900000000000944 ) ;
#2907=DIRECTION ( 'NONE',  ( -1.000000000000000000, 0.000000000000000000, 0.000000000000000000 ) ) ;
#2909=ADVANCED_FACE ( 'NONE', ( #9066 ), #16103, .T. ) ;
#2911=CARTESIAN_POINT ( 'NONE',  ( 0.000000000000000000, 75.11725578898467859, 2.956366410620910656 ) ) ;
#2912=ORIENTED_EDGE ( 'NONE', *, *, #47229, .F. ) ;
#2918=ORIENTED_EDGE ( 'NONE', *, *, #54166, .F. ) ;
#2920=LINE ( 'NONE', #26550, #46624 ) ;
#2921=CARTESIAN_POINT ( 'NONE',  ( 0.000000000000000000, 24.73286445877808148, -73.44644590900034586 ) ) ;
#2923=ADVANCED_FACE ( 'NONE', ( #4474 ), #17220, .T. ) ;
#2932=AXIS2_PLACEMENT_3D ( 'NONE', #48759, #2934, #20926 ) ;
#2934=DIRECTION ( 'NONE',  ( -1.000000000000000000, 0.000000000000000000, 0.000000000000000000 ) ) ;
#2939=ADVANCED_FACE ( 'NONE', ( #73608 ), #33377, .T. ) ;
#2943=CIRCLE ( 'NONE', #30475, 77.49899999999999523 ) ;
#2952=DIRECTION ( 'NONE',  ( 0.000000000000000000, 0.8660254037844363761, -0.5000000000000039968 ) ) ;
#2955=CIRCLE ( 'NONE', #65395, 31.99999999999998579 ) ;
#2972=ORIENTED_EDGE ( 'NONE', *, *, #41908, .F. ) ;
#2980=ORIENTED_EDGE ( 'NONE', *, *, #14651, .T. ) ;
#2981=EDGE_CURVE ( 'NONE', #67992, #45327, #28576, .T. ) ;
#2984=ORIENTED_EDGE ( 'NONE', *, *, #55790, .F. ) ;
#2987=ADVANCED_FACE ( 'NONE', ( #60589 ), #28121, .T. ) ;
#2988=DIRECTION ( 'NONE',  ( 0.000000000000000000, -0.5224985647159380298, -0.8526401643540988395 ) ) ;
#2998=ORIENTED_EDGE ( 'NONE', *, *, #892, .F. ) ;
#3006=CARTESIAN_POINT ( 'NONE',  ( 11.99999999999999822, -51.03279382321125723, 55.19960302592048862 ) ) ;
#3008=FACE_OUTER_BOUND ( 'NONE', #28657, .T. ) ;
#3014=CARTESIAN_POINT ( 'NONE',  ( 15.00000000000000000, -4.261787119644963262, 26.19803753235780164 ) ) ;
#3018=VERTEX_POINT ( 'NONE', #39415 ) ;
#3019=CARTESIAN_POINT ( 'NONE',  ( 6.000000000000000000, 22.90783923731629201, 78.73519480814962890 ) ) ;
#3021=DIRECTION ( 'NONE',  ( 0.000000000000000000, 0.000000000000000000, 1.000000000000000000 ) ) ;
#3023=CYLINDRICAL_SURFACE ( 'NONE', #67196, 82.00000000000000000 ) ;
#3028=CARTESIAN_POINT ( 'NONE',  ( 11.99999999999999822, -49.70050353004932475, 59.46389618801947563 ) ) ;
#3029=DIRECTION ( 'NONE',  ( -1.000000000000000000, 0.000000000000000000, -0.000000000000000000 ) ) ;
#3031=CARTESIAN_POINT ( 'NONE',  ( 0.000000000000000000, 0.000000000000000000, 0.000000000000000000 ) ) ;
#3043=DIRECTION ( 'NONE',  ( -1.000000000000000000, 0.000000000000000000, 0.000000000000000000 ) ) ;
#3052=CIRCLE ( 'NONE', #27235, 77.49900000000000944 ) ;
#3053=CARTESIAN_POINT ( 'NONE',  ( 0.000000000000000000, 0.000000000000000000, 0.000000000000000000 ) ) ;
#3058=CIRCLE ( 'NONE', #6632, 31.99999999999998579 ) ;
#3059=AXIS2_PLACEMENT_3D ( 'NONE', #3031, #25922, #60523 ) ;
#3070=ADVANCED_FACE ( 'NONE', ( #40901 ), #35979, .T. ) ;
#3076=VECTOR ( 'NONE', #65996, 1000.000000000000000 ) ;
#3085=ORIENTED_EDGE ( 'NONE', *, *, #72418, .F. ) ;
#3089=ORIENTED_EDGE ( 'NONE', *, *, #20403, .T. ) ;
#3093=AXIS2_PLACEMENT_3D ( 'NONE', #6227, #58442, #35148 ) ;
#3094=DIRECTION ( 'NONE',  ( -1.000000000000000000, -0.000000000000000000, -0.000000000000000000 ) ) ;
#3095=ORIENTED_EDGE ( 'NONE', *, *, #27938, .T. ) ;
#3106=ORIENTED_EDGE ( 'NONE', *, *, #7489, .T. ) ;
#3110=LINE ( 'NONE', #13974, #72763 ) ;
#3117=EDGE_LOOP ( 'NONE', ( #50067, #147, #54726, #4155 ) ) ;
#3120=EDGE_LOOP ( 'NONE', ( #22259, #41839, #68535, #67491 ) ) ;
#3138=CARTESIAN_POINT ( 'NONE',  ( 15.00000000000000000, 20.85821328998756385, 10.92862929874494249 ) ) ;
#3143=ORIENTED_EDGE ( 'NONE', *, *, #55555, .T. ) ;
#3145=DIRECTION ( 'NONE',  ( -1.000000000000000000, 0.000000000000000000, 0.000000000000000000 ) ) ;
#3151=DIRECTION ( 'NONE',  ( -1.000000000000000000, -0.000000000000000000, -0.000000000000000000 ) ) ;
#3156=CARTESIAN_POINT ( 'NONE',  ( 11.99999999999999822, -31.47745569255092235, -68.26794271651296242 ) ) ;
#3163=EDGE_CURVE ( 'NONE', #24796, #40037, #29745, .T. ) ;
#3165=CIRCLE ( 'NONE', #12728, 31.99999999999998579 ) ;
#3172=ORIENTED_EDGE ( 'NONE', *, *, #71341, .F. ) ;
#3177=ORIENTED_EDGE ( 'NONE', *, *, #12405, .T. ) ;
#3186=DIRECTION ( 'NONE',  ( -1.000000000000000000, -0.000000000000000000, -0.000000000000000000 ) ) ;
#3189=CYLINDRICAL_SURFACE ( 'NONE', #48045, 31.99999999999998579 ) ;
#3200=CARTESIAN_POINT ( 'NONE',  ( 11.99999999999999822, 0.000000000000000000, 0.000000000000000000 ) ) ;
#3203=CARTESIAN_POINT ( 'NONE',  ( 5.999999999999999112, 56.15606465354958488, 59.75363087400094741 ) ) ;
#3208=ORIENTED_EDGE ( 'NONE', *, *, #14740, .F. ) ;
#3220=CARTESIAN_POINT ( 'NONE',  ( -10.00000000000000000, 0.000000000000000000, 0.000000000000000000 ) ) ;
#3236=ORIENTED_EDGE ( 'NONE', *, *, #70742, .T. ) ;
#3245=DIRECTION ( 'NONE',  ( -1.000000000000000000, -0.000000000000000000, -0.000000000000000000 ) ) ;
#3258=AXIS2_PLACEMENT_3D ( 'NONE', #65054, #2668, #47740 ) ;
#3263=EDGE_LOOP ( 'NONE', ( #11188, #40862, #20039, #22412 ) ) ;
#3265=ORIENTED_EDGE ( 'NONE', *, *, #71338, .T. ) ;
#3270=CIRCLE ( 'NONE', #34469, 77.49899999999999523 ) ;
#3297=DIRECTION ( 'NONE',  ( 0.000000000000000000, 0.000000000000000000, 1.000000000000000000 ) ) ;
#3313=DIRECTION ( 'NONE',  ( -1.000000000000000000, 0.000000000000000000, -0.000000000000000000 ) ) ;
#3319=AXIS2_PLACEMENT_3D ( 'NONE', #9727, #33771, #67615 ) ;
#3324=EDGE_CURVE ( 'NONE', #50948, #41513, #8535, .T. ) ;
#3336=AXIS2_PLACEMENT_3D ( 'NONE', #19855, #26977, #20223 ) ;
#3337=ORIENTED_EDGE ( 'NONE', *, *, #58501, .T. ) ;
#3344=EDGE_CURVE ( 'NONE', #24268, #66486, #2920, .T. ) ;
#3347=ORIENTED_EDGE ( 'NONE', *, *, #60288, .F. ) ;
#3351=ORIENTED_EDGE ( 'NONE', *, *, #14574, .T. ) ;
#3352=DIRECTION ( 'NONE',  ( -1.000000000000000000, 0.000000000000000000, -0.000000000000000000 ) ) ;
#3358=ORIENTED_EDGE ( 'NONE', *, *, #17803, .T. ) ;
#3363=CYLINDRICAL_SURFACE ( 'NONE', #39251, 77.49899999999999523 ) ;
#3373=CIRCLE ( 'NONE', #47726, 31.99999999999998934 ) ;
#3374=ORIENTED_EDGE ( 'NONE', *, *, #72333, .T. ) ;
#3376=CARTESIAN_POINT ( 'NONE',  ( 0.000000000000000000, 10.30890764327382136, 81.34940948281339956 ) ) ;
#3377=CARTESIAN_POINT ( 'NONE',  ( 11.99999999999999822, -63.18004540532995605, -44.88180994100445531 ) ) ;
#3387=CIRCLE ( 'NONE', #33341, 77.49900000000000944 ) ;
#3388=CARTESIAN_POINT ( 'NONE',  ( 6.000000000000000000, 76.69515212746016175, 29.01471420065590578 ) ) ;
#3397=CARTESIAN_POINT ( 'NONE',  ( 15.00000000000000000, 20.85821328998741109, -10.92862929874522671 ) ) ;
#3398=CYLINDRICAL_SURFACE ( 'NONE', #36230, 82.00000000000000000 ) ;
#3403=EDGE_CURVE ( 'NONE', #68341, #45880, #56231, .T. ) ;
#3404=PLANE ( 'NONE',  #42489 ) ;
#3411=CARTESIAN_POINT ( 'NONE',  ( 6.000000000000000000, -29.01471420065616513, 76.69515212746007649 ) ) ;
#3412=EDGE_CURVE ( 'NONE', #5010, #3531, #52627, .T. ) ;
#3414=DIRECTION ( 'NONE',  ( -1.000000000000000000, -0.000000000000000000, -0.000000000000000000 ) ) ;
#3415=DIRECTION ( 'NONE',  ( 0.000000000000000000, 0.000000000000000000, 1.000000000000000000 ) ) ;
#3416=VECTOR ( 'NONE', #19366, 1000.000000000000000 ) ;
#3422=LINE ( 'NONE', #32695, #33508 ) ;
#3442=VERTEX_POINT ( 'NONE', #44225 ) ;
#3443=DIRECTION ( 'NONE',  ( -1.000000000000000000, 0.000000000000000000, 0.000000000000000000 ) ) ;
#3453=ORIENTED_EDGE ( 'NONE', *, *, #16539, .F. ) ;
#3457=VERTEX_POINT ( 'NONE', #22787 ) ;
#3473=CARTESIAN_POINT ( 'NONE',  ( 11.99999999999999822, 20.40083707022882820, 72.35432306680490910 ) ) ;
#3475=DIRECTION ( 'NONE',  ( -1.000000000000000000, 0.000000000000000000, 0.000000000000000000 ) ) ;
#3478=LINE ( 'NONE', #50793, #52891 ) ;
#3479=CIRCLE ( 'NONE', #59879, 31.99999999999998934 ) ;
#3493=EDGE_CURVE ( 'NONE', #57268, #14085, #39329, .T. ) ;
#3499=EDGE_CURVE ( 'NONE', #40964, #62894, #11121, .T. ) ;
#3500=LINE ( 'NONE', #62107, #44887 ) ;
#3504=DIRECTION ( 'NONE',  ( -1.000000000000000000, -0.000000000000000000, -0.000000000000000000 ) ) ;
#3513=CIRCLE ( 'NONE', #21504, 31.99999999999999289 ) ;
#3521=ORIENTED_EDGE ( 'NONE', *, *, #48324, .F. ) ;
#3524=CARTESIAN_POINT ( 'NONE',  ( 11.99999999999999822, 0.000000000000000000, 0.000000000000000000 ) ) ;
#3530=AXIS2_PLACEMENT_3D ( 'NONE', #73271, #61268, #55246 ) ;
#3531=VERTEX_POINT ( 'NONE', #17868 ) ;
#3533=CIRCLE ( 'NONE', #40765, 31.99999999999998579 ) ;
#3540=CYLINDRICAL_SURFACE ( 'NONE', #38042, 82.00000000000000000 ) ;
#3544=ORIENTED_EDGE ( 'NONE', *, *, #2065, .T. ) ;
#3548=AXIS2_PLACEMENT_3D ( 'NONE', #44001, #67298, #27055 ) ;
#3551=CARTESIAN_POINT ( 'NONE',  ( 11.99999999999999822, -6.903761155837269570, -77.19088730480530103 ) ) ;
#3552=CARTESIAN_POINT ( 'NONE',  ( 11.99999999999999822, 0.000000000000000000, 0.000000000000000000 ) ) ;
#3564=PLANE ( 'NONE',  #49057 ) ;
#3579=CARTESIAN_POINT ( 'NONE',  ( 0.000000000000000000, 2.946379043147425492, -75.11764819372145041 ) ) ;
#3580=DIRECTION ( 'NONE',  ( -1.000000000000000000, -0.000000000000000000, 0.000000000000000000 ) ) ;
#3591=CARTESIAN_POINT ( 'NONE',  ( 11.99999999999999822, 26.01480285779837232, 70.53064760720326376 ) ) ;
#3605=VECTOR ( 'NONE', #35262, 1000.000000000000000 ) ;
#3616=CARTESIAN_POINT ( 'NONE',  ( 11.99999999999999822, 0.000000000000000000, 0.000000000000000000 ) ) ;
#3626=CARTESIAN_POINT ( 'NONE',  ( 11.99999999999999822, -5.256550761633395297, 77.32052557432841411 ) ) ;
#3632=VERTEX_POINT ( 'NONE', #64117 ) ;
#3641=ORIENTED_EDGE ( 'NONE', *, *, #43555, .F. ) ;
#3651=ADVANCED_FACE ( 'NONE', ( #63376 ), #264, .F. ) ;
#3654=CARTESIAN_POINT ( 'NONE',  ( 11.99999999999999822, 65.59268652807263322, -36.72794159290169347 ) ) ;
#3656=ORIENTED_EDGE ( 'NONE', *, *, #33586, .T. ) ;
#3661=DIRECTION ( 'NONE',  ( 0.000000000000000000, 0.8660254037844432595, 0.4999999999999919509 ) ) ;
#3663=EDGE_LOOP ( 'NONE', ( #30039, #23208, #71126, #73318 ) ) ;
#3667=CIRCLE ( 'NONE', #45681, 31.99999999999998934 ) ;
#3672=VERTEX_POINT ( 'NONE', #7338 ) ;
#3678=CARTESIAN_POINT ( 'NONE',  ( 0.000000000000000000, 0.000000000000000000, 0.000000000000000000 ) ) ;
#3680=CARTESIAN_POINT ( 'NONE',  ( 11.99999999999999822, 0.000000000000000000, 0.000000000000000000 ) ) ;
#3689=ORIENTED_EDGE ( 'NONE', *, *, #67565, .T. ) ;
#3691=CIRCLE ( 'NONE', #45707, 31.99999999999998579 ) ;
#3692=CARTESIAN_POINT ( 'NONE',  ( 12.00000000000000000, -20.55727247249725664, 16.78983467731313084 ) ) ;
#3693=VECTOR ( 'NONE', #45817, 1000.000000000000114 ) ;
#3694=CYLINDRICAL_SURFACE ( 'NONE', #11424, 31.99999999999998579 ) ;
#3696=EDGE_CURVE ( 'NONE', #27913, #12388, #53560, .T. ) ;
#3697=VERTEX_POINT ( 'NONE', #71950 ) ;
#3701=FACE_OUTER_BOUND ( 'NONE', #71447, .T. ) ;
#3703=CIRCLE ( 'NONE', #13285, 31.99999999999999289 ) ;
#3708=VECTOR ( 'NONE', #36218, 1000.000000000000000 ) ;
#3710=ORIENTED_EDGE ( 'NONE', *, *, #37785, .T. ) ;
#3713=DIRECTION ( 'NONE',  ( -1.000000000000000000, 0.000000000000000000, 0.000000000000000000 ) ) ;
#3719=ORIENTED_EDGE ( 'NONE', *, *, #48491, .F. ) ;
#3720=CARTESIAN_POINT ( 'NONE',  ( 11.99999999999999822, -65.64334221924937651, 41.19522573413711797 ) ) ;
#3736=FACE_OUTER_BOUND ( 'NONE', #44081, .T. ) ;
#3740=ORIENTED_EDGE ( 'NONE', *, *, #40999, .T. ) ;
#3741=ORIENTED_EDGE ( 'NONE', *, *, #2780, .T. ) ;
#3742=ADVANCED_FACE ( 'NONE', ( #31358 ), #59577, .F. ) ;
#3744=EDGE_CURVE ( 'NONE', #6114, #3457, #7316, .T. ) ;
#3749=CARTESIAN_POINT ( 'NONE',  ( 0.000000000000000000, 0.000000000000000000, 0.000000000000000000 ) ) ;
#3751=ORIENTED_EDGE ( 'NONE', *, *, #27938, .F. ) ;
#3758=CARTESIAN_POINT ( 'NONE',  ( 11.99999999999999822, 0.000000000000000000, 0.000000000000000000 ) ) ;
#3759=AXIS2_PLACEMENT_3D ( 'NONE', #73157, #68280, #22036 ) ;
#3767=CARTESIAN_POINT ( 'NONE',  ( 15.00000000000000000, -0.9646360437375368635, -23.52805723605589705 ) ) ;
#3771=CARTESIAN_POINT ( 'NONE',  ( 0.000000000000000000, 75.54627589209944460, 17.28742895386110945 ) ) ;
#3779=EDGE_CURVE ( 'NONE', #18854, #33851, #58952, .T. ) ;
#3780=PRODUCT ( 'slow gear_ISO - Spur gear 2M 80T 20PA 12FW ---S80A75H50L38.0N', 'slow gear_ISO - Spur gear 2M 80T 20PA 12FW ---S80A75H50L38.0N', '', ( #46341 ) ) ;
#3781=ADVANCED_FACE ( 'NONE', ( #65225 ), #65592, .T. ) ;
#3782=CARTESIAN_POINT ( 'NONE',  ( 11.99999999999999822, 24.73286445877808148, -73.44644590900034586 ) ) ;
#3783=LINE ( 'NONE', #37976, #49067 ) ;
#3787=CIRCLE ( 'NONE', #48209, 82.00000000000000000 ) ;
#3792=DIRECTION ( 'NONE',  ( -1.000000000000000000, 0.000000000000000000, -0.000000000000000000 ) ) ;
#3803=CIRCLE ( 'NONE', #62628, 77.49899999999999523 ) ;
#3808=DIRECTION ( 'NONE',  ( 0.000000000000000000, 0.000000000000000000, -1.000000000000000000 ) ) ;
#3809=AXIS2_PLACEMENT_3D ( 'NONE', #14565, #38996, #10411 ) ;
#3810=VERTEX_POINT ( 'NONE', #20464 ) ;
#3812=DIRECTION ( 'NONE',  ( 0.000000000000000000, 0.000000000000000000, 1.000000000000000000 ) ) ;
#3814=CARTESIAN_POINT ( 'NONE',  ( 11.99999999999999822, 0.000000000000000000, 0.000000000000000000 ) ) ;
#3818=EDGE_CURVE ( 'NONE', #65052, #23772, #2835, .T. ) ;
#3820=ORIENTED_EDGE ( 'NONE', *, *, #58000, .F. ) ;
#3826=ORIENTED_EDGE ( 'NONE', *, *, #48864, .F. ) ;
#3831=ORIENTED_EDGE ( 'NONE', *, *, #73557, .F. ) ;
#3840=ADVANCED_FACE ( 'NONE', ( #20076 ), #43030, .T. ) ;
#3844=CARTESIAN_POINT ( 'NONE',  ( 6.000000000000000000, -81.96053171279901051, -2.543863470249253300 ) ) ;
#3852=DIRECTION ( 'NONE',  ( -1.000000000000000000, -0.000000000000000000, -0.000000000000000000 ) ) ;
#3854=ADVANCED_FACE ( 'NONE', ( #5042 ), #21559, .T. ) ;
#3858=CARTESIAN_POINT ( 'NONE',  ( 11.99999999999999822, 0.000000000000000000, 0.000000000000000000 ) ) ;
#3861=DIRECTION ( 'NONE',  ( 0.000000000000000000, 0.000000000000000000, 1.000000000000000000 ) ) ;
#3862=EDGE_CURVE ( 'NONE', #60009, #42672, #36123, .T. ) ;
#3865=DIRECTION ( 'NONE',  ( 0.000000000000000000, 0.000000000000000000, -1.000000000000000000 ) ) ;
#3868=CIRCLE ( 'NONE', #26644, 77.49899999999999523 ) ;
#3869=FACE_OUTER_BOUND ( 'NONE', #27647, .T. ) ;
#3872=DIRECTION ( 'NONE',  ( 0.000000000000000000, 0.000000000000000000, 1.000000000000000000 ) ) ;
#3875=ORIENTED_EDGE ( 'NONE', *, *, #451, .F. ) ;
#3876=ADVANCED_FACE ( 'NONE', ( #55409 ), #15928, .T. ) ;
#3878=CARTESIAN_POINT ( 'NONE',  ( 11.99999999999999822, -51.03279382321048985, -55.19960302592120627 ) ) ;
#3879=FACE_OUTER_BOUND ( 'NONE', #30347, .T. ) ;
#3885=DIRECTION ( 'NONE',  ( 0.000000000000000000, 0.000000000000000000, 1.000000000000000000 ) ) ;
#3889=CIRCLE ( 'NONE', #45917, 82.00000000000000000 ) ;
#3905=VERTEX_POINT ( 'NONE', #51245 ) ;
#3911=EDGE_LOOP ( 'NONE', ( #5013, #19866, #17811, #55294 ) ) ;
#3916=ADVANCED_FACE ( 'NONE', ( #3932 ), #26829, .T. ) ;
#3927=UNCERTAINTY_MEASURE_WITH_UNIT (LENGTH_MEASURE( 1.000000000000000082E-05 ), #1311, 'distance_accuracy_value', 'NONE');
#3932=FACE_OUTER_BOUND ( 'NONE', #23383, .T. ) ;
#3934=DIRECTION ( 'NONE',  ( -1.000000000000000000, -0.000000000000000000, 0.000000000000000000 ) ) ;
#3945=CARTESIAN_POINT ( 'NONE',  ( 0.000000000000000000, -20.40083707022829174, -72.35432306680507963 ) ) ;
#3948=DIRECTION ( 'NONE',  ( 0.000000000000000000, 0.4539904997395477482, -0.8910065241883674547 ) ) ;
#3954=EDGE_CURVE ( 'NONE', #63285, #12380, #57771, .T. ) ;
#3957=AXIS2_PLACEMENT_3D ( 'NONE', #28761, #17850, #69726 ) ;
#3959=DIRECTION ( 'NONE',  ( 0.000000000000000000, -0.9238795325112906243, 0.3826834323650805114 ) ) ;
#3962=CARTESIAN_POINT ( 'NONE',  ( 5.999999999999999112, -60.67117009219097667, -55.16347631943106933 ) ) ;
#3963=CIRCLE ( 'NONE', #72358, 82.00000000000000000 ) ;
#3972=AXIS2_PLACEMENT_3D ( 'NONE', #23270, #45845, #62011 ) ;
#3976=DIRECTION ( 'NONE',  ( -1.000000000000000000, 0.000000000000000000, 0.000000000000000000 ) ) ;
#3985=CARTESIAN_POINT ( 'NONE',  ( 11.99999999999999822, 72.35160999960844208, -20.41045688087747223 ) ) ;
#3991=ORIENTED_EDGE ( 'NONE', *, *, #36938, .F. ) ;
#3995=ORIENTED_EDGE ( 'NONE', *, *, #69770, .T. ) ;
#3997=CARTESIAN_POINT ( 'NONE',  ( 11.99999999999999822, 0.000000000000000000, 0.000000000000000000 ) ) ;
#3998=CIRCLE ( 'NONE', #27967, 82.00000000000000000 ) ;
#4001=EDGE_CURVE ( 'NONE', #43677, #19971, #53038, .T. ) ;
#4002=LINE ( 'NONE', #31798, #68843 ) ;
#4004=FACE_OUTER_BOUND ( 'NONE', #70162, .T. ) ;
#4006=EDGE_CURVE ( 'NONE', #32135, #66160, #3787, .T. ) ;
#4019=DIRECTION ( 'NONE',  ( 0.000000000000000000, -0.3826834323650772363, -0.9238795325112919565 ) ) ;
#4021=FACE_OUTER_BOUND ( 'NONE', #13527, .T. ) ;
#4029=DIRECTION ( 'NONE',  ( -1.000000000000000000, -0.000000000000000000, -0.000000000000000000 ) ) ;
#4030=ORIENTED_EDGE ( 'NONE', *, *, #43706, .F. ) ;
#4031=ORIENTED_EDGE ( 'NONE', *, *, #58982, .F. ) ;
#4033=ADVANCED_FACE ( 'NONE', ( #64027 ), #24530, .T. ) ;
#4041=DIRECTION ( 'NONE',  ( 0.000000000000000000, 0.000000000000000000, 1.000000000000000000 ) ) ;
#4049=CARTESIAN_POINT ( 'NONE',  ( 11.99999999999999822, 0.000000000000000000, 0.000000000000000000 ) ) ;
#4055=CARTESIAN_POINT ( 'NONE',  ( 11.99999999999999822, -63.97538442413463855, 51.29473840253199057 ) ) ;
#4058=DIRECTION ( 'NONE',  ( 1.000000000000000000, -0.000000000000000000, -0.000000000000000000 ) ) ;
#4059=CIRCLE ( 'NONE', #20834, 82.00000000000000000 ) ;
#4061=VERTEX_POINT ( 'NONE', #34329 ) ;
#4062=DIRECTION ( 'NONE',  ( -1.000000000000000000, 0.000000000000000000, -0.000000000000000000 ) ) ;
#4064=CARTESIAN_POINT ( 'NONE',  ( 0.000000000000000000, 60.67117009219135326, 55.16347631943062169 ) ) ;
#4065=DIRECTION ( 'NONE',  ( 0.000000000000000000, 0.8910065241883691201, -0.4539904997395446951 ) ) ;
#4067=AXIS2_PLACEMENT_3D ( 'NONE', #69393, #57383, #35187 ) ;
#4076=CARTESIAN_POINT ( 'NONE',  ( 11.99999999999999822, -41.76106447765533147, 62.50884508063410294 ) ) ;
#4082=VECTOR ( 'NONE', #68738, 1000.000000000000000 ) ;
#4083=EDGE_CURVE ( 'NONE', #28695, #64186, #24225, .T. ) ;
#4084=EDGE_LOOP ( 'NONE', ( #40160, #53720, #50854, #26797 ) ) ;
#4088=LINE ( 'NONE', #55568, #41757 ) ;
#4091=ORIENTED_EDGE ( 'NONE', *, *, #34732, .T. ) ;
#4101=DIRECTION ( 'NONE',  ( 0.000000000000000000, 0.000000000000000000, 1.000000000000000000 ) ) ;
#4105=VERTEX_POINT ( 'NONE', #40718 ) ;
#4111=AXIS2_PLACEMENT_3D ( 'NONE', #65108, #1251, #1615 ) ;
#4121=VERTEX_POINT ( 'NONE', #36540 ) ;
#4132=AXIS2_PLACEMENT_3D ( 'NONE', #35377, #46656, #33892 ) ;
#4141=CARTESIAN_POINT ( 'NONE',  ( 0.000000000000000000, 0.000000000000000000, 0.000000000000000000 ) ) ;
#4144=DIRECTION ( 'NONE',  ( 1.000000000000000000, -0.000000000000000000, -0.000000000000000000 ) ) ;
#4147=EDGE_CURVE ( 'NONE', #15890, #15888, #57823, .T. ) ;
#4155=ORIENTED_EDGE ( 'NONE', *, *, #22922, .T. ) ;
#4173=CIRCLE ( 'NONE', #10114, 31.99999999999998224 ) ;
#4174=PLANE ( 'NONE',  #20075 ) ;
#4176=ORIENTED_EDGE ( 'NONE', *, *, #8054, .T. ) ;
#4177=DIRECTION ( 'NONE',  ( 0.000000000000000000, 0.8526401643540897357, 0.5224985647159527957 ) ) ;
#4179=CARTESIAN_POINT ( 'NONE',  ( 15.00000000000000000, -10.45096189432344502, -21.10159698893425784 ) ) ;
#4184=EDGE_LOOP ( 'NONE', ( #23491, #19316, #36047, #73859 ) ) ;
#4185=FACE_OUTER_BOUND ( 'NONE', #47158, .T. ) ;
#4186=EDGE_CURVE ( 'NONE', #55121, #39963, #53474, .T. ) ;
#4192=CARTESIAN_POINT ( 'NONE',  ( 11.99999999999999822, 77.32052557432841411, 5.256550761633121738 ) ) ;
#4209=LINE ( 'NONE', #56447, #25979 ) ;
#4212=CARTESIAN_POINT ( 'NONE',  ( 11.99999999999999822, 41.19522573413826194, -65.64334221924865176 ) ) ;
#4216=AXIS2_PLACEMENT_3D ( 'NONE', #73132, #22014, #26903 ) ;
#4219=CARTESIAN_POINT ( 'NONE',  ( 11.99999999999999822, 0.000000000000000000, 0.000000000000000000 ) ) ;
#4226=CIRCLE ( 'NONE', #33011, 31.99999999999998579 ) ;
#4230=DIRECTION ( 'NONE',  ( 0.000000000000000000, 0.3090169943749450088, -0.9510565162951544194 ) ) ;
#4236=ADVANCED_FACE ( 'NONE', ( #20368 ), #2010, .T. ) ;
#4238=ORIENTED_EDGE ( 'NONE', *, *, #26477, .F. ) ;
#4249=EDGE_CURVE ( 'NONE', #6916, #55524, #10947, .T. ) ;
#4250=CARTESIAN_POINT ( 'NONE',  ( 11.99999999999999822, -75.11764819372149304, 2.946379043146075905 ) ) ;
#4276=ORIENTED_EDGE ( 'NONE', *, *, #57134, .F. ) ;
#4281=EDGE_LOOP ( 'NONE', ( #54923, #43602, #71072, #26070 ) ) ;
#4291=CARTESIAN_POINT ( 'NONE',  ( 11.99999999999999822, 33.71516098798741012, 74.74816331893441657 ) ) ;
#4294=EDGE_CURVE ( 'NONE', #20558, #12759, #42209, .T. ) ;
#4302=DIRECTION ( 'NONE',  ( 0.000000000000000000, 0.9876883405951371042, 0.1564344650402346715 ) ) ;
#4304=DIRECTION ( 'NONE',  ( -1.000000000000000000, -0.000000000000000000, -0.000000000000000000 ) ) ;
#4309=CARTESIAN_POINT ( 'NONE',  ( 0.000000000000000000, 77.49459641780886443, 0.8261519478433866359 ) ) ;
#4311=ORIENTED_EDGE ( 'NONE', *, *, #64511, .T. ) ;
#4318=DIRECTION ( 'NONE',  ( -1.000000000000000000, -0.000000000000000000, -0.000000000000000000 ) ) ;
#4319=DIRECTION ( 'NONE',  ( 0.000000000000000000, 0.000000000000000000, 1.000000000000000000 ) ) ;
#4346=VECTOR ( 'NONE', #5332, 1000.000000000000000 ) ;
#4360=ORIENTED_EDGE ( 'NONE', *, *, #1175, .F. ) ;
#4364=FACE_OUTER_BOUND ( 'NONE', #32659, .T. ) ;
#4371=CARTESIAN_POINT ( 'NONE',  ( 0.000000000000000000, 74.74816331893477184, -33.71516098798660011 ) ) ;
#4376=DIRECTION ( 'NONE',  ( -1.000000000000000000, 0.000000000000000000, -0.000000000000000000 ) ) ;
#4385=CARTESIAN_POINT ( 'NONE',  ( 11.99999999999999822, 74.65491531819118620, -8.830959090342659579 ) ) ;
#4389=VERTEX_POINT ( 'NONE', #16960 ) ;
#4390=CARTESIAN_POINT ( 'NONE',  ( 15.00000000000000000, -10.45096189432344502, -21.10159698893425784 ) ) ;
#4391=CARTESIAN_POINT ( 'NONE',  ( 11.99999999999999822, -18.89407956138310496, 75.16055320797023853 ) ) ;
#4394=AXIS2_PLACEMENT_3D ( 'NONE', #51611, #62925, #46347 ) ;
#4398=CARTESIAN_POINT ( 'NONE',  ( 11.99999999999999822, 50.95692526931329525, 58.39081064771768581 ) ) ;
#4399=AXIS2_PLACEMENT_3D ( 'NONE', #29425, #547, #70020 ) ;
#4400=AXIS2_PLACEMENT_3D ( 'NONE', #40542, #40180, #57473 ) ;
#4402=CYLINDRICAL_SURFACE ( 'NONE', #55754, 77.49899999999999523 ) ;
#4404=ORIENTED_EDGE ( 'NONE', *, *, #60095, .T. ) ;
#4409=AXIS2_PLACEMENT_3D ( 'NONE', #48070, #48796, #60831 ) ;
#4418=DIRECTION ( 'NONE',  ( 0.000000000000000000, 0.000000000000000000, 1.000000000000000000 ) ) ;
#4421=ORIENTED_EDGE ( 'NONE', *, *, #49055, .F. ) ;
#4424=CYLINDRICAL_SURFACE ( 'NONE', #25131, 31.99999999999998579 ) ;
#4428=VERTEX_POINT ( 'NONE', #41008 ) ;
#4434=EDGE_CURVE ( 'NONE', #35261, #72991, #20612, .T. ) ;
#4440=ORIENTED_EDGE ( 'NONE', *, *, #14063, .F. ) ;
#4442=EDGE_CURVE ( 'NONE', #41319, #32106, #57870, .T. ) ;
#4461=VERTEX_POINT ( 'NONE', #23702 ) ;
#4469=EDGE_LOOP ( 'NONE', ( #27550, #28544, #35900, #23981 ) ) ;
#4470=CARTESIAN_POINT ( 'NONE',  ( 0.000000000000000000, 35.91791733033570466, -68.67312586194960033 ) ) ;
#4474=FACE_OUTER_BOUND ( 'NONE', #12027, .T. ) ;
#4475=DIRECTION ( 'NONE',  ( -1.000000000000000000, -0.000000000000000000, -0.000000000000000000 ) ) ;
#4478=ORIENTED_EDGE ( 'NONE', *, *, #7311, .F. ) ;
#4479=DIRECTION ( 'NONE',  ( -1.000000000000000000, -0.000000000000000000, -0.000000000000000000 ) ) ;
#4481=ORIENTED_EDGE ( 'NONE', *, *, #4684, .T. ) ;
#4487=VERTEX_POINT ( 'NONE', #46638 ) ;
#4491=AXIS2_PLACEMENT_3D ( 'NONE', #368, #13797, #36740 ) ;
#4493=CARTESIAN_POINT ( 'NONE',  ( 0.000000000000000000, -75.16055320797016748, -18.89407956138335365 ) ) ;
#4495=AXIS2_PLACEMENT_3D ( 'NONE', #43658, #38374, #61315 ) ;
#4496=CARTESIAN_POINT ( 'NONE',  ( 11.99999999999999822, -28.89263327155796190, 71.91182617369179297 ) ) ;
#4502=CARTESIAN_POINT ( 'NONE',  ( -10.00000000000000000, 0.000000000000000000, 0.000000000000000000 ) ) ;
#4505=LINE ( 'NONE', #71776, #60422 ) ;
#4509=LINE ( 'NONE', #17258, #65123 ) ;
#4511=CARTESIAN_POINT ( 'NONE',  ( 11.99999999999999822, -31.47745569255189224, 68.26794271651249346 ) ) ;
#4522=EDGE_CURVE ( 'NONE', #21534, #43826, #73468, .T. ) ;
#4523=DIRECTION ( 'NONE',  ( 0.000000000000000000, 0.000000000000000000, 1.000000000000000000 ) ) ;
#4540=AXIS2_PLACEMENT_3D ( 'NONE', #9660, #43887, #60438 ) ;
#4543=EDGE_LOOP ( 'NONE', ( #52155, #56620, #25910, #2241 ) ) ;
#4553=DIRECTION ( 'NONE',  ( 0.000000000000000000, 0.000000000000000000, -1.000000000000000000 ) ) ;
#4575=VECTOR ( 'NONE', #68501, 1000.000000000000000 ) ;
#4587=EDGE_LOOP ( 'NONE', ( #54556, #11819, #45649, #6919 ) ) ;
#4605=CIRCLE ( 'NONE', #29793, 77.49899999999999523 ) ;
#4611=ORIENTED_EDGE ( 'NONE', *, *, #21739, .T. ) ;
#4616=ORIENTED_EDGE ( 'NONE', *, *, #60012, .T. ) ;
#4618=DIRECTION ( 'NONE',  ( 0.000000000000000000, -0.1045284632676558301, -0.9945218953682731788 ) ) ;
#4623=CYLINDRICAL_SURFACE ( 'NONE', #45172, 77.49899999999999523 ) ;
#4632=VERTEX_POINT ( 'NONE', #53752 ) ;
#4634=ORIENTED_EDGE ( 'NONE', *, *, #42625, .T. ) ;
#4636=ORIENTED_EDGE ( 'NONE', *, *, #59330, .T. ) ;
#4651=ORIENTED_EDGE ( 'NONE', *, *, #73424, .F. ) ;
#4655=DIRECTION ( 'NONE',  ( -1.000000000000000000, -0.000000000000000000, 0.000000000000000000 ) ) ;
#4659=VECTOR ( 'NONE', #44360, 1000.000000000000000 ) ;
#4669=CARTESIAN_POINT ( 'NONE',  ( 11.99999999999999822, -8.830959090341869100, -74.65491531819127147 ) ) ;
#4672=DIRECTION ( 'NONE',  ( -1.000000000000000000, -0.000000000000000000, -0.000000000000000000 ) ) ;
#4678=VERTEX_POINT ( 'NONE', #32286 ) ;
#4681=EDGE_CURVE ( 'NONE', #590, #53279, #72233, .T. ) ;
#4684=EDGE_CURVE ( 'NONE', #28756, #67162, #44713, .T. ) ;
#4687=DIRECTION ( 'NONE',  ( -1.000000000000000000, 0.000000000000000000, 0.000000000000000000 ) ) ;
#4690=CARTESIAN_POINT ( 'NONE',  ( -10.00000000000000000, 0.000000000000000000, 0.000000000000000000 ) ) ;
#4707=EDGE_CURVE ( 'NONE', #53279, #27772, #48256, .T. ) ;
#4711=CARTESIAN_POINT ( 'NONE',  ( 11.99999999999999822, 0.000000000000000000, 0.000000000000000000 ) ) ;
#4712=ORIENTED_EDGE ( 'NONE', *, *, #4083, .F. ) ;
#4720=EDGE_LOOP ( 'NONE', ( #43881, #62723, #19486, #53336 ) ) ;
#4728=VECTOR ( 'NONE', #3792, 1000.000000000000000 ) ;
#4730=ORIENTED_EDGE ( 'NONE', *, *, #27899, .F. ) ;
#4738=CARTESIAN_POINT ( 'NONE',  ( 15.00000000000000000, -0.9646360437372099028, 23.52805723605590771 ) ) ;
#4745=ORIENTED_EDGE ( 'NONE', *, *, #22268, .T. ) ;
#4754=VERTEX_POINT ( 'NONE', #8999 ) ;
#4763=AXIS2_PLACEMENT_3D ( 'NONE', #43745, #73772, #33928 ) ;
#4765=AXIS2_PLACEMENT_3D ( 'NONE', #20948, #43172, #55168 ) ;
#4780=EDGE_CURVE ( 'NONE', #9094, #31764, #25449, .T. ) ;
#4794=LINE ( 'NONE', #56657, #38165 ) ;
#4801=CARTESIAN_POINT ( 'NONE',  ( 11.99999999999999822, 55.38113227695783536, 54.21277698773694453 ) ) ;
#4804=DIRECTION ( 'NONE',  ( -1.000000000000000000, -0.000000000000000000, -0.000000000000000000 ) ) ;
#4810=EDGE_CURVE ( 'NONE', #32525, #38945, #2686, .T. ) ;
#4814=AXIS2_PLACEMENT_3D ( 'NONE', #7524, #7885, #59036 ) ;
#4817=CARTESIAN_POINT ( 'NONE',  ( 0.000000000000000000, 36.72794159290241822, 65.59268652807223532 ) ) ;
#4825=FACE_OUTER_BOUND ( 'NONE', #45978, .T. ) ;
#4827=DIRECTION ( 'NONE',  ( -1.000000000000000000, 0.000000000000000000, 0.000000000000000000 ) ) ;
#4833=ORIENTED_EDGE ( 'NONE', *, *, #12635, .T. ) ;
#4838=AXIS2_PLACEMENT_3D ( 'NONE', #67813, #28317, #34336 ) ;
#4847=DIRECTION ( 'NONE',  ( 1.000000000000000000, -0.000000000000000000, -0.000000000000000000 ) ) ;
#4849=CARTESIAN_POINT ( 'NONE',  ( 5.999999999999999112, -74.74816331893453025, 33.71516098798714722 ) ) ;
#4851=CARTESIAN_POINT ( 'NONE',  ( 11.99999999999999822, -75.11725578898466438, -2.956366410621452001 ) ) ;
#4856=CARTESIAN_POINT ( 'NONE',  ( 0.000000000000000000, -65.64334221924882229, -41.19522573413803457 ) ) ;
#4857=CARTESIAN_POINT ( 'NONE',  ( 11.99999999999999822, 49.70050353004889132, 59.46389618801982380 ) ) ;
#4864=EDGE_CURVE ( 'NONE', #46823, #55642, #23619, .T. ) ;
#4865=ORIENTED_EDGE ( 'NONE', *, *, #70498, .T. ) ;
#4872=ORIENTED_EDGE ( 'NONE', *, *, #52524, .T. ) ;
#4876=FACE_OUTER_BOUND ( 'NONE', #11519, .T. ) ;
#4881=AXIS2_PLACEMENT_3D ( 'NONE', #69394, #17893, #8094 ) ;
#4883=VECTOR ( 'NONE', #50976, 1000.000000000000000 ) ;
#4887=DIRECTION ( 'NONE',  ( 0.000000000000000000, 0.7071067811865487940, -0.7071067811865462405 ) ) ;
#4893=DIRECTION ( 'NONE',  ( -1.000000000000000000, -0.000000000000000000, -0.000000000000000000 ) ) ;
#4901=DIRECTION ( 'NONE',  ( 0.000000000000000000, 0.000000000000000000, 1.000000000000000000 ) ) ;
#4905=PLANE ( 'NONE',  #40732 ) ;
#4907=LINE ( 'NONE', #33817, #54603 ) ;
#4920=ORIENTED_EDGE ( 'NONE', *, *, #54975, .T. ) ;
#4922=FACE_OUTER_BOUND ( 'NONE', #32370, .T. ) ;
#4927=VERTEX_POINT ( 'NONE', #40175 ) ;
#4929=ORIENTED_EDGE ( 'NONE', *, *, #41501, .T. ) ;
#4931=ORIENTED_EDGE ( 'NONE', *, *, #63199, .T. ) ;
#4934=ORIENTED_EDGE ( 'NONE', *, *, #4522, .F. ) ;
#4946=CIRCLE ( 'NONE', #70914, 31.99999999999998224 ) ;
#4947=LINE ( 'NONE', #11298, #56306 ) ;
#4955=ORIENTED_EDGE ( 'NONE', *, *, #72326, .F. ) ;
#4957=CARTESIAN_POINT ( 'NONE',  ( 0.000000000000000000, 36.73666225445988687, -65.58780272294035285 ) ) ;
#4959=FACE_OUTER_BOUND ( 'NONE', #13933, .T. ) ;
#4960=DIRECTION ( 'NONE',  ( -1.000000000000000000, 0.000000000000000000, 0.000000000000000000 ) ) ;
#4963=CARTESIAN_POINT ( 'NONE',  ( 0.000000000000000000, -81.34940948281328588, -10.30890764327469000 ) ) ;
#4970=CARTESIAN_POINT ( 'NONE',  ( 11.99999999999999822, 0.000000000000000000, 0.000000000000000000 ) ) ;
#4971=VERTEX_POINT ( 'NONE', #71213 ) ;
#4972=DIRECTION ( 'NONE',  ( 1.000000000000000000, 0.000000000000000000, 0.000000000000000000 ) ) ;
#4982=CARTESIAN_POINT ( 'NONE',  ( 11.99999999999999822, 60.67117009219215618, -55.16347631942976903 ) ) ;
#4985=LINE ( 'NONE', #62499, #73098 ) ;
#4993=ORIENTED_EDGE ( 'NONE', *, *, #43578, .F. ) ;
#4997=AXIS2_PLACEMENT_3D ( 'NONE', #59062, #13910, #7556 ) ;
#5002=FACE_OUTER_BOUND ( 'NONE', #67402, .T. ) ;
#5003=ORIENTED_EDGE ( 'NONE', *, *, #30145, .F. ) ;
#5009=EDGE_CURVE ( 'NONE', #36701, #2723, #3889, .T. ) ;
#5010=VERTEX_POINT ( 'NONE', #30999 ) ;
#5011=CYLINDRICAL_SURFACE ( 'NONE', #8326, 31.99999999999998579 ) ;
#5013=ORIENTED_EDGE ( 'NONE', *, *, #55166, .F. ) ;
#5019=ORIENTED_EDGE ( 'NONE', *, *, #55166, .T. ) ;
#5022=ORIENTED_EDGE ( 'NONE', *, *, #65799, .F. ) ;
#5031=DIRECTION ( 'NONE',  ( 0.000000000000000000, 0.000000000000000000, 1.000000000000000000 ) ) ;
#5036=ORIENTED_EDGE ( 'NONE', *, *, #11805, .T. ) ;
#5042=FACE_OUTER_BOUND ( 'NONE', #32724, .T. ) ;
#5049=VECTOR ( 'NONE', #15711, 1000.000000000000000 ) ;
#5050=CARTESIAN_POINT ( 'NONE',  ( 11.99999999999999822, -2.946379043145784582, -75.11764819372150725 ) ) ;
#5070=FACE_OUTER_BOUND ( 'NONE', #42634, .T. ) ;
#5071=DIRECTION ( 'NONE',  ( -1.000000000000000000, 0.000000000000000000, 0.000000000000000000 ) ) ;
#5074=VECTOR ( 'NONE', #17177, 1000.000000000000000 ) ;
#5078=VERTEX_POINT ( 'NONE', #37775 ) ;
#5089=CARTESIAN_POINT ( 'NONE',  ( 0.000000000000000000, 0.000000000000000000, 0.000000000000000000 ) ) ;
#5090=ORIENTED_EDGE ( 'NONE', *, *, #38272, .T. ) ;
#5095=CARTESIAN_POINT ( 'NONE',  ( 0.000000000000000000, 54.21277698773752007, -55.38113227695726692 ) ) ;
#5096=AXIS2_PLACEMENT_3D ( 'NONE', #32089, #26821, #2829 ) ;
#5105=DIRECTION ( 'NONE',  ( 0.000000000000000000, 0.000000000000000000, -1.000000000000000000 ) ) ;
#5110=ADVANCED_FACE ( 'NONE', ( #70853 ), #37024, .T. ) ;
#5111=ORIENTED_EDGE ( 'NONE', *, *, #27610, .F. ) ;
#5120=ORIENTED_EDGE ( 'NONE', *, *, #28333, .T. ) ;
#5131=CARTESIAN_POINT ( 'NONE',  ( 11.99999999999999822, 75.11764819372149304, 29.05362095685338275 ) ) ;
#5133=CARTESIAN_POINT ( 'NONE',  ( 11.99999999999999822, 39.78640506895698792, -66.50666863321958999 ) ) ;
#5134=DIRECTION ( 'NONE',  ( 0.000000000000000000, 0.9945218953682731788, -0.1045284632676558162 ) ) ;
#5140=AXIS2_PLACEMENT_3D ( 'NONE', #1694, #47512, #18198 ) ;
#5144=EDGE_CURVE ( 'NONE', #24191, #27546, #52352, .T. ) ;
#5145=DIRECTION ( 'NONE',  ( 0.000000000000000000, 0.000000000000000000, -1.000000000000000000 ) ) ;
#5154=CARTESIAN_POINT ( 'NONE',  ( 11.99999999999999822, 0.000000000000000000, 0.000000000000000000 ) ) ;
#5161=DIRECTION ( 'NONE',  ( 0.000000000000000000, 0.000000000000000000, 1.000000000000000000 ) ) ;
#5164=DIRECTION ( 'NONE',  ( 0.000000000000000000, 0.000000000000000000, -1.000000000000000000 ) ) ;
#5167=DIRECTION ( 'NONE',  ( 0.000000000000000000, 0.000000000000000000, 1.000000000000000000 ) ) ;
#5175=ORIENTED_EDGE ( 'NONE', *, *, #20763, .F. ) ;
#5179=EDGE_CURVE ( 'NONE', #65292, #28695, #16294, .T. ) ;
#5183=ADVANCED_FACE ( 'NONE', ( #67445 ), #27198, .T. ) ;
#5185=EDGE_LOOP ( 'NONE', ( #13673, #18299, #60395, #6570 ) ) ;
#5186=EDGE_CURVE ( 'NONE', #58816, #13817, #21110, .T. ) ;
#5190=CIRCLE ( 'NONE', #17151, 77.49900000000000944 ) ;
#5192=CARTESIAN_POINT ( 'NONE',  ( -10.00000000000000000, 0.000000000000000000, 0.000000000000000000 ) ) ;
#5196=EDGE_CURVE ( 'NONE', #9195, #74276, #47526, .T. ) ;
#5215=EDGE_LOOP ( 'NONE', ( #8543, #50370, #54130, #65513 ) ) ;
#5220=ORIENTED_EDGE ( 'NONE', *, *, #60553, .F. ) ;
#5223=CARTESIAN_POINT ( 'NONE',  ( 11.99999999999999822, 0.000000000000000000, 0.000000000000000000 ) ) ;
#5229=ORIENTED_EDGE ( 'NONE', *, *, #61687, .F. ) ;
#5236=DIRECTION ( 'NONE',  ( 0.000000000000000000, 0.000000000000000000, -1.000000000000000000 ) ) ;
#5239=EDGE_LOOP ( 'NONE', ( #16836, #34230, #21273, #30327 ) ) ;
#5242=DIRECTION ( 'NONE',  ( 0.000000000000000000, -0.9723699203976789995, 0.2334453638558957045 ) ) ;
#5243=ADVANCED_FACE ( 'NONE', ( #38505 ), #61817, .T. ) ;
#5251=DIRECTION ( 'NONE',  ( 0.000000000000000000, 0.5224985647159441360, 0.8526401643540952868 ) ) ;
#5254=DIRECTION ( 'NONE',  ( -1.000000000000000000, 0.000000000000000000, -0.000000000000000000 ) ) ;
#5255=DIRECTION ( 'NONE',  ( -1.000000000000000000, 0.000000000000000000, 0.000000000000000000 ) ) ;
#5257=DIRECTION ( 'NONE',  ( -1.000000000000000000, 0.000000000000000000, 0.000000000000000000 ) ) ;
#5258=AXIS2_PLACEMENT_3D ( 'NONE', #64695, #70678, #65075 ) ;
#5260=DIRECTION ( 'NONE',  ( 1.000000000000000000, -0.000000000000000000, -0.000000000000000000 ) ) ;
#5262=CARTESIAN_POINT ( 'NONE',  ( 15.00000000000000000, -22.32062822937469093, 14.36278369418830181 ) ) ;
#5265=DIRECTION ( 'NONE',  ( 0.000000000000000000, -0.8910065241883626808, -0.4539904997395569075 ) ) ;
#5279=ORIENTED_EDGE ( 'NONE', *, *, #59405, .T. ) ;
#5289=VERTEX_POINT ( 'NONE', #21570 ) ;
#5291=VERTEX_POINT ( 'NONE', #44526 ) ;
#5302=CIRCLE ( 'NONE', #72451, 77.49900000000000944 ) ;
#5304=DIRECTION ( 'NONE',  ( 0.000000000000000000, 0.000000000000000000, -1.000000000000000000 ) ) ;
#5309=VERTEX_POINT ( 'NONE', #6521 ) ;
#5313=ADVANCED_FACE ( 'NONE', ( #53120 ), #41466, .T. ) ;
#5316=ORIENTED_EDGE ( 'NONE', *, *, #19427, .F. ) ;
#5327=DIRECTION ( 'NONE',  ( 0.000000000000000000, -0.5877852522924624790, -0.8090169943749551118 ) ) ;
#5331=CARTESIAN_POINT ( 'NONE',  ( 11.99999999999999822, -70.52718814184240159, -26.02418014898383802 ) ) ;
#5332=DIRECTION ( 'NONE',  ( -1.000000000000000000, -0.000000000000000000, -0.000000000000000000 ) ) ;
#5333=FACE_OUTER_BOUND ( 'NONE', #49638, .T. ) ;
#5337=DIRECTION ( 'NONE',  ( -1.000000000000000000, 0.000000000000000000, 0.000000000000000000 ) ) ;
#5338=DIRECTION ( 'NONE',  ( -1.000000000000000000, -0.000000000000000000, -0.000000000000000000 ) ) ;
#5350=CARTESIAN_POINT ( 'NONE',  ( 11.99999999999999822, 49.70050353004975818, -59.46389618801909904 ) ) ;
#5357=CARTESIAN_POINT ( 'NONE',  ( 11.99999999999999822, 23.16143007188426850, 73.95703589263983702 ) ) ;
#5360=AXIS2_PLACEMENT_3D ( 'NONE', #38055, #55344, #44449 ) ;
#5368=ORIENTED_EDGE ( 'NONE', *, *, #53039, .T. ) ;
#5377=DIRECTION ( 'NONE',  ( -0.000000000000000000, 0.4999999999999921174, -0.8660254037844432595 ) ) ;
#5380=ORIENTED_EDGE ( 'NONE', *, *, #18856, .T. ) ;
#5405=LINE ( 'NONE', #16664, #11997 ) ;
#5406=LINE ( 'NONE', #15920, #5882 ) ;
#5419=DIRECTION ( 'NONE',  ( 0.000000000000000000, -0.5877852522924801315, 0.8090169943749423442 ) ) ;
#5423=CYLINDRICAL_SURFACE ( 'NONE', #22696, 31.99999999999998579 ) ;
#5425=ORIENTED_EDGE ( 'NONE', *, *, #11475, .T. ) ;
#5433=EDGE_LOOP ( 'NONE', ( #48980, #66613, #16684, #21842 ) ) ;
#5436=PLANE ( 'NONE',  #23539 ) ;
#5437=LINE ( 'NONE', #10681, #57047 ) ;
#5440=CIRCLE ( 'NONE', #47432, 31.99999999999998934 ) ;
#5443=ADVANCED_FACE ( 'NONE', ( #46009 ), #52752, .T. ) ;
#5448=EDGE_CURVE ( 'NONE', #24686, #22781, #40386, .T. ) ;
#5452=DIRECTION ( 'NONE',  ( 1.000000000000000000, 0.000000000000000000, 0.000000000000000000 ) ) ;
#5454=DIRECTION ( 'NONE',  ( -1.000000000000000000, 0.000000000000000000, 0.000000000000000000 ) ) ;
#5460=DIRECTION ( 'NONE',  ( 0.000000000000000000, 0.000000000000000000, 1.000000000000000000 ) ) ;
#5461=EDGE_LOOP ( 'NONE', ( #16299, #28936, #3820, #70069 ) ) ;
#5467=AXIS2_PLACEMENT_3D ( 'NONE', #64610, #30380, #53326 ) ;
#5468=EDGE_LOOP ( 'NONE', ( #47206, #51966, #6133, #7628 ) ) ;
#5471=EDGE_LOOP ( 'NONE', ( #64129, #62753, #17020, #67015 ) ) ;
#5473=EDGE_CURVE ( 'NONE', #48807, #37410, #37972, .T. ) ;
#5481=ORIENTED_EDGE ( 'NONE', *, *, #7819, .T. ) ;
#5483=ORIENTED_EDGE ( 'NONE', *, *, #24029, .T. ) ;
#5488=CARTESIAN_POINT ( 'NONE',  ( 11.99999999999999822, 0.000000000000000000, 0.000000000000000000 ) ) ;
#5490=LINE ( 'NONE', #28386, #37178 ) ;
#5491=DIRECTION ( 'NONE',  ( -1.000000000000000000, -0.000000000000000000, 0.000000000000000000 ) ) ;
#5496=VERTEX_POINT ( 'NONE', #14734 ) ;
#5502=DIRECTION ( 'NONE',  ( -1.000000000000000000, 0.000000000000000000, -0.000000000000000000 ) ) ;
#5510=ORIENTED_EDGE ( 'NONE', *, *, #53695, .T. ) ;
#5513=EDGE_CURVE ( 'NONE', #72105, #27765, #15102, .T. ) ;
#5516=FACE_OUTER_BOUND ( 'NONE', #55866, .T. ) ;
#5521=DIRECTION ( 'NONE',  ( 0.000000000000000000, 0.000000000000000000, 1.000000000000000000 ) ) ;
#5525=CIRCLE ( 'NONE', #43931, 31.99999999999998579 ) ;
#5536=AXIS2_PLACEMENT_3D ( 'NONE', #62950, #39623, #33972 ) ;
#5547=DIRECTION ( 'NONE',  ( 0.000000000000000000, -0.2334453638558922628, -0.9723699203976798877 ) ) ;
#5548=ORIENTED_EDGE ( 'NONE', *, *, #53789, .F. ) ;
#5550=DIRECTION ( 'NONE',  ( 0.000000000000000000, -0.3090169943749471737, 0.9510565162951537532 ) ) ;
#5556=ORIENTED_EDGE ( 'NONE', *, *, #2780, .F. ) ;
#5559=EDGE_CURVE ( 'NONE', #38945, #4632, #19266, .T. ) ;
#5565=EDGE_CURVE ( 'NONE', #73113, #11201, #5583, .T. ) ;
#5569=ORIENTED_EDGE ( 'NONE', *, *, #73557, .T. ) ;
#5583=CIRCLE ( 'NONE', #70366, 77.49899999999999523 ) ;
#5584=ORIENTED_EDGE ( 'NONE', *, *, #5473, .T. ) ;
#5594=EDGE_LOOP ( 'NONE', ( #14899, #42394, #34769, #46058 ) ) ;
#5595=FACE_OUTER_BOUND ( 'NONE', #69437, .T. ) ;
#5597=EDGE_LOOP ( 'NONE', ( #33846, #52334, #14884, #54547 ) ) ;
#5602=CARTESIAN_POINT ( 'NONE',  ( 0.000000000000000000, -71.21200624218825226, 40.65526001592589722 ) ) ;
#5604=EDGE_LOOP ( 'NONE', ( #33258, #63531, #38590, #6918 ) ) ;
#5626=CARTESIAN_POINT ( 'NONE',  ( 11.99999999999999822, -49.70050353004846500, -59.46389618802017907 ) ) ;
#5630=CARTESIAN_POINT ( 'NONE',  ( 11.99999999999999822, 2.956366410621684260, -75.11725578898465017 ) ) ;
#5631=VECTOR ( 'NONE', #35443, 1000.000000000000000 ) ;
#5633=CIRCLE ( 'NONE', #34369, 82.00000000000000000 ) ;
#5635=AXIS2_PLACEMENT_3D ( 'NONE', #60893, #9378, #32296 ) ;
#5657=ORIENTED_EDGE ( 'NONE', *, *, #43327, .F. ) ;
#5662=ORIENTED_EDGE ( 'NONE', *, *, #24333, .T. ) ;
#5667=ORIENTED_EDGE ( 'NONE', *, *, #10518, .F. ) ;
#5671=ORIENTED_EDGE ( 'NONE', *, *, #32218, .T. ) ;
#5674=ORIENTED_EDGE ( 'NONE', *, *, #5179, .T. ) ;
#5676=AXIS2_PLACEMENT_3D ( 'NONE', #21848, #71854, #61710 ) ;
#5679=DIRECTION ( 'NONE',  ( -1.000000000000000000, 0.000000000000000000, -0.000000000000000000 ) ) ;
#5691=DIRECTION ( 'NONE',  ( -1.000000000000000000, 0.000000000000000000, 0.000000000000000000 ) ) ;
#5696=DIRECTION ( 'NONE',  ( 0.000000000000000000, 0.000000000000000000, 1.000000000000000000 ) ) ;
#5701=LINE ( 'NONE', #34998, #15913 ) ;
#5710=EDGE_CURVE ( 'NONE', #359, #24340, #22610, .T. ) ;
#5720=VECTOR ( 'NONE', #18384, 1000.000000000000000 ) ;
#5724=DIRECTION ( 'NONE',  ( -1.000000000000000000, -0.000000000000000000, 0.000000000000000000 ) ) ;
#5725=VECTOR ( 'NONE', #34971, 1000.000000000000000 ) ;
#5745=VERTEX_POINT ( 'NONE', #1569 ) ;
#5748=ORIENTED_EDGE ( 'NONE', *, *, #17800, .T. ) ;
#5750=VECTOR ( 'NONE', #38051, 1000.000000000000000 ) ;
#5752=ORIENTED_EDGE ( 'NONE', *, *, #7489, .F. ) ;
#5755=CARTESIAN_POINT ( 'NONE',  ( 0.000000000000000000, -26.02418014898260878, -70.52718814184285634 ) ) ;
#5756=ORIENTED_EDGE ( 'NONE', *, *, #32942, .T. ) ;
#5759=ORIENTED_EDGE ( 'NONE', *, *, #56951, .F. ) ;
#5764=DIRECTION ( 'NONE',  ( -1.000000000000000000, 0.000000000000000000, 0.000000000000000000 ) ) ;
#5766=CARTESIAN_POINT ( 'NONE',  ( 11.99999999999999822, 51.03279382321088065, 55.19960302592086521 ) ) ;
#5776=AXIS2_PLACEMENT_3D ( 'NONE', #52600, #24773, #70615 ) ;
#5782=VECTOR ( 'NONE', #56283, 1000.000000000000000 ) ;
#5791=AXIS2_PLACEMENT_3D ( 'NONE', #53865, #60984, #3865 ) ;
#5796=CARTESIAN_POINT ( 'NONE',  ( 15.00000000000000000, -13.04903810567646971, 19.60159698893442481 ) ) ;
#5798=CARTESIAN_POINT ( 'NONE',  ( 15.00000000000000000, 26.50000000000000355, -1.500000000000000000 ) ) ;
#5804=CARTESIAN_POINT ( 'NONE',  ( 0.000000000000000000, 68.55367621811204515, -44.99326035065983120 ) ) ;
#5806=DIRECTION ( 'NONE',  ( 0.000000000000000000, 0.000000000000000000, 1.000000000000000000 ) ) ;
#5807=DIRECTION ( 'NONE',  ( 0.000000000000000000, 0.000000000000000000, 1.000000000000000000 ) ) ;
#5812=EDGE_CURVE ( 'NONE', #2580, #30548, #56001, .T. ) ;
#5817=CARTESIAN_POINT ( 'NONE',  ( 11.99999999999999822, -30.41916302227062019, -71.27951684758059514 ) ) ;
#5818=DIRECTION ( 'NONE',  ( 0.000000000000000000, 0.4539904997395413644, 0.8910065241883706744 ) ) ;
#5824=ORIENTED_EDGE ( 'NONE', *, *, #72222, .T. ) ;
#5830=CIRCLE ( 'NONE', #74228, 31.99999999999998579 ) ;
#5831=CIRCLE ( 'NONE', #65879, 31.99999999999998579 ) ;
#5832=DIRECTION ( 'NONE',  ( 0.000000000000000000, -1.000000000000000000, -1.301042606982602560E-15 ) ) ;
#5835=VERTEX_POINT ( 'NONE', #18437 ) ;
#5850=CARTESIAN_POINT ( 'NONE',  ( 0.000000000000000000, -51.03279382321125723, 55.19960302592048862 ) ) ;
#5858=ORIENTED_EDGE ( 'NONE', *, *, #65443, .T. ) ;
#5878=ORIENTED_EDGE ( 'NONE', *, *, #14323, .F. ) ;
#5882=VECTOR ( 'NONE', #16289, 1000.000000000000000 ) ;
#5889=VERTEX_POINT ( 'NONE', #36106 ) ;
#5894=DIRECTION ( 'NONE',  ( -1.000000000000000000, 0.000000000000000000, -0.000000000000000000 ) ) ;
#5904=EDGE_CURVE ( 'NONE', #27052, #22824, #42800, .T. ) ;
#5906=AXIS2_PLACEMENT_3D ( 'NONE', #20376, #38035, #19626 ) ;
#5909=AXIS2_PLACEMENT_3D ( 'NONE', #41722, #64664, #63935 ) ;
#5923=CARTESIAN_POINT ( 'NONE',  ( 5.999999999999999112, 2.543863470248399761, 81.96053171279903893 ) ) ;
#5924=ORIENTED_EDGE ( 'NONE', *, *, #73686, .T. ) ;
#5925=ORIENTED_EDGE ( 'NONE', *, *, #55880, .F. ) ;
#5931=DIRECTION ( 'NONE',  ( -0.000000000000000000, 0.1045284632676569680, 0.9945218953682730678 ) ) ;
#5935=AXIS2_PLACEMENT_3D ( 'NONE', #24851, #31229, #53429 ) ;
#5938=ORIENTED_EDGE ( 'NONE', *, *, #61140, .F. ) ;
#5940=ORIENTED_EDGE ( 'NONE', *, *, #8821, .F. ) ;
#5956=ORIENTED_EDGE ( 'NONE', *, *, #21030, .F. ) ;
#5961=DIRECTION ( 'NONE',  ( -1.000000000000000000, 0.000000000000000000, -0.000000000000000000 ) ) ;
#5964=AXIS2_PLACEMENT_3D ( 'NONE', #1918, #47007, #58648 ) ;
#5965=CYLINDRICAL_SURFACE ( 'NONE', #11352, 77.49899999999999523 ) ;
#5968=CARTESIAN_POINT ( 'NONE',  ( 12.00000000000000000, 16.61724383029390140, 20.69703378468902955 ) ) ;
#5974=CARTESIAN_POINT ( 'NONE',  ( 12.00000000000000000, 0.000000000000000000, 0.000000000000000000 ) ) ;
#5976=CIRCLE ( 'NONE', #73114, 77.49900000000000944 ) ;
#5978=LINE ( 'NONE', #34897, #56394 ) ;
#5982=VERTEX_POINT ( 'NONE', #71778 ) ;
#5985=FACE_OUTER_BOUND ( 'NONE', #7155, .T. ) ;
#5997=LINE ( 'NONE', #39828, #39906 ) ;
#6002=VECTOR ( 'NONE', #67434, 1000.000000000000000 ) ;
#6007=AXIS2_PLACEMENT_3D ( 'NONE', #32849, #55799, #44147 ) ;
#6011=DIRECTION ( 'NONE',  ( -1.000000000000000000, -0.000000000000000000, -0.000000000000000000 ) ) ;
#6012=CARTESIAN_POINT ( 'NONE',  ( 15.00000000000000000, -4.261787119644963262, 26.19803753235780164 ) ) ;
#6018=ORIENTED_EDGE ( 'NONE', *, *, #36475, .T. ) ;
#6019=VECTOR ( 'NONE', #1258, 1000.000000000000000 ) ;
#6031=ORIENTED_EDGE ( 'NONE', *, *, #50053, .F. ) ;
#6037=ORIENTED_EDGE ( 'NONE', *, *, #44770, .F. ) ;
#6039=EDGE_CURVE ( 'NONE', #52228, #72105, #30823, .T. ) ;
#6041=CARTESIAN_POINT ( 'NONE',  ( 0.000000000000000000, -8.840884882375609877, 74.65374052328647281 ) ) ;
#6042=EDGE_LOOP ( 'NONE', ( #43040, #37058, #6629, #52785 ) ) ;
#6048=ORIENTED_EDGE ( 'NONE', *, *, #51684, .T. ) ;
#6051=CARTESIAN_POINT ( 'NONE',  ( -10.00000000000000000, 0.000000000000000000, 0.000000000000000000 ) ) ;
#6054=VECTOR ( 'NONE', #48125, 1000.000000000000000 ) ;
#6057=CARTESIAN_POINT ( 'NONE',  ( 11.99999999999999822, 0.000000000000000000, 0.000000000000000000 ) ) ;
#6068=LINE ( 'NONE', #28974, #70469 ) ;
#6074=DIRECTION ( 'NONE',  ( -1.000000000000000000, 0.000000000000000000, -0.000000000000000000 ) ) ;
#6082=DIRECTION ( 'NONE',  ( 0.000000000000000000, 0.3090169943749410675, 0.9510565162951556406 ) ) ;
#6098=AXIS2_PLACEMENT_3D ( 'NONE', #40549, #28899, #40189 ) ;
#6103=DIRECTION ( 'NONE',  ( -1.000000000000000000, 0.000000000000000000, -0.000000000000000000 ) ) ;
#6104=DIRECTION ( 'NONE',  ( 0.000000000000000000, 0.4067366430758010409, 0.9135454576426005335 ) ) ;
#6110=CYLINDRICAL_SURFACE ( 'NONE', #58487, 31.99999999999998579 ) ;
#6112=ORIENTED_EDGE ( 'NONE', *, *, #73907, .T. ) ;
#6114=VERTEX_POINT ( 'NONE', #38704 ) ;
#6117=EDGE_CURVE ( 'NONE', #74276, #31156, #58417, .T. ) ;
#6123=EDGE_CURVE ( 'NONE', #62092, #70160, #73637, .T. ) ;
#6124=VERTEX_POINT ( 'NONE', #22155 ) ;
#6125=CARTESIAN_POINT ( 'NONE',  ( 11.99999999999999822, 17.28742895386084655, 75.54627589209950145 ) ) ;
#6126=VERTEX_POINT ( 'NONE', #33044 ) ;
#6133=ORIENTED_EDGE ( 'NONE', *, *, #21709, .F. ) ;
#6144=ORIENTED_EDGE ( 'NONE', *, *, #37130, .T. ) ;
#6167=EDGE_CURVE ( 'NONE', #33089, #35131, #8024, .T. ) ;
#6174=EDGE_CURVE ( 'NONE', #50325, #12497, #74030, .T. ) ;
#6176=CIRCLE ( 'NONE', #12154, 31.99999999999998579 ) ;
#6179=DIRECTION ( 'NONE',  ( 0.000000000000000000, -0.7071067811865536790, 0.7071067811865414665 ) ) ;
#6201=CIRCLE ( 'NONE', #31343, 82.00000000000000000 ) ;
#6203=CIRCLE ( 'NONE', #2632, 31.99999999999998579 ) ;
#6219=VERTEX_POINT ( 'NONE', #22909 ) ;
#6220=LINE ( 'NONE', #29120, #41871 ) ;
#6227=CARTESIAN_POINT ( 'NONE',  ( 11.99999999999999822, 0.000000000000000000, 0.000000000000000000 ) ) ;
#6228=CARTESIAN_POINT ( 'NONE',  ( 11.99999999999999822, -8.840884882375609877, 74.65374052328647281 ) ) ;
#6243=FACE_OUTER_BOUND ( 'NONE', #46420, .T. ) ;
#6247=EDGE_CURVE ( 'NONE', #64554, #53358, #12342, .T. ) ;
#6248=EDGE_CURVE ( 'NONE', #54778, #36975, #6711, .T. ) ;
#6258=VECTOR ( 'NONE', #50329, 1000.000000000000000 ) ;
#6262=CARTESIAN_POINT ( 'NONE',  ( 11.99999999999999822, -46.54456581323847786, 59.03342792756247093 ) ) ;
#6267=DIRECTION ( 'NONE',  ( 0.000000000000000000, 0.5877852522924743583, -0.8090169943749465631 ) ) ;
#6274=ORIENTED_EDGE ( 'NONE', *, *, #60939, .F. ) ;
#6277=AXIS2_PLACEMENT_3D ( 'NONE', #3473, #9830, #32746 ) ;
#6280=ORIENTED_EDGE ( 'NONE', *, *, #71200, .T. ) ;
#6284=EDGE_CURVE ( 'NONE', #6672, #60240, #378, .T. ) ;
#6285=EDGE_CURVE ( 'NONE', #37614, #53249, #70415, .T. ) ;
#6288=EDGE_CURVE ( 'NONE', #71207, #33546, #22529, .T. ) ;
#6295=DIRECTION ( 'NONE',  ( -1.000000000000000000, 0.000000000000000000, -0.000000000000000000 ) ) ;
#6296=DIRECTION ( 'NONE',  ( 0.000000000000000000, 0.000000000000000000, 1.000000000000000000 ) ) ;
#6303=ORIENTED_EDGE ( 'NONE', *, *, #57680, .T. ) ;
#6316=VERTEX_POINT ( 'NONE', #11238 ) ;
#6319=ORIENTED_EDGE ( 'NONE', *, *, #61190, .F. ) ;
#6323=ORIENTED_EDGE ( 'NONE', *, *, #32001, .F. ) ;
#6351=CARTESIAN_POINT ( 'NONE',  ( 11.99999999999999822, 46.54456581323805153, 59.03342792756280488 ) ) ;
#6353=PLANE ( 'NONE',  #26468 ) ;
#6354=CARTESIAN_POINT ( 'NONE',  ( 0.000000000000000000, -55.20638768913724448, -51.02545421589383068 ) ) ;
#6356=CARTESIAN_POINT ( 'NONE',  ( 11.99999999999999822, 23.16143007188530589, -73.95703589263951017 ) ) ;
#6361=CARTESIAN_POINT ( 'NONE',  ( 15.00000000000000000, -26.23277895567251505, -4.042438405569750870 ) ) ;
#6367=EDGE_LOOP ( 'NONE', ( #21007, #30234, #46739, #8667 ) ) ;
#6388=VERTEX_POINT ( 'NONE', #65707 ) ;
#6390=ORIENTED_EDGE ( 'NONE', *, *, #9994, .F. ) ;
#6391=ORIENTED_EDGE ( 'NONE', *, *, #17836, .F. ) ;
#6392=DIRECTION ( 'NONE',  ( -1.000000000000000000, 0.000000000000000000, 0.000000000000000000 ) ) ;
#6398=ORIENTED_EDGE ( 'NONE', *, *, #47397, .F. ) ;
#6403=CARTESIAN_POINT ( 'NONE',  ( 11.99999999999999822, -26.02418014898359289, 70.52718814184250107 ) ) ;
#6410=DIRECTION ( 'NONE',  ( -1.000000000000000000, 0.000000000000000000, 0.000000000000000000 ) ) ;
#6413=AXIS2_PLACEMENT_3D ( 'NONE', #50079, #36971, #8404 ) ;
#6414=EDGE_LOOP ( 'NONE', ( #46005, #25090, #49882, #14494 ) ) ;
#6423=EDGE_LOOP ( 'NONE', ( #62138, #21822, #50264, #72977 ) ) ;
#6424=DIRECTION ( 'NONE',  ( -1.000000000000000000, -0.000000000000000000, -0.000000000000000000 ) ) ;
#6432=FACE_OUTER_BOUND ( 'NONE', #56599, .T. ) ;
#6434=AXIS2_PLACEMENT_3D ( 'NONE', #41384, #12798, #70300 ) ;
#6443=DIRECTION ( 'NONE',  ( 0.000000000000000000, 0.000000000000000000, -1.000000000000000000 ) ) ;
#6446=DIRECTION ( 'NONE',  ( 1.000000000000000000, 0.000000000000000000, 0.000000000000000000 ) ) ;
#6448=CARTESIAN_POINT ( 'NONE',  ( 11.99999999999999822, 63.18004540533092239, -44.88180994100307686 ) ) ;
#6451=EDGE_CURVE ( 'NONE', #73300, #55761, #26046, .T. ) ;
#6465=DIRECTION ( 'NONE',  ( 1.000000000000000000, 0.000000000000000000, 0.000000000000000000 ) ) ;
#6470=CIRCLE ( 'NONE', #70098, 31.99999999999998579 ) ;
#6471=EDGE_CURVE ( 'NONE', #18143, #56853, #25478, .T. ) ;
#6472=ORIENTED_EDGE ( 'NONE', *, *, #37086, .T. ) ;
#6473=CARTESIAN_POINT ( 'NONE',  ( 11.99999999999999822, -75.11725578898470701, 2.956366410620372864 ) ) ;
#6474=ORIENTED_EDGE ( 'NONE', *, *, #58489, .F. ) ;
#6477=EDGE_LOOP ( 'NONE', ( #62339, #38164, #59540, #65023 ) ) ;
#6486=ORIENTED_EDGE ( 'NONE', *, *, #22922, .F. ) ;
#6492=AXIS2_PLACEMENT_3D ( 'NONE', #34502, #44310, #16861 ) ;
#6493=VERTEX_POINT ( 'NONE', #13810 ) ;
#6498=CARTESIAN_POINT ( 'NONE',  ( 0.000000000000000000, 0.000000000000000000, 0.000000000000000000 ) ) ;
#6505=VECTOR ( 'NONE', #10393, 1000.000000000000114 ) ;
#6507=EDGE_LOOP ( 'NONE', ( #42951, #49920, #3347, #49503 ) ) ;
#6517=ORIENTED_EDGE ( 'NONE', *, *, #61564, .T. ) ;
#6518=AXIS2_PLACEMENT_3D ( 'NONE', #9422, #9054, #54195 ) ;
#6521=CARTESIAN_POINT ( 'NONE',  ( 11.99999999999999822, 76.41127070299290835, -12.93880638057234123 ) ) ;
#6534=EDGE_CURVE ( 'NONE', #30413, #23323, #36428, .T. ) ;
#6545=CARTESIAN_POINT ( 'NONE',  ( 15.00000000000000000, -18.13022148937242761, 15.02647892043569122 ) ) ;
#6547=EDGE_CURVE ( 'NONE', #3697, #37374, #44255, .T. ) ;
#6548=CYLINDRICAL_SURFACE ( 'NONE', #30485, 82.00000000000000000 ) ;
#6555=CARTESIAN_POINT ( 'NONE',  ( 0.000000000000000000, 0.000000000000000000, 0.000000000000000000 ) ) ;
#6557=EDGE_LOOP ( 'NONE', ( #8731, #55011, #39479, #37474 ) ) ;
#6564=ORIENTED_EDGE ( 'NONE', *, *, #63134, .T. ) ;
#6568=ADVANCED_FACE ( 'NONE', ( #38237 ), #27700, .T. ) ;
#6570=ORIENTED_EDGE ( 'NONE', *, *, #61234, .T. ) ;
#6573=PLANE ( 'NONE',  #51562 ) ;
#6574=CIRCLE ( 'NONE', #48595, 31.99999999999999289 ) ;
#6576=ORIENTED_EDGE ( 'NONE', *, *, #40768, .F. ) ;
#6581=EDGE_LOOP ( 'NONE', ( #25698, #66222, #32349, #39592 ) ) ;
#6582=AXIS2_PLACEMENT_3D ( 'NONE', #21883, #33524, #56486 ) ;
#6584=FACE_OUTER_BOUND ( 'NONE', #45451, .T. ) ;
#6589=ORIENTED_EDGE ( 'NONE', *, *, #60595, .T. ) ;
#6597=ORIENTED_EDGE ( 'NONE', *, *, #27035, .T. ) ;
#6602=ORIENTED_EDGE ( 'NONE', *, *, #68133, .F. ) ;
#6603=CARTESIAN_POINT ( 'NONE',  ( 12.00000000000000000, -26.23277895567245466, 4.042438405570107030 ) ) ;
#6617=DIRECTION ( 'NONE',  ( -1.000000000000000000, 0.000000000000000000, 0.000000000000000000 ) ) ;
#6619=CARTESIAN_POINT ( 'NONE',  ( 11.99999999999999822, 0.000000000000000000, 0.000000000000000000 ) ) ;
#6624=DIRECTION ( 'NONE',  ( -0.000000000000000000, 0.1045284632676548031, 0.9945218953682732899 ) ) ;
#6625=EDGE_CURVE ( 'NONE', #40077, #71422, #27312, .T. ) ;
#6626=AXIS2_PLACEMENT_3D ( 'NONE', #32723, #55677, #50014 ) ;
#6629=ORIENTED_EDGE ( 'NONE', *, *, #59881, .F. ) ;
#6632=AXIS2_PLACEMENT_3D ( 'NONE', #40474, #63424, #16434 ) ;
#6635=VERTEX_POINT ( 'NONE', #43536 ) ;
#6639=ORIENTED_EDGE ( 'NONE', *, *, #43425, .T. ) ;
#6659=ORIENTED_EDGE ( 'NONE', *, *, #49055, .T. ) ;
#6672=VERTEX_POINT ( 'NONE', #38988 ) ;
#6683=DIRECTION ( 'NONE',  ( 0.000000000000000000, -0.8090169943749504489, -0.5877852522924689183 ) ) ;
#6684=CIRCLE ( 'NONE', #35493, 82.00000000000000000 ) ;
#6688=VECTOR ( 'NONE', #64497, 999.9999999999998863 ) ;
#6689=FACE_BOUND ( 'NONE', #1320, .T. ) ;
#6693=CIRCLE ( 'NONE', #11515, 31.99999999999998934 ) ;
#6699=DIRECTION ( 'NONE',  ( -1.000000000000000000, 0.000000000000000000, 0.000000000000000000 ) ) ;
#6703=EDGE_CURVE ( 'NONE', #73508, #42429, #46110, .T. ) ;
#6710=CARTESIAN_POINT ( 'NONE',  ( 15.00000000000000000, -3.948201729842032215, 23.21447184625297666 ) ) ;
#6711=LINE ( 'NONE', #68767, #68032 ) ;
#6720=EDGE_CURVE ( 'NONE', #24697, #9702, #28001, .T. ) ;
#6724=CYLINDRICAL_SURFACE ( 'NONE', #53421, 77.49899999999999523 ) ;
#6726=CIRCLE ( 'NONE', #24749, 77.49900000000000944 ) ;
#6731=EDGE_CURVE ( 'NONE', #14085, #4461, #58020, .T. ) ;
#6732=EDGE_CURVE ( 'NONE', #63525, #40273, #649, .T. ) ;
#6735=VECTOR ( 'NONE', #70862, 1000.000000000000000 ) ;
#6737=DIRECTION ( 'NONE',  ( -1.000000000000000000, -0.000000000000000000, -0.000000000000000000 ) ) ;
#6745=ORIENTED_EDGE ( 'NONE', *, *, #62075, .F. ) ;
#6747=ORIENTED_EDGE ( 'NONE', *, *, #29457, .T. ) ;
#6751=ORIENTED_EDGE ( 'NONE', *, *, #69035, .F. ) ;
#6757=ORIENTED_EDGE ( 'NONE', *, *, #43843, .F. ) ;
#6759=CYLINDRICAL_SURFACE ( 'NONE', #19297, 77.49899999999999523 ) ;
#6766=VERTEX_POINT ( 'NONE', #1022 ) ;
#6769=LINE ( 'NONE', #65040, #38457 ) ;
#6770=DIRECTION ( 'NONE',  ( -1.000000000000000000, 0.000000000000000000, -0.000000000000000000 ) ) ;
#6779=DIRECTION ( 'NONE',  ( -1.000000000000000000, 0.000000000000000000, -0.000000000000000000 ) ) ;
#6788=ADVANCED_FACE ( 'NONE', ( #23542 ), #62297, .T. ) ;
#6789=CARTESIAN_POINT ( 'NONE',  ( 11.99999999999999822, 72.35432306680485226, -20.40083707022909110 ) ) ;
#6791=AXIS2_PLACEMENT_3D ( 'NONE', #62253, #40053, #253 ) ;
#6793=CARTESIAN_POINT ( 'NONE',  ( 0.000000000000000000, 0.000000000000000000, 0.000000000000000000 ) ) ;
#6805=LINE ( 'NONE', #6448, #68837 ) ;
#6810=ORIENTED_EDGE ( 'NONE', *, *, #72124, .T. ) ;
#6814=CARTESIAN_POINT ( 'NONE',  ( 5.999999999999999112, -27.74655509720617630, -77.16300072079690153 ) ) ;
#6816=DIRECTION ( 'NONE',  ( 0.000000000000000000, 0.000000000000000000, -1.000000000000000000 ) ) ;
#6819=CARTESIAN_POINT ( 'NONE',  ( 11.99999999999999822, 8.840884882376133902, -74.65374052328640175 ) ) ;
#6820=ORIENTED_EDGE ( 'NONE', *, *, #57955, .T. ) ;
#6824=ORIENTED_EDGE ( 'NONE', *, *, #61288, .F. ) ;
#6826=AXIS2_PLACEMENT_3D ( 'NONE', #10165, #33457, #45136 ) ;
#6827=ORIENTED_EDGE ( 'NONE', *, *, #66744, .F. ) ;
#6829=VERTEX_POINT ( 'NONE', #52109 ) ;
#6835=VECTOR ( 'NONE', #70865, 1000.000000000000000 ) ;
#6862=EDGE_CURVE ( 'NONE', #50810, #42112, #26823, .T. ) ;
#6869=DIRECTION ( 'NONE',  ( 0.000000000000000000, 0.000000000000000000, 1.000000000000000000 ) ) ;
#6876=DIRECTION ( 'NONE',  ( -1.000000000000000000, -0.000000000000000000, 0.000000000000000000 ) ) ;
#6878=ORIENTED_EDGE ( 'NONE', *, *, #18069, .T. ) ;
#6881=CARTESIAN_POINT ( 'NONE',  ( 11.99999999999999822, 74.65374052328660071, -8.840884882374309583 ) ) ;
#6883=CARTESIAN_POINT ( 'NONE',  ( 6.000000000000000000, 74.18225833017937987, -34.94270380257559339 ) ) ;
#6884=DIRECTION ( 'NONE',  ( 0.000000000000000000, -0.8660254037844363761, 0.5000000000000038858 ) ) ;
#6885=CARTESIAN_POINT ( 'NONE',  ( 11.99999999999999822, 74.65491531819118620, -8.830959090342659579 ) ) ;
#6888=EDGE_LOOP ( 'NONE', ( #49753, #7608, #30221, #14110 ) ) ;
#6890=CIRCLE ( 'NONE', #40478, 77.49899999999999523 ) ;
#6895=CARTESIAN_POINT ( 'NONE',  ( 12.00000000000000000, 8.688484142253932063, -21.88630264137371029 ) ) ;
#6902=ADVANCED_FACE ( 'NONE', ( #2513 ), #24290, .T. ) ;
#6907=CARTESIAN_POINT ( 'NONE',  ( 11.99999999999999822, 18.89407956138362010, -75.16055320797013906 ) ) ;
#6913=FACE_OUTER_BOUND ( 'NONE', #64183, .T. ) ;
#6915=DIRECTION ( 'NONE',  ( 0.000000000000000000, 0.000000000000000000, 1.000000000000000000 ) ) ;
#6916=VERTEX_POINT ( 'NONE', #19736 ) ;
#6917=DIRECTION ( 'NONE',  ( -1.000000000000000000, 0.000000000000000000, 0.000000000000000000 ) ) ;
#6918=ORIENTED_EDGE ( 'NONE', *, *, #61542, .T. ) ;
#6919=ORIENTED_EDGE ( 'NONE', *, *, #72571, .T. ) ;
#6934=DIRECTION ( 'NONE',  ( 0.000000000000000000, -0.5224985647159380298, -0.8526401643540988395 ) ) ;
#6947=ORIENTED_EDGE ( 'NONE', *, *, #15118, .T. ) ;
#6950=ORIENTED_EDGE ( 'NONE', *, *, #13215, .F. ) ;
#6958=CARTESIAN_POINT ( 'NONE',  ( 0.000000000000000000, -22.90783923731575200, -78.73519480814978522 ) ) ;
#6974=DIRECTION ( 'NONE',  ( 0.000000000000000000, 0.000000000000000000, 1.000000000000000000 ) ) ;
#6976=DIRECTION ( 'NONE',  ( -1.000000000000000000, 0.000000000000000000, 0.000000000000000000 ) ) ;
#6990=ORIENTED_EDGE ( 'NONE', *, *, #51705, .T. ) ;
#6994=VECTOR ( 'NONE', #10304, 1000.000000000000000 ) ;
#6997=ORIENTED_EDGE ( 'NONE', *, *, #46879, .F. ) ;
#6998=EDGE_LOOP ( 'NONE', ( #30721, #64306, #50564, #51435 ) ) ;
#7003=CIRCLE ( 'NONE', #41845, 31.99999999999998934 ) ;
#7005=ORIENTED_EDGE ( 'NONE', *, *, #49496, .F. ) ;
#7007=VECTOR ( 'NONE', #13642, 1000.000000000000114 ) ;
#7014=CARTESIAN_POINT ( 'NONE',  ( 11.99999999999999822, -66.50666863321974631, -39.78640506895675344 ) ) ;
#7025=EDGE_CURVE ( 'NONE', #26361, #63641, #27221, .T. ) ;
#7033=VERTEX_POINT ( 'NONE', #9581 ) ;
#7035=AXIS2_PLACEMENT_3D ( 'NONE', #62553, #11036, #26462 ) ;
#7041=LINE ( 'NONE', #18323, #33781 ) ;
#7045=VERTEX_POINT ( 'NONE', #60724 ) ;
#7048=ORIENTED_EDGE ( 'NONE', *, *, #11978, .F. ) ;
#7063=AXIS2_PLACEMENT_3D ( 'NONE', #43363, #8392, #60644 ) ;
#7064=ORIENTED_EDGE ( 'NONE', *, *, #32233, .F. ) ;
#7068=AXIS2_PLACEMENT_3D ( 'NONE', #32258, #48818, #60491 ) ;
#7077=CARTESIAN_POINT ( 'NONE',  ( 11.99999999999999822, 0.000000000000000000, 0.000000000000000000 ) ) ;
#7083=EDGE_CURVE ( 'NONE', #48585, #10371, #8842, .T. ) ;
#7084=DIRECTION ( 'NONE',  ( -1.000000000000000000, -0.000000000000000000, 0.000000000000000000 ) ) ;
#7098=CIRCLE ( 'NONE', #62225, 77.49899999999999523 ) ;
#7106=ORIENTED_EDGE ( 'NONE', *, *, #37091, .F. ) ;
#7111=ADVANCED_FACE ( 'NONE', ( #72356 ), #15591, .T. ) ;
#7112=CARTESIAN_POINT ( 'NONE',  ( 11.99999999999999822, -68.26794271651239399, -31.47745569255214093 ) ) ;
#7117=CIRCLE ( 'NONE', #10716, 82.00000000000000000 ) ;
#7118=EDGE_CURVE ( 'NONE', #36401, #37377, #20869, .T. ) ;
#7134=ORIENTED_EDGE ( 'NONE', *, *, #4707, .F. ) ;
#7136=ORIENTED_EDGE ( 'NONE', *, *, #35084, .T. ) ;
#7140=CARTESIAN_POINT ( 'NONE',  ( 0.000000000000000000, 55.38113227695783536, 54.21277698773694453 ) ) ;
#7143=ORIENTED_EDGE ( 'NONE', *, *, #72075, .T. ) ;
#7144=EDGE_LOOP ( 'NONE', ( #45827, #45959, #17104, #11694 ) ) ;
#7155=EDGE_LOOP ( 'NONE', ( #8988, #13476, #18055, #42338 ) ) ;
#7158=LINE ( 'NONE', #25548, #34412 ) ;
#7168=AXIS2_PLACEMENT_3D ( 'NONE', #61939, #57042, #15316 ) ;
#7170=DIRECTION ( 'NONE',  ( -1.000000000000000000, -0.000000000000000000, -0.000000000000000000 ) ) ;
#7176=CIRCLE ( 'NONE', #62471, 31.99999999999998579 ) ;
#7184=AXIS2_PLACEMENT_3D ( 'NONE', #22474, #23856, #56695 ) ;
#7212=CARTESIAN_POINT ( 'NONE',  ( 11.99999999999999822, 0.000000000000000000, 0.000000000000000000 ) ) ;
#7214=CARTESIAN_POINT ( 'NONE',  ( 11.99999999999999822, -76.41127070299280888, 12.93880638057290788 ) ) ;
#7215=LINE ( 'NONE', #6125, #22456 ) ;
#7217=ORIENTED_EDGE ( 'NONE', *, *, #43833, .F. ) ;
#7218=LINE ( 'NONE', #36885, #22634 ) ;
#7219=EDGE_LOOP ( 'NONE', ( #70030, #19350, #25331, #71093 ) ) ;
#7220=DIRECTION ( 'NONE',  ( 0.000000000000000000, 0.000000000000000000, 1.000000000000000000 ) ) ;
#7223=AXIS2_PLACEMENT_3D ( 'NONE', #73533, #22043, #10017 ) ;
#7236=CYLINDRICAL_SURFACE ( 'NONE', #18073, 82.00000000000000000 ) ;
#7244=VERTEX_POINT ( 'NONE', #65852 ) ;
#7255=CARTESIAN_POINT ( 'NONE',  ( 11.99999999999999822, 46.53671651294032330, -59.03961581697353012 ) ) ;
#7256=CARTESIAN_POINT ( 'NONE',  ( 11.99999999999999822, -62.50329211542407393, -41.76937507738853839 ) ) ;
#7260=EDGE_LOOP ( 'NONE', ( #38681, #28136, #67593, #54277 ) ) ;
#7267=CARTESIAN_POINT ( 'NONE',  ( 11.99999999999999822, 0.000000000000000000, 0.000000000000000000 ) ) ;
#7269=CYLINDRICAL_SURFACE ( 'NONE', #22448, 77.49899999999999523 ) ;
#7270=VECTOR ( 'NONE', #31289, 1000.000000000000000 ) ;
#7272=CARTESIAN_POINT ( 'NONE',  ( 11.99999999999999822, 74.65491531819118620, 23.16904090965732621 ) ) ;
#7278=DIRECTION ( 'NONE',  ( 0.000000000000000000, 0.000000000000000000, 1.000000000000000000 ) ) ;
#7279=CYLINDRICAL_SURFACE ( 'NONE', #49032, 82.00000000000000000 ) ;
#7282=DIRECTION ( 'NONE',  ( 0.000000000000000000, 0.000000000000000000, 1.000000000000000000 ) ) ;
#7284=VERTEX_POINT ( 'NONE', #73996 ) ;
#7285=DIRECTION ( 'NONE',  ( -1.000000000000000000, 0.000000000000000000, -0.000000000000000000 ) ) ;
#7294=ORIENTED_EDGE ( 'NONE', *, *, #21569, .T. ) ;
#7297=ORIENTED_EDGE ( 'NONE', *, *, #71036, .F. ) ;
#7302=CYLINDRICAL_SURFACE ( 'NONE', #57413, 77.49899999999999523 ) ;
#7310=CARTESIAN_POINT ( 'NONE',  ( 11.99999999999999822, -15.33399622253425321, -80.55351364060605590 ) ) ;
#7311=EDGE_CURVE ( 'NONE', #31915, #45341, #39804, .T. ) ;
#7316=CIRCLE ( 'NONE', #64964, 82.00000000000000000 ) ;
#7317=EDGE_LOOP ( 'NONE', ( #70092, #57940, #29661, #57874 ) ) ;
#7319=AXIS2_PLACEMENT_3D ( 'NONE', #38510, #39629, #4319 ) ;
#7322=DIRECTION ( 'NONE',  ( 0.000000000000000000, 0.3826834323650841752, 0.9238795325112891810 ) ) ;
#7326=CARTESIAN_POINT ( 'NONE',  ( 0.000000000000000000, -73.73191006444561424, -14.66109333815538918 ) ) ;
#7335=VERTEX_POINT ( 'NONE', #33783 ) ;
#7336=EDGE_CURVE ( 'NONE', #6388, #32813, #66499, .T. ) ;
#7338=CARTESIAN_POINT ( 'NONE',  ( 0.000000000000000000, -59.75363087400035056, -56.15606465355020305 ) ) ;
#7343=CARTESIAN_POINT ( 'NONE',  ( 0.000000000000000000, -75.54627589209955829, 17.28742895386058009 ) ) ;
#7349=CIRCLE ( 'NONE', #49345, 31.99999999999998579 ) ;
#7350=ORIENTED_EDGE ( 'NONE', *, *, #36099, .F. ) ;
#7353=DIRECTION ( 'NONE',  ( 1.000000000000000000, -0.000000000000000000, -0.000000000000000000 ) ) ;
#7354=DIRECTION ( 'NONE',  ( 0.000000000000000000, 0.2334453638559058908, -0.9723699203976764460 ) ) ;
#7364=DIRECTION ( 'NONE',  ( -1.000000000000000000, 0.000000000000000000, -0.000000000000000000 ) ) ;
#7367=CARTESIAN_POINT ( 'NONE',  ( 11.99999999999999822, 68.26794271651262136, 31.47745569255165066 ) ) ;
#7371=VERTEX_POINT ( 'NONE', #63479 ) ;
#7373=DIRECTION ( 'NONE',  ( 0.000000000000000000, 0.9723699203976756689, 0.2334453638559094157 ) ) ;
#7376=AXIS2_PLACEMENT_3D ( 'NONE', #68012, #40931, #22906 ) ;
#7377=AXIS2_PLACEMENT_3D ( 'NONE', #2028, #26394, #66263 ) ;
#7380=ORIENTED_EDGE ( 'NONE', *, *, #48377, .F. ) ;
#7381=EDGE_CURVE ( 'NONE', #50810, #28846, #34080, .T. ) ;
#7383=ORIENTED_EDGE ( 'NONE', *, *, #50570, .F. ) ;
#7388=CARTESIAN_POINT ( 'NONE',  ( 11.99999999999999822, -70.52718814184277107, 26.02418014898285037 ) ) ;
#7389=CARTESIAN_POINT ( 'NONE',  ( 11.99999999999999822, -68.67312586194971402, -35.91791733033549860 ) ) ;
#7392=VERTEX_POINT ( 'NONE', #17238 ) ;
#7400=DIRECTION ( 'NONE',  ( 0.000000000000000000, 0.8526401643540897357, 0.5224985647159527957 ) ) ;
#7402=ORIENTED_EDGE ( 'NONE', *, *, #64604, .T. ) ;
#7403=ORIENTED_EDGE ( 'NONE', *, *, #16049, .T. ) ;
#7405=ORIENTED_EDGE ( 'NONE', *, *, #34886, .T. ) ;
#7424=DIRECTION ( 'NONE',  ( 0.000000000000000000, -0.07845909572785234043, 0.9969173337331274087 ) ) ;
#7433=ORIENTED_EDGE ( 'NONE', *, *, #23785, .T. ) ;
#7436=DIRECTION ( 'NONE',  ( -1.000000000000000000, -0.000000000000000000, -0.000000000000000000 ) ) ;
#7440=VERTEX_POINT ( 'NONE', #13060 ) ;
#7442=DIRECTION ( 'NONE',  ( 0.000000000000000000, 0.8526401643540897357, 0.5224985647159527957 ) ) ;
#7445=FACE_OUTER_BOUND ( 'NONE', #18948, .T. ) ;
#7447=FACE_OUTER_BOUND ( 'NONE', #56263, .T. ) ;
#7448=DIRECTION ( 'NONE',  ( 1.000000000000000000, 0.000000000000000000, 0.000000000000000000 ) ) ;
#7450=PLANE ( 'NONE',  #49602 ) ;
#7455=CARTESIAN_POINT ( 'NONE',  ( 0.000000000000000000, 78.73519480814955784, 22.90783923731656557 ) ) ;
#7457=CARTESIAN_POINT ( 'NONE',  ( 11.99999999999999822, -68.27212725128254078, -31.46837873495049465 ) ) ;
#7465=CARTESIAN_POINT ( 'NONE',  ( 11.99999999999999822, -62.20884554313985149, -46.21855187248698371 ) ) ;
#7472=CIRCLE ( 'NONE', #66300, 31.99999999999998579 ) ;
#7475=AXIS2_PLACEMENT_3D ( 'NONE', #72341, #15195, #53955 ) ;
#7479=LINE ( 'NONE', #42070, #16142 ) ;
#7480=AXIS2_PLACEMENT_3D ( 'NONE', #40524, #57089, #69464 ) ;
#7485=ORIENTED_EDGE ( 'NONE', *, *, #46101, .F. ) ;
#7489=EDGE_CURVE ( 'NONE', #13137, #46053, #50924, .T. ) ;
#7492=AXIS2_PLACEMENT_3D ( 'NONE', #56989, #34406, #16381 ) ;
#7493=CARTESIAN_POINT ( 'NONE',  ( 11.99999999999999822, -62.50884508063395373, -41.76106447765554464 ) ) ;
#7499=CARTESIAN_POINT ( 'NONE',  ( 6.000000000000000000, -81.34940948281328588, -10.30890764327469000 ) ) ;
#7503=EDGE_LOOP ( 'NONE', ( #53823, #1874, #37109, #39941 ) ) ;
#7512=DIRECTION ( 'NONE',  ( 0.000000000000000000, 0.8660254037844374864, -0.5000000000000019984 ) ) ;
#7513=ORIENTED_EDGE ( 'NONE', *, *, #67295, .T. ) ;
#7524=CARTESIAN_POINT ( 'NONE',  ( 0.000000000000000000, 20.41045688087930898, -72.35160999960793049 ) ) ;
#7531=CARTESIAN_POINT ( 'NONE',  ( 11.99999999999999822, 17.28742895386084655, 75.54627589209950145 ) ) ;
#7535=CARTESIAN_POINT ( 'NONE',  ( 50.00005079999999680, 2.571758278209441661E-15, -21.00000000000000000 ) ) ;
#7536=CARTESIAN_POINT ( 'NONE',  ( -10.00000000000000000, 0.000000000000000000, 0.000000000000000000 ) ) ;
#7545=CIRCLE ( 'NONE', #8729, 31.99999999999998579 ) ;
#7547=CARTESIAN_POINT ( 'NONE',  ( 15.00000000000000000, 24.81905959214260804, -9.408202855044828894 ) ) ;
#7548=AXIS2_PLACEMENT_3D ( 'NONE', #30815, #30087, #1568 ) ;
#7550=EDGE_CURVE ( 'NONE', #17105, #26000, #10018, .T. ) ;
#7555=ADVANCED_FACE ( 'NONE', ( #26932 ), #14917, .T. ) ;
#7556=DIRECTION ( 'NONE',  ( 0.000000000000000000, 0.000000000000000000, -1.000000000000000000 ) ) ;
#7557=EDGE_LOOP ( 'NONE', ( #51494, #51711, #31987, #43694 ) ) ;
#7559=CARTESIAN_POINT ( 'NONE',  ( 11.99999999999999822, -55.16347631942997509, -60.67117009219195722 ) ) ;
#7560=CARTESIAN_POINT ( 'NONE',  ( 6.000000000000000000, -8.966570791700160470, -81.50828551894237251 ) ) ;
#7562=EDGE_CURVE ( 'NONE', #51749, #37374, #44932, .T. ) ;
#7563=CARTESIAN_POINT ( 'NONE',  ( 11.99999999999999822, 78.73519480814954363, 22.90783923731657268 ) ) ;
#7564=EDGE_CURVE ( 'NONE', #5745, #9042, #43875, .T. ) ;
#7567=EDGE_LOOP ( 'NONE', ( #30297, #72474, #11493, #56517 ) ) ;
#7576=EDGE_CURVE ( 'NONE', #25675, #7033, #55518, .T. ) ;
#7579=VERTEX_POINT ( 'NONE', #38219 ) ;
#7581=EDGE_LOOP ( 'NONE', ( #66657, #40869, #58158, #72769 ) ) ;
#7584=VERTEX_POINT ( 'NONE', #55139 ) ;
#7601=LINE ( 'NONE', #42929, #57191 ) ;
#7602=FACE_OUTER_BOUND ( 'NONE', #26247, .T. ) ;
#7608=ORIENTED_EDGE ( 'NONE', *, *, #60041, .T. ) ;
#7613=CYLINDRICAL_SURFACE ( 'NONE', #14017, 31.99999999999998579 ) ;
#7624=DIRECTION ( 'NONE',  ( -1.000000000000000000, -0.000000000000000000, -0.000000000000000000 ) ) ;
#7628=ORIENTED_EDGE ( 'NONE', *, *, #64087, .T. ) ;
#7633=DIRECTION ( 'NONE',  ( -1.000000000000000000, 0.000000000000000000, 0.000000000000000000 ) ) ;
#7645=CARTESIAN_POINT ( 'NONE',  ( 0.000000000000000000, -55.19960302592104284, 51.03279382321070301 ) ) ;
#7650=CIRCLE ( 'NONE', #46087, 31.99999999999999289 ) ;
#7652=DIRECTION ( 'NONE',  ( 0.000000000000000000, 0.8090169943749486725, -0.5877852522924713607 ) ) ;
#7654=EDGE_CURVE ( 'NONE', #21827, #54492, #41320, .T. ) ;
#7661=ORIENTED_EDGE ( 'NONE', *, *, #34461, .T. ) ;
#7669=ORIENTED_EDGE ( 'NONE', *, *, #56882, .T. ) ;
#7685=CARTESIAN_POINT ( 'NONE',  ( 15.00000000000000000, 16.61724383029390140, 20.69703378468902955 ) ) ;
#7719=VECTOR ( 'NONE', #5764, 1000.000000000000000 ) ;
#7720=ADVANCED_FACE ( 'NONE', ( #5516 ), #4402, .T. ) ;
#7722=LINE ( 'NONE', #37036, #3076 ) ;
#7725=LINE ( 'NONE', #70123, #62071 ) ;
#7728=DIRECTION ( 'NONE',  ( -1.000000000000000000, 0.000000000000000000, 0.000000000000000000 ) ) ;
#7732=EDGE_CURVE ( 'NONE', #56025, #57064, #56646, .T. ) ;
#7737=DIRECTION ( 'NONE',  ( 0.000000000000000000, 0.000000000000000000, -1.000000000000000000 ) ) ;
#7752=AXIS2_PLACEMENT_3D ( 'NONE', #15600, #26508, #49438 ) ;
#7760=VECTOR ( 'NONE', #39856, 1000.000000000000000 ) ;
#7780=LINE ( 'NONE', #24335, #30187 ) ;
#7788=ORIENTED_EDGE ( 'NONE', *, *, #14651, .F. ) ;
#7796=DIRECTION ( 'NONE',  ( 0.000000000000000000, 0.000000000000000000, 1.000000000000000000 ) ) ;
#7799=ORIENTED_EDGE ( 'NONE', *, *, #64674, .F. ) ;
#7800=AXIS2_PLACEMENT_3D ( 'NONE', #72174, #9394, #16525 ) ;
#7802=AXIS2_PLACEMENT_3D ( 'NONE', #72937, #44405, #28571 ) ;
#7813=VECTOR ( 'NONE', #54781, 1000.000000000000000 ) ;
#7819=EDGE_CURVE ( 'NONE', #48253, #38472, #55887, .T. ) ;
#7829=EDGE_LOOP ( 'NONE', ( #47522, #18086, #61325, #71625 ) ) ;
#7842=CARTESIAN_POINT ( 'NONE',  ( 11.99999999999999822, -59.03342792756297541, 46.54456581323783126 ) ) ;
#7847=EDGE_LOOP ( 'NONE', ( #20526, #60945, #45325, #63356 ) ) ;
#7850=VECTOR ( 'NONE', #52960, 1000.000000000000000 ) ;
#7855=ORIENTED_EDGE ( 'NONE', *, *, #49320, .T. ) ;
#7866=ORIENTED_EDGE ( 'NONE', *, *, #54328, .F. ) ;
#7867=CIRCLE ( 'NONE', #19879, 77.49900000000000944 ) ;
#7877=EDGE_CURVE ( 'NONE', #72240, #48807, #637, .T. ) ;
#7885=DIRECTION ( 'NONE',  ( -1.000000000000000000, -0.000000000000000000, 0.000000000000000000 ) ) ;
#7887=ORIENTED_EDGE ( 'NONE', *, *, #28259, .F. ) ;
#7899=LINE ( 'NONE', #53765, #73097 ) ;
#7901=EDGE_CURVE ( 'NONE', #46053, #71434, #19739, .T. ) ;
#7909=LINE ( 'NONE', #47400, #50201 ) ;
#7915=AXIS2_PLACEMENT_3D ( 'NONE', #4141, #43978, #43619 ) ;
#7921=LINE ( 'NONE', #26681, #52669 ) ;
#7923=FACE_OUTER_BOUND ( 'NONE', #3663, .T. ) ;
#7927=DIRECTION ( 'NONE',  ( 0.000000000000000000, 0.000000000000000000, 1.000000000000000000 ) ) ;
#7941=ORIENTED_EDGE ( 'NONE', *, *, #43110, .T. ) ;
#7942=DIRECTION ( 'NONE',  ( 0.000000000000000000, 0.000000000000000000, 1.000000000000000000 ) ) ;
#7944=ORIENTED_EDGE ( 'NONE', *, *, #5513, .F. ) ;
#7963=LINE ( 'NONE', #24517, #71600 ) ;
#7979=LINE ( 'NONE', #9085, #22346 ) ;
#7987=CIRCLE ( 'NONE', #38037, 82.00000000000000000 ) ;
#7988=VERTEX_POINT ( 'NONE', #46839 ) ;
#7996=EDGE_LOOP ( 'NONE', ( #12479, #33784, #4745, #12957 ) ) ;
#7999=ADVANCED_FACE ( 'NONE', ( #53210 ), #24634, .T. ) ;
#8011=LINE ( 'NONE', #59150, #34599 ) ;
#8020=CYLINDRICAL_SURFACE ( 'NONE', #72095, 82.00000000000000000 ) ;
#8022=ORIENTED_EDGE ( 'NONE', *, *, #48358, .F. ) ;
#8024=CIRCLE ( 'NONE', #5635, 31.99999999999998579 ) ;
#8029=CIRCLE ( 'NONE', #63267, 31.99999999999999289 ) ;
#8030=ORIENTED_EDGE ( 'NONE', *, *, #58555, .T. ) ;
#8044=ORIENTED_EDGE ( 'NONE', *, *, #16366, .F. ) ;
#8047=ORIENTED_EDGE ( 'NONE', *, *, #40923, .F. ) ;
#8053=CARTESIAN_POINT ( 'NONE',  ( 12.00000000000000000, -23.29833615347109088, -3.418703333116486665 ) ) ;
#8054=EDGE_CURVE ( 'NONE', #42911, #12729, #57773, .T. ) ;
#8064=CARTESIAN_POINT ( 'NONE',  ( 5.999999999999999112, -40.65526001592663619, 71.21200624218782593 ) ) ;
#8070=ORIENTED_EDGE ( 'NONE', *, *, #23754, .F. ) ;
#8071=CARTESIAN_POINT ( 'NONE',  ( 5.999999999999999112, -74.74816331893404708, -33.71516098798818462 ) ) ;
#8073=EDGE_LOOP ( 'NONE', ( #2381, #39893, #39237, #7294 ) ) ;
#8080=CARTESIAN_POINT ( 'NONE',  ( 11.99999999999999822, 15.33399622253482342, 80.55351364060595643 ) ) ;
#8081=VECTOR ( 'NONE', #52300, 1000.000000000000000 ) ;
#8084=CYLINDRICAL_SURFACE ( 'NONE', #38383, 31.99999999999998579 ) ;
#8085=ORIENTED_EDGE ( 'NONE', *, *, #10342, .T. ) ;
#8087=ADVANCED_FACE ( 'NONE', ( #8464 ), #31004, .T. ) ;
#8088=EDGE_CURVE ( 'NONE', #29971, #48817, #43348, .T. ) ;
#8094=DIRECTION ( 'NONE',  ( 0.000000000000000000, 0.000000000000000000, 1.000000000000000000 ) ) ;
#8106=ORIENTED_EDGE ( 'NONE', *, *, #58163, .F. ) ;
#8112=FACE_OUTER_BOUND ( 'NONE', #56803, .T. ) ;
#8118=CARTESIAN_POINT ( 'NONE',  ( 11.99999999999999822, -41.19522573413689059, -65.64334221924951862 ) ) ;
#8120=CARTESIAN_POINT ( 'NONE',  ( 6.000000000000000000, -2.543863470247820224, -81.96053171279903893 ) ) ;
#8127=VERTEX_POINT ( 'NONE', #15197 ) ;
#8136=DIRECTION ( 'NONE',  ( 0.000000000000000000, 0.000000000000000000, 1.000000000000000000 ) ) ;
#8138=AXIS2_PLACEMENT_3D ( 'NONE', #16732, #10336, #33255 ) ;
#8140=ORIENTED_EDGE ( 'NONE', *, *, #49494, .F. ) ;
#8165=VERTEX_POINT ( 'NONE', #55429 ) ;
#8173=CARTESIAN_POINT ( 'NONE',  ( 0.000000000000000000, -75.11764819372145041, -2.946379043147127064 ) ) ;
#8178=CARTESIAN_POINT ( 'NONE',  ( 0.000000000000000000, 0.000000000000000000, 0.000000000000000000 ) ) ;
#8179=DIRECTION ( 'NONE',  ( -1.000000000000000000, 0.000000000000000000, -0.000000000000000000 ) ) ;
#8188=VECTOR ( 'NONE', #27281, 1000.000000000000000 ) ;
#8195=DIRECTION ( 'NONE',  ( 0.000000000000000000, -0.8090169943749530024, 0.5877852522924653655 ) ) ;
#8198=ORIENTED_EDGE ( 'NONE', *, *, #23597, .F. ) ;
#8200=ORIENTED_EDGE ( 'NONE', *, *, #25986, .F. ) ;
#8205=DIRECTION ( 'NONE',  ( 1.000000000000000000, 0.000000000000000000, 0.000000000000000000 ) ) ;
#8211=AXIS2_PLACEMENT_3D ( 'NONE', #63966, #35380, #22622 ) ;
#8214=CARTESIAN_POINT ( 'NONE',  ( 6.000000000000000000, 15.33399622253601002, -80.55351364060572905 ) ) ;
#8220=VECTOR ( 'NONE', #116, 1000.000000000000000 ) ;
#8227=DIRECTION ( 'NONE',  ( -1.000000000000000000, 0.000000000000000000, -0.000000000000000000 ) ) ;
#8231=ADVANCED_FACE ( 'NONE', ( #44531 ), #22715, .T. ) ;
#8243=FACE_OUTER_BOUND ( 'NONE', #4184, .T. ) ;
#8253=ORIENTED_EDGE ( 'NONE', *, *, #9944, .F. ) ;
#8256=VERTEX_POINT ( 'NONE', #5798 ) ;
#8257=EDGE_CURVE ( 'NONE', #17105, #23233, #2533, .T. ) ;
#8264=FACE_OUTER_BOUND ( 'NONE', #41793, .T. ) ;
#8287=VERTEX_POINT ( 'NONE', #39259 ) ;
#8298=VERTEX_POINT ( 'NONE', #28704 ) ;
#8304=CIRCLE ( 'NONE', #29748, 77.49899999999999523 ) ;
#8307=EDGE_LOOP ( 'NONE', ( #58591, #40606, #46771, #46162 ) ) ;
#8317=ORIENTED_EDGE ( 'NONE', *, *, #71639, .T. ) ;
#8324=VECTOR ( 'NONE', #53837, 1000.000000000000114 ) ;
#8325=EDGE_CURVE ( 'NONE', #31594, #25082, #1353, .T. ) ;
#8326=AXIS2_PLACEMENT_3D ( 'NONE', #66665, #62139, #44487 ) ;
#8327=VERTEX_POINT ( 'NONE', #192 ) ;
#8328=VECTOR ( 'NONE', #4058, 1000.000000000000000 ) ;
#8329=CIRCLE ( 'NONE', #24017, 31.99999999999998934 ) ;
#8335=DIRECTION ( 'NONE',  ( 0.000000000000000000, -0.9510565162951566398, 0.3090169943749381809 ) ) ;
#8338=ORIENTED_EDGE ( 'NONE', *, *, #66073, .T. ) ;
#8364=ORIENTED_EDGE ( 'NONE', *, *, #3862, .T. ) ;
#8365=DIRECTION ( 'NONE',  ( 1.000000000000000000, 0.000000000000000000, 0.000000000000000000 ) ) ;
#8366=CIRCLE ( 'NONE', #41964, 82.00000000000000000 ) ;
#8373=CARTESIAN_POINT ( 'NONE',  ( 15.00000000000000000, 18.84667830672605859, 18.68964196561243796 ) ) ;
#8374=VERTEX_POINT ( 'NONE', #57664 ) ;
#8375=CARTESIAN_POINT ( 'NONE',  ( 11.99999999999999822, -63.18004540532995605, -44.88180994100445531 ) ) ;
#8376=DIRECTION ( 'NONE',  ( 0.000000000000000000, 0.000000000000000000, 1.000000000000000000 ) ) ;
#8386=CIRCLE ( 'NONE', #19169, 31.99999999999998224 ) ;
#8392=DIRECTION ( 'NONE',  ( 1.000000000000000000, 0.000000000000000000, 0.000000000000000000 ) ) ;
#8404=DIRECTION ( 'NONE',  ( 0.000000000000000000, -0.9238795325112906243, 0.3826834323650805114 ) ) ;
#8410=AXIS2_PLACEMENT_3D ( 'NONE', #40710, #68912, #52346 ) ;
#8412=ORIENTED_EDGE ( 'NONE', *, *, #62038, .T. ) ;
#8414=AXIS2_PLACEMENT_3D ( 'NONE', #45973, #41795, #7220 ) ;
#8415=VERTEX_POINT ( 'NONE', #23809 ) ;
#8423=ADVANCED_FACE ( 'NONE', ( #63305 ), #34720, .T. ) ;
#8429=CIRCLE ( 'NONE', #30035, 31.99999999999998579 ) ;
#8445=ORIENTED_EDGE ( 'NONE', *, *, #9436, .T. ) ;
#8450=EDGE_CURVE ( 'NONE', #9220, #61985, #17789, .T. ) ;
#8452=AXIS2_PLACEMENT_3D ( 'NONE', #63138, #51089, #11236 ) ;
#8456=DIRECTION ( 'NONE',  ( 0.000000000000000000, 0.3090169943749560555, 0.9510565162951506446 ) ) ;
#8459=VECTOR ( 'NONE', #53395, 1000.000000000000000 ) ;
#8461=LINE ( 'NONE', #19355, #18951 ) ;
#8464=FACE_OUTER_BOUND ( 'NONE', #71168, .T. ) ;
#8471=CARTESIAN_POINT ( 'NONE',  ( 11.99999999999999822, 0.000000000000000000, 0.000000000000000000 ) ) ;
#8472=CARTESIAN_POINT ( 'NONE',  ( 11.99999999999999822, -0.8261519478436571973, 77.49459641780886443 ) ) ;
#8482=ORIENTED_EDGE ( 'NONE', *, *, #37794, .F. ) ;
#8493=EDGE_LOOP ( 'NONE', ( #41062, #44934, #6398, #59628 ) ) ;
#8495=AXIS2_PLACEMENT_3D ( 'NONE', #23913, #70868, #70483 ) ;
#8501=CARTESIAN_POINT ( 'NONE',  ( 0.000000000000000000, -71.91182617369167929, -28.89263327155821059 ) ) ;
#8505=DIRECTION ( 'NONE',  ( -1.000000000000000000, -0.000000000000000000, -0.000000000000000000 ) ) ;
#8515=CIRCLE ( 'NONE', #14510, 31.99999999999998934 ) ;
#8525=CARTESIAN_POINT ( 'NONE',  ( 11.99999999999999822, 35.91791733033476675, 68.67312586195008350 ) ) ;
#8535=LINE ( 'NONE', #70924, #43044 ) ;
#8537=CARTESIAN_POINT ( 'NONE',  ( 0.000000000000000000, -65.58780272294100655, 36.73666225445870737 ) ) ;
#8541=CARTESIAN_POINT ( 'NONE',  ( 0.000000000000000000, -0.8261519478425841667, -77.49459641780886443 ) ) ;
#8543=ORIENTED_EDGE ( 'NONE', *, *, #30901, .T. ) ;
#8544=DIRECTION ( 'NONE',  ( -1.000000000000000000, -0.000000000000000000, 0.000000000000000000 ) ) ;
#8556=CYLINDRICAL_SURFACE ( 'NONE', #69534, 82.00000000000000000 ) ;
#8586=EDGE_CURVE ( 'NONE', #27635, #8982, #67412, .T. ) ;
#8590=DIRECTION ( 'NONE',  ( 0.000000000000000000, -0.1045284632676569680, -0.9945218953682730678 ) ) ;
#8596=CARTESIAN_POINT ( 'NONE',  ( 5.999999999999999112, -46.11716303203233736, 67.80270845531873647 ) ) ;
#8599=DIRECTION ( 'NONE',  ( -1.000000000000000000, 0.000000000000000000, 0.000000000000000000 ) ) ;
#8625=VECTOR ( 'NONE', #42002, 1000.000000000000000 ) ;
#8627=ORIENTED_EDGE ( 'NONE', *, *, #37117, .F. ) ;
#8629=AXIS2_PLACEMENT_3D ( 'NONE', #34362, #21974, #57305 ) ;
#8632=ORIENTED_EDGE ( 'NONE', *, *, #12870, .T. ) ;
#8634=CYLINDRICAL_SURFACE ( 'NONE', #28688, 31.99999999999999289 ) ;
#8636=CARTESIAN_POINT ( 'NONE',  ( -10.00000000000000000, 0.000000000000000000, 0.000000000000000000 ) ) ;
#8648=ADVANCED_FACE ( 'NONE', ( #740 ), #22526, .T. ) ;
#8652=DIRECTION ( 'NONE',  ( 0.000000000000000000, 0.5877852522924797984, 0.8090169943749426773 ) ) ;
#8655=CARTESIAN_POINT ( 'NONE',  ( 6.000000000000000000, -15.33399622253424432, -80.55351364060604169 ) ) ;
#8660=DIRECTION ( 'NONE',  ( -1.000000000000000000, 0.000000000000000000, -0.000000000000000000 ) ) ;
#8661=CARTESIAN_POINT ( 'NONE',  ( -10.00000000000000000, 0.000000000000000000, 0.000000000000000000 ) ) ;
#8667=ORIENTED_EDGE ( 'NONE', *, *, #67032, .T. ) ;
#8669=CARTESIAN_POINT ( 'NONE',  ( 11.99999999999999822, -77.32052557432837148, -5.256550761633681290 ) ) ;
#8675=ORIENTED_EDGE ( 'NONE', *, *, #5559, .F. ) ;
#8685=ORIENTED_EDGE ( 'NONE', *, *, #28181, .F. ) ;
#8690=ORIENTED_EDGE ( 'NONE', *, *, #46591, .F. ) ;
#8693=CARTESIAN_POINT ( 'NONE',  ( 15.00000000000000000, 18.84667830672579569, -18.68964196561269375 ) ) ;
#8707=AXIS2_PLACEMENT_3D ( 'NONE', #72160, #16141, #66897 ) ;
#8711=CARTESIAN_POINT ( 'NONE',  ( 0.000000000000000000, 77.16300072079660310, 27.74655509720697211 ) ) ;
#8725=FACE_OUTER_BOUND ( 'NONE', #57234, .T. ) ;
#8729=AXIS2_PLACEMENT_3D ( 'NONE', #24633, #53574, #37415 ) ;
#8730=CARTESIAN_POINT ( 'NONE',  ( 11.99999999999999822, -74.65374052328654386, 8.840884882374837161 ) ) ;
#8731=ORIENTED_EDGE ( 'NONE', *, *, #20605, .T. ) ;
#8733=ORIENTED_EDGE ( 'NONE', *, *, #35638, .F. ) ;
#8736=LINE ( 'NONE', #70019, #55468 ) ;
#8737=EDGE_CURVE ( 'NONE', #48817, #57658, #375, .T. ) ;
#8740=DIRECTION ( 'NONE',  ( 1.000000000000000000, -0.000000000000000000, -0.000000000000000000 ) ) ;
#8759=ORIENTED_EDGE ( 'NONE', *, *, #7564, .F. ) ;
#8765=ORIENTED_EDGE ( 'NONE', *, *, #61518, .T. ) ;
#8771=CYLINDRICAL_SURFACE ( 'NONE', #54430, 31.99999999999998579 ) ;
#8772=EDGE_CURVE ( 'NONE', #1170, #13817, #58573, .T. ) ;
#8804=EDGE_CURVE ( 'NONE', #20251, #62534, #42400, .T. ) ;
#8812=LINE ( 'NONE', #26092, #73477 ) ;
#8815=DIRECTION ( 'NONE',  ( -1.000000000000000000, -0.000000000000000000, -0.000000000000000000 ) ) ;
#8820=ORIENTED_EDGE ( 'NONE', *, *, #50052, .T. ) ;
#8821=EDGE_CURVE ( 'NONE', #28736, #15229, #6201, .T. ) ;
#8830=ORIENTED_EDGE ( 'NONE', *, *, #40385, .T. ) ;
#8842=LINE ( 'NONE', #71980, #44878 ) ;
#8859=DIRECTION ( 'NONE',  ( 0.000000000000000000, 0.000000000000000000, 1.000000000000000000 ) ) ;
#8865=ORIENTED_EDGE ( 'NONE', *, *, #58982, .T. ) ;
#8878=ORIENTED_EDGE ( 'NONE', *, *, #1387, .F. ) ;
#8884=DIRECTION ( 'NONE',  ( 0.000000000000000000, -0.7431448254773871387, 0.6691306063588661202 ) ) ;
#8886=ORIENTED_EDGE ( 'NONE', *, *, #46587, .T. ) ;
#8890=ORIENTED_EDGE ( 'NONE', *, *, #71338, .F. ) ;
#8894=DIRECTION ( 'NONE',  ( 1.000000000000000000, -0.000000000000000000, 0.000000000000000000 ) ) ;
#8904=DIRECTION ( 'NONE',  ( -1.000000000000000000, 0.000000000000000000, -0.000000000000000000 ) ) ;
#8910=LINE ( 'NONE', #32568, #42008 ) ;
#8912=DIRECTION ( 'NONE',  ( -0.000000000000000000, 0.8090169943749426773, -0.5877852522924796874 ) ) ;
#8915=EDGE_LOOP ( 'NONE', ( #58379, #71808, #12743, #71647 ) ) ;
#8924=DIRECTION ( 'NONE',  ( 0.000000000000000000, -0.2079116908177554846, 0.9781476007338064660 ) ) ;
#8928=DIRECTION ( 'NONE',  ( 0.000000000000000000, -0.7604059656000227152, -0.6494480483301933171 ) ) ;
#8929=AXIS2_PLACEMENT_3D ( 'NONE', #69891, #63909, #35325 ) ;
#8933=ORIENTED_EDGE ( 'NONE', *, *, #58938, .T. ) ;
#8936=EDGE_CURVE ( 'NONE', #10371, #66496, #54231, .T. ) ;
#8937=AXIS2_PLACEMENT_3D ( 'NONE', #5262, #34181, #750 ) ;
#8941=PLANE ( 'NONE',  #58222 ) ;
#8947=DIRECTION ( 'NONE',  ( 1.000000000000000000, -0.000000000000000000, 0.000000000000000000 ) ) ;
#8948=CIRCLE ( 'NONE', #18548, 77.49899999999999523 ) ;
#8959=ORIENTED_EDGE ( 'NONE', *, *, #28802, .F. ) ;
#8964=CIRCLE ( 'NONE', #36548, 31.99999999999998224 ) ;
#8971=ORIENTED_EDGE ( 'NONE', *, *, #45406, .T. ) ;
#8974=ORIENTED_EDGE ( 'NONE', *, *, #63035, .F. ) ;
#8975=ORIENTED_EDGE ( 'NONE', *, *, #39970, .F. ) ;
#8982=VERTEX_POINT ( 'NONE', #31842 ) ;
#8988=ORIENTED_EDGE ( 'NONE', *, *, #42369, .F. ) ;
#8989=LINE ( 'NONE', #19521, #10930 ) ;
#8990=EDGE_CURVE ( 'NONE', #5309, #2536, #72792, .T. ) ;
#8991=VERTEX_POINT ( 'NONE', #48770 ) ;
#8994=ORIENTED_EDGE ( 'NONE', *, *, #43037, .F. ) ;
#8999=CARTESIAN_POINT ( 'NONE',  ( 0.000000000000000000, 65.64334221924964652, -41.19522573413665611 ) ) ;
#9000=CARTESIAN_POINT ( 'NONE',  ( 15.00000000000000000, 16.83928648764945635, 16.46020748918027010 ) ) ;
#9009=CARTESIAN_POINT ( 'NONE',  ( 11.99999999999999822, 12.93880638057315657, 76.41127070299278046 ) ) ;
#9010=ADVANCED_FACE ( 'NONE', ( #14558 ), #20937, .T. ) ;
#9012=ADVANCED_FACE ( 'NONE', ( #54415 ), #55152, .T. ) ;
#9019=EDGE_CURVE ( 'NONE', #42337, #62167, #58891, .T. ) ;
#9031=CARTESIAN_POINT ( 'NONE',  ( 11.99999999999999822, -80.55351364060599906, 15.33399622253457295 ) ) ;
#9032=CIRCLE ( 'NONE', #46290, 82.00000000000000000 ) ;
#9034=CIRCLE ( 'NONE', #4400, 31.99999999999998579 ) ;
#9042=VERTEX_POINT ( 'NONE', #66446 ) ;
#9053=ORIENTED_EDGE ( 'NONE', *, *, #55746, .T. ) ;
#9054=DIRECTION ( 'NONE',  ( -1.000000000000000000, 0.000000000000000000, 0.000000000000000000 ) ) ;
#9062=ADVANCED_FACE ( 'NONE', ( #43156 ), #26578, .F. ) ;
#9066=FACE_OUTER_BOUND ( 'NONE', #30586, .T. ) ;
#9068=DIRECTION ( 'NONE',  ( 1.000000000000000000, 0.000000000000000000, 0.000000000000000000 ) ) ;
#9071=EDGE_CURVE ( 'NONE', #46914, #39517, #3691, .T. ) ;
#9079=ORIENTED_EDGE ( 'NONE', *, *, #54247, .T. ) ;
#9081=CARTESIAN_POINT ( 'NONE',  ( 0.000000000000000000, 0.000000000000000000, 0.000000000000000000 ) ) ;
#9084=AXIS2_PLACEMENT_3D ( 'NONE', #29504, #41181, #52440 ) ;
#9085=CARTESIAN_POINT ( 'NONE',  ( 15.00000000000000000, -19.89357724625003598, -12.59942793731059041 ) ) ;
#9092=ORIENTED_EDGE ( 'NONE', *, *, #30363, .T. ) ;
#9094=VERTEX_POINT ( 'NONE', #50999 ) ;
#9099=EDGE_CURVE ( 'NONE', #61610, #58013, #22901, .T. ) ;
#9108=DIRECTION ( 'NONE',  ( 0.000000000000000000, 0.7604059656000322631, -0.6494480483301821039 ) ) ;
#9111=AXIS2_PLACEMENT_3D ( 'NONE', #16623, #21890, #16251 ) ;
#9112=DIRECTION ( 'NONE',  ( -1.000000000000000000, -0.000000000000000000, -0.000000000000000000 ) ) ;
#9116=DIRECTION ( 'NONE',  ( -1.000000000000000000, -0.000000000000000000, 0.000000000000000000 ) ) ;
#9123=DIRECTION ( 'NONE',  ( -1.000000000000000000, 0.000000000000000000, 0.000000000000000000 ) ) ;
#9124=ORIENTED_EDGE ( 'NONE', *, *, #5473, .F. ) ;
#9127=CARTESIAN_POINT ( 'NONE',  ( 11.99999999999999822, 65.59268652807210742, 36.72794159290264560 ) ) ;
#9138=ORIENTED_EDGE ( 'NONE', *, *, #14680, .T. ) ;
#9141=EDGE_CURVE ( 'NONE', #4678, #4428, #46874, .T. ) ;
#9142=VERTEX_POINT ( 'NONE', #45001 ) ;
#9164=DIRECTION ( 'NONE',  ( -1.000000000000000000, -0.000000000000000000, 0.000000000000000000 ) ) ;
#9167=ORIENTED_EDGE ( 'NONE', *, *, #26303, .F. ) ;
#9174=DIRECTION ( 'NONE',  ( -1.000000000000000000, 0.000000000000000000, 0.000000000000000000 ) ) ;
#9177=LINE ( 'NONE', #3203, #65077 ) ;
#9179=DIRECTION ( 'NONE',  ( 0.000000000000000000, 0.000000000000000000, 1.000000000000000000 ) ) ;
#9181=ORIENTED_EDGE ( 'NONE', *, *, #43055, .F. ) ;
#9183=EDGE_LOOP ( 'NONE', ( #61514, #69800, #5956, #38867 ) ) ;
#9195=VERTEX_POINT ( 'NONE', #68302 ) ;
#9200=DIRECTION ( 'NONE',  ( 0.000000000000000000, 0.000000000000000000, 1.000000000000000000 ) ) ;
#9211=CARTESIAN_POINT ( 'NONE',  ( 11.99999999999999822, 0.000000000000000000, 0.000000000000000000 ) ) ;
#9217=DIRECTION ( 'NONE',  ( -1.000000000000000000, -0.000000000000000000, -0.000000000000000000 ) ) ;
#9220=VERTEX_POINT ( 'NONE', #39734 ) ;
#9223=CIRCLE ( 'NONE', #18824, 82.00000000000000000 ) ;
#9235=EDGE_LOOP ( 'NONE', ( #60570, #11534, #14327, #6048 ) ) ;
#9266=LINE ( 'NONE', #60418, #32307 ) ;
#9267=VERTEX_POINT ( 'NONE', #24646 ) ;
#9274=DIRECTION ( 'NONE',  ( -1.000000000000000000, -0.000000000000000000, 0.000000000000000000 ) ) ;
#9275=EDGE_CURVE ( 'NONE', #65739, #14207, #49268, .T. ) ;
#9281=CARTESIAN_POINT ( 'NONE',  ( 0.000000000000000000, 46.11716303203283474, -67.80270845531839541 ) ) ;
#9282=FACE_OUTER_BOUND ( 'NONE', #63, .T. ) ;
#9285=DIRECTION ( 'NONE',  ( 0.000000000000000000, 0.000000000000000000, 1.000000000000000000 ) ) ;
#9299=AXIS2_PLACEMENT_3D ( 'NONE', #15844, #26374, #32743 ) ;
#9300=VECTOR ( 'NONE', #61832, 1000.000000000000000 ) ;
#9301=CARTESIAN_POINT ( 'NONE',  ( 11.99999999999999822, -27.74655509720725277, 77.16300072079650363 ) ) ;
#9306=ADVANCED_FACE ( 'NONE', ( #41946 ), #47577, .T. ) ;
#9313=ORIENTED_EDGE ( 'NONE', *, *, #32434, .T. ) ;
#9322=ORIENTED_EDGE ( 'NONE', *, *, #68240, .T. ) ;
#9340=ADVANCED_FACE ( 'NONE', ( #41205 ), #31013, .T. ) ;
#9344=DIRECTION ( 'NONE',  ( -1.000000000000000000, -0.000000000000000000, -0.000000000000000000 ) ) ;
#9345=VERTEX_POINT ( 'NONE', #35919 ) ;
#9348=EDGE_CURVE ( 'NONE', #50206, #25707, #29528, .T. ) ;
#9351=CIRCLE ( 'NONE', #51376, 77.49900000000000944 ) ;
#9355=ORIENTED_EDGE ( 'NONE', *, *, #20258, .T. ) ;
#9369=VECTOR ( 'NONE', #9615, 1000.000000000000000 ) ;
#9377=CIRCLE ( 'NONE', #22591, 77.49899999999999523 ) ;
#9378=DIRECTION ( 'NONE',  ( 1.000000000000000000, 0.000000000000000000, 0.000000000000000000 ) ) ;
#9394=DIRECTION ( 'NONE',  ( -1.000000000000000000, -0.000000000000000000, -0.000000000000000000 ) ) ;
#9399=ORIENTED_EDGE ( 'NONE', *, *, #47945, .F. ) ;
#9416=ORIENTED_EDGE ( 'NONE', *, *, #49320, .F. ) ;
#9419=CARTESIAN_POINT ( 'NONE',  ( 11.99999999999999822, 0.000000000000000000, 0.000000000000000000 ) ) ;
#9422=CARTESIAN_POINT ( 'NONE',  ( 0.000000000000000000, -36.73666225445940370, 65.58780272294062286 ) ) ;
#9423=FACE_OUTER_BOUND ( 'NONE', #37899, .T. ) ;
#9424=EDGE_CURVE ( 'NONE', #44140, #60240, #58629, .T. ) ;
#9428=ORIENTED_EDGE ( 'NONE', *, *, #18568, .F. ) ;
#9436=EDGE_CURVE ( 'NONE', #55763, #47354, #33447, .T. ) ;
#9439=ORIENTED_EDGE ( 'NONE', *, *, #69770, .F. ) ;
#9443=CIRCLE ( 'NONE', #20404, 31.99999999999998579 ) ;
#9458=DIRECTION ( 'NONE',  ( 0.000000000000000000, 0.8090169943749445647, 0.5877852522924770229 ) ) ;
#9460=CIRCLE ( 'NONE', #50240, 77.49899999999999523 ) ;
#9462=CARTESIAN_POINT ( 'NONE',  ( 11.99999999999999822, 41.19522573413826194, -65.64334221924865176 ) ) ;
#9464=DIRECTION ( 'NONE',  ( 0.000000000000000000, 1.000000000000000000, 3.491481338843133355E-15 ) ) ;
#9468=CARTESIAN_POINT ( 'NONE',  ( 11.99999999999999822, 77.19088730480524418, 6.903761155838049390 ) ) ;
#9469=EDGE_LOOP ( 'NONE', ( #33001, #60948, #27646, #23876 ) ) ;
#9471=CIRCLE ( 'NONE', #58864, 82.00000000000000000 ) ;
#9481=VECTOR ( 'NONE', #63150, 1000.000000000000000 ) ;
#9499=ORIENTED_EDGE ( 'NONE', *, *, #36150, .T. ) ;
#9503=CARTESIAN_POINT ( 'NONE',  ( 11.99999999999999822, -74.65491531819111515, -8.830959090343204920 ) ) ;
#9508=AXIS2_PLACEMENT_3D ( 'NONE', #19060, #42011, #64947 ) ;
#9511=AXIS2_PLACEMENT_3D ( 'NONE', #61636, #43253, #66176 ) ;
#9513=ORIENTED_EDGE ( 'NONE', *, *, #35169, .T. ) ;
#9520=EDGE_LOOP ( 'NONE', ( #25737, #51509, #27207, #39210 ) ) ;
#9521=VERTEX_POINT ( 'NONE', #59991 ) ;
#9527=ORIENTED_EDGE ( 'NONE', *, *, #43968, .T. ) ;
#9528=VERTEX_POINT ( 'NONE', #38146 ) ;
#9529=CYLINDRICAL_SURFACE ( 'NONE', #67089, 82.00000000000000000 ) ;
#9540=DIRECTION ( 'NONE',  ( -1.000000000000000000, -0.000000000000000000, -0.000000000000000000 ) ) ;
#9542=DIRECTION ( 'NONE',  ( 0.000000000000000000, 0.9723699203976756689, 0.2334453638559095823 ) ) ;
#9543=AXIS2_PLACEMENT_3D ( 'NONE', #27420, #21400, #61652 ) ;
#9545=ORIENTED_EDGE ( 'NONE', *, *, #30817, .F. ) ;
#9549=ORIENTED_EDGE ( 'NONE', *, *, #73602, .T. ) ;
#9554=CARTESIAN_POINT ( 'NONE',  ( 15.00000000000000000, 26.50000000000000355, -1.500000000000000000 ) ) ;
#9555=DIRECTION ( 'NONE',  ( -1.000000000000000000, -0.000000000000000000, -0.000000000000000000 ) ) ;
#9556=CARTESIAN_POINT ( 'NONE',  ( 11.99999999999999822, 0.000000000000000000, 0.000000000000000000 ) ) ;
#9563=CARTESIAN_POINT ( 'NONE',  ( 0.000000000000000000, 0.000000000000000000, 0.000000000000000000 ) ) ;
#9565=CARTESIAN_POINT ( 'NONE',  ( 11.99999999999999822, 0.000000000000000000, 0.000000000000000000 ) ) ;
#9566=DIRECTION ( 'NONE',  ( -1.000000000000000000, 0.000000000000000000, 0.000000000000000000 ) ) ;
#9570=AXIS2_PLACEMENT_3D ( 'NONE', #45259, #50508, #56154 ) ;
#9578=DIRECTION ( 'NONE',  ( -1.000000000000000000, 0.000000000000000000, 0.000000000000000000 ) ) ;
#9581=CARTESIAN_POINT ( 'NONE',  ( 0.000000000000000000, -34.44570377933647620, 69.42325613327427902 ) ) ;
#9583=EDGE_CURVE ( 'NONE', #35612, #33344, #74210, .T. ) ;
#9605=ORIENTED_EDGE ( 'NONE', *, *, #5144, .F. ) ;
#9615=DIRECTION ( 'NONE',  ( -1.000000000000000000, 0.000000000000000000, 0.000000000000000000 ) ) ;
#9623=FACE_OUTER_BOUND ( 'NONE', #51130, .T. ) ;
#9630=VERTEX_POINT ( 'NONE', #61834 ) ;
#9634=EDGE_LOOP ( 'NONE', ( #15336, #63512, #40741, #26798 ) ) ;
#9645=CARTESIAN_POINT ( 'NONE',  ( 12.00000000000000000, -13.04903810567646971, 19.60159698893442481 ) ) ;
#9646=ORIENTED_EDGE ( 'NONE', *, *, #73983, .T. ) ;
#9648=VECTOR ( 'NONE', #16938, 1000.000000000000227 ) ;
#9651=FACE_OUTER_BOUND ( 'NONE', #41059, .T. ) ;
#9657=ORIENTED_EDGE ( 'NONE', *, *, #31848, .F. ) ;
#9660=CARTESIAN_POINT ( 'NONE',  ( 0.000000000000000000, 0.000000000000000000, 0.000000000000000000 ) ) ;
#9663=DIRECTION ( 'NONE',  ( 0.000000000000000000, 0.000000000000000000, 1.000000000000000000 ) ) ;
#9675=EDGE_CURVE ( 'NONE', #23551, #5835, #15416, .T. ) ;
#9677=AXIS2_PLACEMENT_3D ( 'NONE', #60441, #32585, #8924 ) ;
#9685=VECTOR ( 'NONE', #49222, 1000.000000000000000 ) ;
#9692=EDGE_CURVE ( 'NONE', #11414, #13516, #2274, .T. ) ;
#9696=CYLINDRICAL_SURFACE ( 'NONE', #10169, 31.99999999999998579 ) ;
#9702=VERTEX_POINT ( 'NONE', #45675 ) ;
#9713=ORIENTED_EDGE ( 'NONE', *, *, #66976, .F. ) ;
#9718=CYLINDRICAL_SURFACE ( 'NONE', #33154, 31.99999999999998579 ) ;
#9722=CARTESIAN_POINT ( 'NONE',  ( 11.99999999999999822, 73.95703589264006439, -23.16143007188350822 ) ) ;
#9724=AXIS2_PLACEMENT_3D ( 'NONE', #56538, #72677, #45257 ) ;
#9727=CARTESIAN_POINT ( 'NONE',  ( -10.00000000000000000, 0.000000000000000000, 0.000000000000000000 ) ) ;
#9728=AXIS2_PLACEMENT_3D ( 'NONE', #43052, #3580, #25745 ) ;
#9746=DIRECTION ( 'NONE',  ( -1.000000000000000000, -0.000000000000000000, -0.000000000000000000 ) ) ;
#9748=EDGE_CURVE ( 'NONE', #4389, #32475, #26212, .T. ) ;
#9751=DIRECTION ( 'NONE',  ( 0.000000000000000000, 0.000000000000000000, 1.000000000000000000 ) ) ;
#9752=VECTOR ( 'NONE', #45852, 1000.000000000000227 ) ;
#9767=ADVANCED_FACE ( 'NONE', ( #24214 ), #18189, .F. ) ;
#9770=DIRECTION ( 'NONE',  ( 0.000000000000000000, -0.7431448254773954654, -0.6691306063588569053 ) ) ;
#9772=FACE_OUTER_BOUND ( 'NONE', #59467, .T. ) ;
#9773=AXIS2_PLACEMENT_3D ( 'NONE', #32500, #20853, #49052 ) ;
#9803=CARTESIAN_POINT ( 'NONE',  ( 0.000000000000000000, 0.000000000000000000, 0.000000000000000000 ) ) ;
#9810=CYLINDRICAL_SURFACE ( 'NONE', #6626, 77.49899999999999523 ) ;
#9830=DIRECTION ( 'NONE',  ( -1.000000000000000000, 0.000000000000000000, 0.000000000000000000 ) ) ;
#9853=CARTESIAN_POINT ( 'NONE',  ( 11.99999999999999822, 0.000000000000000000, 0.000000000000000000 ) ) ;
#9855=EDGE_CURVE ( 'NONE', #20819, #19963, #70789, .T. ) ;
#9858=CYLINDRICAL_SURFACE ( 'NONE', #55090, 82.00000000000000000 ) ;
#9859=CARTESIAN_POINT ( 'NONE',  ( 11.99999999999999822, -46.53671651293907274, -59.03961581697448935 ) ) ;
#9863=FACE_OUTER_BOUND ( 'NONE', #26775, .T. ) ;
#9872=CARTESIAN_POINT ( 'NONE',  ( 0.000000000000000000, -40.65526001592663619, 71.21200624218782593 ) ) ;
#9880=ORIENTED_EDGE ( 'NONE', *, *, #15038, .T. ) ;
#9881=ORIENTED_EDGE ( 'NONE', *, *, #23845, .T. ) ;
#9887=ORIENTED_EDGE ( 'NONE', *, *, #36435, .T. ) ;
#9889=DIRECTION ( 'NONE',  ( 0.000000000000000000, -0.9723699203976789995, 0.2334453638558956767 ) ) ;
#9893=VERTEX_POINT ( 'NONE', #21131 ) ;
#9895=ORIENTED_EDGE ( 'NONE', *, *, #34092, .T. ) ;
#9903=CARTESIAN_POINT ( 'NONE',  ( -10.00000000000000000, 0.000000000000000000, 0.000000000000000000 ) ) ;
#9916=CARTESIAN_POINT ( 'NONE',  ( 11.99999999999999822, -73.72996012237429397, -14.67089635893794508 ) ) ;
#9918=DIRECTION ( 'NONE',  ( 0.000000000000000000, 0.8660254037844363761, -0.5000000000000039968 ) ) ;
#9920=ORIENTED_EDGE ( 'NONE', *, *, #39907, .F. ) ;
#9921=EDGE_CURVE ( 'NONE', #47732, #64554, #10712, .T. ) ;
#9927=CYLINDRICAL_SURFACE ( 'NONE', #34808, 77.49899999999999523 ) ;
#9931=CARTESIAN_POINT ( 'NONE',  ( 11.99999999999999822, 81.34940948281335693, 10.30890764327412334 ) ) ;
#9933=ADVANCED_FACE ( 'NONE', ( #72626 ), #38065, .T. ) ;
#9942=DIRECTION ( 'NONE',  ( 0.000000000000000000, 0.000000000000000000, 1.000000000000000000 ) ) ;
#9943=CARTESIAN_POINT ( 'NONE',  ( 11.99999999999999822, -70.53064760720297954, -26.01480285779911839 ) ) ;
#9944=EDGE_CURVE ( 'NONE', #65739, #24686, #49700, .T. ) ;
#9945=ADVANCED_FACE ( 'NONE', ( #49342 ), #14013, .T. ) ;
#9948=CARTESIAN_POINT ( 'NONE',  ( 11.99999999999999822, 0.000000000000000000, 0.000000000000000000 ) ) ;
#9964=ORIENTED_EDGE ( 'NONE', *, *, #69501, .T. ) ;
#9966=VERTEX_POINT ( 'NONE', #32413 ) ;
#9968=CARTESIAN_POINT ( 'NONE',  ( 11.99999999999999822, -71.27951684758045303, 30.41916302227090085 ) ) ;
#9971=AXIS2_PLACEMENT_3D ( 'NONE', #55903, #10032, #67185 ) ;
#9982=VECTOR ( 'NONE', #70983, 1000.000000000000000 ) ;
#9983=DIRECTION ( 'NONE',  ( 0.000000000000000000, -0.8090169943749503378, -0.5877852522924690293 ) ) ;
#9989=EDGE_CURVE ( 'NONE', #4105, #62322, #59939, .T. ) ;
#9990=ORIENTED_EDGE ( 'NONE', *, *, #31852, .T. ) ;
#9994=EDGE_CURVE ( 'NONE', #52585, #68824, #2289, .T. ) ;
#10002=CARTESIAN_POINT ( 'NONE',  ( 11.99999999999999822, 0.000000000000000000, 0.000000000000000000 ) ) ;
#10004=DIRECTION ( 'NONE',  ( -0.000000000000000000, -0.3090169943749572767, -0.9510565162951503115 ) ) ;
#10005=DIRECTION ( 'NONE',  ( 1.000000000000000000, 0.000000000000000000, -0.000000000000000000 ) ) ;
#10007=ORIENTED_EDGE ( 'NONE', *, *, #70342, .F. ) ;
#10017=DIRECTION ( 'NONE',  ( 0.000000000000000000, 0.9510565162951544194, -0.3090169943749448977 ) ) ;
#10018=LINE ( 'NONE', #54404, #72534 ) ;
#10022=DIRECTION ( 'NONE',  ( -1.000000000000000000, 0.000000000000000000, -0.000000000000000000 ) ) ;
#10023=ORIENTED_EDGE ( 'NONE', *, *, #54268, .F. ) ;
#10029=CARTESIAN_POINT ( 'NONE',  ( 0.000000000000000000, 74.65491531819105830, 8.830959090343693418 ) ) ;
#10032=DIRECTION ( 'NONE',  ( -1.000000000000000000, 0.000000000000000000, 0.000000000000000000 ) ) ;
#10033=EDGE_CURVE ( 'NONE', #66558, #5889, #20248, .T. ) ;
#10034=DIRECTION ( 'NONE',  ( -1.000000000000000000, -0.000000000000000000, 0.000000000000000000 ) ) ;
#10041=ORIENTED_EDGE ( 'NONE', *, *, #66376, .T. ) ;
#10048=VECTOR ( 'NONE', #22193, 1000.000000000000000 ) ;
#10058=ORIENTED_EDGE ( 'NONE', *, *, #51354, .T. ) ;
#10059=EDGE_CURVE ( 'NONE', #21642, #46085, #20311, .T. ) ;
#10060=CARTESIAN_POINT ( 'NONE',  ( 11.99999999999999822, -10.30890764327323872, -81.34940948281347062 ) ) ;
#10066=CIRCLE ( 'NONE', #56885, 82.00000000000000000 ) ;
#10074=EDGE_LOOP ( 'NONE', ( #31170, #72002, #47823, #58927 ) ) ;
#10078=EDGE_CURVE ( 'NONE', #48721, #7988, #50305, .T. ) ;
#10082=CARTESIAN_POINT ( 'NONE',  ( 11.99999999999999822, -73.44644590900077219, 24.73286445877677764 ) ) ;
#10090=DIRECTION ( 'NONE',  ( 0.000000000000000000, 0.9945218953682730678, -0.1045284632676570929 ) ) ;
#10093=DIRECTION ( 'NONE',  ( 0.000000000000000000, 0.4067366430757887730, -0.9135454576426059736 ) ) ;
#10094=ORIENTED_EDGE ( 'NONE', *, *, #47052, .T. ) ;
#10107=ORIENTED_EDGE ( 'NONE', *, *, #42346, .F. ) ;
#10114=AXIS2_PLACEMENT_3D ( 'NONE', #11432, #44554, #73841 ) ;
#10137=DIRECTION ( 'NONE',  ( -0.000000000000000000, 0.4999999999999921174, -0.8660254037844432595 ) ) ;
#10141=CIRCLE ( 'NONE', #52170, 31.99999999999998579 ) ;
#10163=ORIENTED_EDGE ( 'NONE', *, *, #45450, .F. ) ;
#10165=CARTESIAN_POINT ( 'NONE',  ( 0.000000000000000000, -75.11764819372149304, 2.946379043146075905 ) ) ;
#10168=CARTESIAN_POINT ( 'NONE',  ( 0.000000000000000000, 8.966570791700705811, 81.50828551894228724 ) ) ;
#10169=AXIS2_PLACEMENT_3D ( 'NONE', #4076, #59725, #26973 ) ;
#10175=ORIENTED_EDGE ( 'NONE', *, *, #44383, .F. ) ;
#10176=ORIENTED_EDGE ( 'NONE', *, *, #18154, .T. ) ;
#10180=ORIENTED_EDGE ( 'NONE', *, *, #55064, .F. ) ;
#10181=VERTEX_POINT ( 'NONE', #60873 ) ;
#10182=LINE ( 'NONE', #33103, #12101 ) ;
#10184=VERTEX_POINT ( 'NONE', #49209 ) ;
#10185=EDGE_CURVE ( 'NONE', #237, #25980, #38687, .T. ) ;
#10187=EDGE_LOOP ( 'NONE', ( #41812, #65272, #41711, #17592 ) ) ;
#10190=ORIENTED_EDGE ( 'NONE', *, *, #53039, .F. ) ;
#10203=DIRECTION ( 'NONE',  ( -1.000000000000000000, -0.000000000000000000, -0.000000000000000000 ) ) ;
#10204=DIRECTION ( 'NONE',  ( -1.000000000000000000, 0.000000000000000000, 0.000000000000000000 ) ) ;
#10209=DIRECTION ( 'NONE',  ( -1.000000000000000000, -0.000000000000000000, 0.000000000000000000 ) ) ;
#10210=CIRCLE ( 'NONE', #1833, 82.00000000000000000 ) ;
#10212=AXIS2_PLACEMENT_3D ( 'NONE', #44030, #50396, #31991 ) ;
#10214=CIRCLE ( 'NONE', #63116, 82.00000000000000000 ) ;
#10223=ORIENTED_EDGE ( 'NONE', *, *, #27512, .F. ) ;
#10224=CARTESIAN_POINT ( 'NONE',  ( 11.99999999999999822, 81.50828551894227303, 8.966570791700986476 ) ) ;
#10229=CARTESIAN_POINT ( 'NONE',  ( 0.000000000000000000, -22.90783923731685334, 78.73519480814945837 ) ) ;
#10230=DIRECTION ( 'NONE',  ( 0.000000000000000000, -0.5877852522924801315, 0.8090169943749423442 ) ) ;
#10239=ORIENTED_EDGE ( 'NONE', *, *, #62397, .F. ) ;
#10240=ADVANCED_FACE ( 'NONE', ( #37209 ), #8634, .T. ) ;
#10242=ORIENTED_EDGE ( 'NONE', *, *, #60934, .T. ) ;
#10243=DIRECTION ( 'NONE',  ( 0.000000000000000000, 0.000000000000000000, 1.000000000000000000 ) ) ;
#10258=VECTOR ( 'NONE', #57373, 1000.000000000000000 ) ;
#10260=AXIS2_PLACEMENT_3D ( 'NONE', #69739, #70100, #18601 ) ;
#10262=ORIENTED_EDGE ( 'NONE', *, *, #66198, .F. ) ;
#10268=VECTOR ( 'NONE', #43015, 1000.000000000000114 ) ;
#10280=ORIENTED_EDGE ( 'NONE', *, *, #3744, .F. ) ;
#10283=AXIS2_PLACEMENT_3D ( 'NONE', #12510, #36183, #59129 ) ;
#10295=ADVANCED_FACE ( 'NONE', ( #51526 ), #57551, .F. ) ;
#10296=EDGE_CURVE ( 'NONE', #13681, #12324, #22976, .T. ) ;
#10304=DIRECTION ( 'NONE',  ( -1.000000000000000000, 0.000000000000000000, 0.000000000000000000 ) ) ;
#10308=CARTESIAN_POINT ( 'NONE',  ( 0.000000000000000000, 41.19522573413826194, -65.64334221924865176 ) ) ;
#10312=LINE ( 'NONE', #20849, #21015 ) ;
#10313=CYLINDRICAL_SURFACE ( 'NONE', #69401, 31.99999999999998579 ) ;
#10318=VECTOR ( 'NONE', #35076, 1000.000000000000000 ) ;
#10322=ORIENTED_EDGE ( 'NONE', *, *, #13581, .T. ) ;
#10331=ORIENTED_EDGE ( 'NONE', *, *, #17541, .T. ) ;
#10333=LINE ( 'NONE', #20510, #39267 ) ;
#10336=DIRECTION ( 'NONE',  ( -1.000000000000000000, -0.000000000000000000, -0.000000000000000000 ) ) ;
#10337=ADVANCED_FACE ( 'NONE', ( #30069 ), #48476, .T. ) ;
#10342=EDGE_CURVE ( 'NONE', #719, #27052, #64768, .T. ) ;
#10355=CARTESIAN_POINT ( 'NONE',  ( 15.00000000000000000, -4.261787119645322974, -26.19803753235774835 ) ) ;
#10357=CARTESIAN_POINT ( 'NONE',  ( 0.000000000000000000, 0.000000000000000000, 0.000000000000000000 ) ) ;
#10371=VERTEX_POINT ( 'NONE', #1550 ) ;
#10373=CIRCLE ( 'NONE', #21198, 31.99999999999998934 ) ;
#10375=CARTESIAN_POINT ( 'NONE',  ( 11.99999999999999822, -15.33399622253540606, 80.55351364060582853 ) ) ;
#10376=LINE ( 'NONE', #22405, #14609 ) ;
#10381=DIRECTION ( 'NONE',  ( -0.000000000000000000, -0.9135454576426058626, -0.4067366430757889395 ) ) ;
#10387=ORIENTED_EDGE ( 'NONE', *, *, #3403, .T. ) ;
#10390=AXIS2_PLACEMENT_3D ( 'NONE', #71408, #31561, #71041 ) ;
#10393=DIRECTION ( 'NONE',  ( -0.000000000000000000, -0.3090169943749450088, 0.9510565162951543083 ) ) ;
#10397=VERTEX_POINT ( 'NONE', #35355 ) ;
#10401=FACE_OUTER_BOUND ( 'NONE', #6888, .T. ) ;
#10406=DIRECTION ( 'NONE',  ( 0.000000000000000000, 0.000000000000000000, 1.000000000000000000 ) ) ;
#10411=DIRECTION ( 'NONE',  ( 0.000000000000000000, 0.7071067811865487940, -0.7071067811865462405 ) ) ;
#10414=CARTESIAN_POINT ( 'NONE',  ( 0.000000000000000000, 17.28742895386189105, -75.54627589209924565 ) ) ;
#10418=AXIS2_PLACEMENT_3D ( 'NONE', #61623, #66882, #15370 ) ;
#10427=ORIENTED_EDGE ( 'NONE', *, *, #39817, .T. ) ;
#10434=CARTESIAN_POINT ( 'NONE',  ( 11.99999999999999822, 65.59268652807210742, 36.72794159290264560 ) ) ;
#10445=VERTEX_POINT ( 'NONE', #2661 ) ;
#10453=ORIENTED_EDGE ( 'NONE', *, *, #11978, .T. ) ;
#10460=VERTEX_POINT ( 'NONE', #71025 ) ;
#10466=CARTESIAN_POINT ( 'NONE',  ( 0.000000000000000000, 75.11725578898472122, -2.956366410619845730 ) ) ;
#10472=ORIENTED_EDGE ( 'NONE', *, *, #48624, .F. ) ;
#10474=DIRECTION ( 'NONE',  ( 0.000000000000000000, 0.000000000000000000, 1.000000000000000000 ) ) ;
#10481=CARTESIAN_POINT ( 'NONE',  ( 11.99999999999999822, -8.830959090342926032, 74.65491531819115778 ) ) ;
#10484=CIRCLE ( 'NONE', #5676, 82.00000000000000000 ) ;
#10491=CARTESIAN_POINT ( 'NONE',  ( 11.99999999999999822, 0.000000000000000000, 0.000000000000000000 ) ) ;
#10494=CARTESIAN_POINT ( 'NONE',  ( 11.99999999999999822, 71.27951684758069462, -30.41916302227037150 ) ) ;
#10496=EDGE_CURVE ( 'NONE', #63285, #58109, #43230, .T. ) ;
#10507=DIRECTION ( 'NONE',  ( -1.000000000000000000, 0.000000000000000000, 0.000000000000000000 ) ) ;
#10518=EDGE_CURVE ( 'NONE', #58524, #66160, #26647, .T. ) ;
#10548=AXIS2_PLACEMENT_3D ( 'NONE', #63110, #50682, #45812 ) ;
#10549=VERTEX_POINT ( 'NONE', #61616 ) ;
#10557=VECTOR ( 'NONE', #29363, 1000.000000000000000 ) ;
#10590=DIRECTION ( 'NONE',  ( 0.000000000000000000, 0.4067366430757889950, -0.9135454576426058626 ) ) ;
#10597=AXIS2_PLACEMENT_3D ( 'NONE', #52393, #65175, #63701 ) ;
#10598=DIRECTION ( 'NONE',  ( 0.000000000000000000, 0.000000000000000000, 1.000000000000000000 ) ) ;
#10612=EDGE_CURVE ( 'NONE', #48915, #1061, #73171, .T. ) ;
#10618=DIRECTION ( 'NONE',  ( 0.000000000000000000, 0.4539904997395477482, -0.8910065241883674547 ) ) ;
#10620=VERTEX_POINT ( 'NONE', #60150 ) ;
#10626=ORIENTED_EDGE ( 'NONE', *, *, #38642, .F. ) ;
#10633=VERTEX_POINT ( 'NONE', #3376 ) ;
#10634=AXIS2_PLACEMENT_3D ( 'NONE', #39544, #22248, #60725 ) ;
#10647=DIRECTION ( 'NONE',  ( -1.000000000000000000, -0.000000000000000000, -0.000000000000000000 ) ) ;
#10657=DIRECTION ( 'NONE',  ( 0.000000000000000000, 0.000000000000000000, 1.000000000000000000 ) ) ;
#10663=ORIENTED_EDGE ( 'NONE', *, *, #63071, .F. ) ;
#10667=AXIS2_PLACEMENT_3D ( 'NONE', #71891, #43718, #3872 ) ;
#10672=DIRECTION ( 'NONE',  ( -1.000000000000000000, -0.000000000000000000, 0.000000000000000000 ) ) ;
#10675=DIRECTION ( 'NONE',  ( -1.000000000000000000, -0.000000000000000000, -0.000000000000000000 ) ) ;
#10677=ORIENTED_EDGE ( 'NONE', *, *, #29843, .T. ) ;
#10681=CARTESIAN_POINT ( 'NONE',  ( 11.99999999999999822, -69.42325613327466272, 34.44570377933573724 ) ) ;
#10684=DIRECTION ( 'NONE',  ( -1.000000000000000000, 0.000000000000000000, -0.000000000000000000 ) ) ;
#10686=CARTESIAN_POINT ( 'NONE',  ( 12.00000000000000000, -25.60904388321925040, -6.976881207771165272 ) ) ;
#10687=EDGE_CURVE ( 'NONE', #13012, #25707, #5978, .T. ) ;
#10694=FACE_OUTER_BOUND ( 'NONE', #46553, .T. ) ;
#10706=ADVANCED_FACE ( 'NONE', ( #27769 ), #34512, .T. ) ;
#10711=AXIS2_PLACEMENT_3D ( 'NONE', #15676, #32945, #55895 ) ;
#10712=CIRCLE ( 'NONE', #7063, 31.99999999999998579 ) ;
#10716=AXIS2_PLACEMENT_3D ( 'NONE', #27289, #4029, #73158 ) ;
#10721=VECTOR ( 'NONE', #36119, 1000.000000000000000 ) ;
#10730=ORIENTED_EDGE ( 'NONE', *, *, #56302, .T. ) ;
#10735=CARTESIAN_POINT ( 'NONE',  ( -10.00000000000000000, 0.000000000000000000, 0.000000000000000000 ) ) ;
#10740=CARTESIAN_POINT ( 'NONE',  ( 11.99999999999999822, 0.000000000000000000, 0.000000000000000000 ) ) ;
#10745=VERTEX_POINT ( 'NONE', #40530 ) ;
#10751=CYLINDRICAL_SURFACE ( 'NONE', #28284, 77.49899999999999523 ) ;
#10761=EDGE_LOOP ( 'NONE', ( #31247, #57768, #34294, #71749 ) ) ;
#10762=VERTEX_POINT ( 'NONE', #5602 ) ;
#10763=VECTOR ( 'NONE', #16437, 1000.000000000000000 ) ;
#10768=VERTEX_POINT ( 'NONE', #11955 ) ;
#10779=DIRECTION ( 'NONE',  ( -1.000000000000000000, 0.000000000000000000, -0.000000000000000000 ) ) ;
#10782=AXIS2_PLACEMENT_3D ( 'NONE', #44106, #21914, #9889 ) ;
#10789=DIRECTION ( 'NONE',  ( 0.000000000000000000, -1.000000000000000000, -1.047444401652940007E-14 ) ) ;
#10792=DIRECTION ( 'NONE',  ( -1.000000000000000000, -0.000000000000000000, 0.000000000000000000 ) ) ;
#10798=EDGE_LOOP ( 'NONE', ( #69527, #52040, #25731, #33109 ) ) ;
#10802=FACE_OUTER_BOUND ( 'NONE', #47240, .T. ) ;
#10816=FACE_OUTER_BOUND ( 'NONE', #10919, .T. ) ;
#10820=EDGE_LOOP ( 'NONE', ( #30215, #6031, #5671, #52031 ) ) ;
#10823=AXIS2_PLACEMENT_3D ( 'NONE', #16050, #44258, #4418 ) ;
#10837=DIRECTION ( 'NONE',  ( 0.000000000000000000, -0.6494480483301904306, 0.7604059656000252687 ) ) ;
#10843=DIRECTION ( 'NONE',  ( -1.000000000000000000, 0.000000000000000000, 0.000000000000000000 ) ) ;
#10848=CARTESIAN_POINT ( 'NONE',  ( 11.99999999999999822, 55.20638768913760686, 51.02545421589343988 ) ) ;
#10852=DIRECTION ( 'NONE',  ( -1.000000000000000000, -0.000000000000000000, -0.000000000000000000 ) ) ;
#10853=ORIENTED_EDGE ( 'NONE', *, *, #59107, .T. ) ;
#10860=CARTESIAN_POINT ( 'NONE',  ( 0.000000000000000000, -59.03961581697432592, 46.53671651293927880 ) ) ;
#10863=VECTOR ( 'NONE', #29995, 1000.000000000000000 ) ;
#10864=EDGE_CURVE ( 'NONE', #46178, #38445, #11995, .T. ) ;
#10870=VECTOR ( 'NONE', #71669, 1000.000000000000000 ) ;
#10874=DIRECTION ( 'NONE',  ( 0.000000000000000000, 0.000000000000000000, -1.000000000000000000 ) ) ;
#10876=DIRECTION ( 'NONE',  ( -1.000000000000000000, -0.000000000000000000, -0.000000000000000000 ) ) ;
#10877=EDGE_CURVE ( 'NONE', #31156, #56792, #7176, .T. ) ;
#10880=DIRECTION ( 'NONE',  ( 0.000000000000000000, 0.000000000000000000, 1.000000000000000000 ) ) ;
#10883=AXIS2_PLACEMENT_3D ( 'NONE', #70759, #8365, #13622 ) ;
#10898=EDGE_CURVE ( 'NONE', #45130, #6635, #2444, .T. ) ;
#10899=EDGE_CURVE ( 'NONE', #45508, #55684, #25207, .T. ) ;
#10902=ORIENTED_EDGE ( 'NONE', *, *, #6247, .T. ) ;
#10911=ORIENTED_EDGE ( 'NONE', *, *, #27499, .T. ) ;
#10919=EDGE_LOOP ( 'NONE', ( #67892, #22869, #74067, #71018 ) ) ;
#10925=VERTEX_POINT ( 'NONE', #63851 ) ;
#10928=CARTESIAN_POINT ( 'NONE',  ( 11.99999999999999822, 74.65374052328648702, 8.840884882375350529 ) ) ;
#10930=VECTOR ( 'NONE', #54480, 999.9999999999998863 ) ;
#10934=CARTESIAN_POINT ( 'NONE',  ( 0.000000000000000000, -14.67089635893764665, 73.72996012237435082 ) ) ;
#10946=ORIENTED_EDGE ( 'NONE', *, *, #71800, .F. ) ;
#10947=LINE ( 'NONE', #44794, #19380 ) ;
#10951=EDGE_CURVE ( 'NONE', #70963, #66932, #46920, .T. ) ;
#10952=CARTESIAN_POINT ( 'NONE',  ( 15.00000000000000000, 5.835314593368777558, 22.81335362449846471 ) ) ;
#10966=AXIS2_PLACEMENT_3D ( 'NONE', #38325, #66891, #19270 ) ;
#10970=DIRECTION ( 'NONE',  ( -1.000000000000000000, 0.000000000000000000, 0.000000000000000000 ) ) ;
#10973=ADVANCED_FACE ( 'NONE', ( #9651 ), #26563, .F. ) ;
#10975=ADVANCED_FACE ( 'NONE', ( #60427 ), #61533, .T. ) ;
#10995=ORIENTED_EDGE ( 'NONE', *, *, #34092, .F. ) ;
#11000=ORIENTED_EDGE ( 'NONE', *, *, #27220, .T. ) ;
#11001=VERTEX_POINT ( 'NONE', #31088 ) ;
#11002=FACE_OUTER_BOUND ( 'NONE', #72293, .T. ) ;
#11020=CARTESIAN_POINT ( 'NONE',  ( 0.000000000000000000, 0.000000000000000000, 0.000000000000000000 ) ) ;
#11023=EDGE_CURVE ( 'NONE', #8327, #42112, #8910, .T. ) ;
#11036=DIRECTION ( 'NONE',  ( -1.000000000000000000, 0.000000000000000000, 0.000000000000000000 ) ) ;
#11042=ADVANCED_FACE ( 'NONE', ( #48756 ), #49857, .T. ) ;
#11044=FACE_OUTER_BOUND ( 'NONE', #62351, .T. ) ;
#11046=VECTOR ( 'NONE', #21328, 1000.000000000000000 ) ;
#11049=VECTOR ( 'NONE', #14898, 1000.000000000000000 ) ;
#11053=DIRECTION ( 'NONE',  ( 1.000000000000000000, 0.000000000000000000, 0.000000000000000000 ) ) ;
#11059=VERTEX_POINT ( 'NONE', #44236 ) ;
#11078=CIRCLE ( 'NONE', #53092, 31.99999999999998579 ) ;
#11083=DIRECTION ( 'NONE',  ( 0.000000000000000000, 0.5877852522924684742, 0.8090169943749506709 ) ) ;
#11088=AXIS2_PLACEMENT_3D ( 'NONE', #22394, #45342, #68266 ) ;
#11089=ORIENTED_EDGE ( 'NONE', *, *, #32143, .T. ) ;
#11098=FACE_OUTER_BOUND ( 'NONE', #2751, .T. ) ;
#11121=LINE ( 'NONE', #27667, #50196 ) ;
#11124=DIRECTION ( 'NONE',  ( -1.000000000000000000, 0.000000000000000000, -0.000000000000000000 ) ) ;
#11140=CARTESIAN_POINT ( 'NONE',  ( 11.99999999999999822, 0.000000000000000000, 0.000000000000000000 ) ) ;
#11148=EDGE_CURVE ( 'NONE', #63122, #19859, #1260, .T. ) ;
#11157=DIRECTION ( 'NONE',  ( 0.000000000000000000, -0.8090169943749531134, 0.5877852522924653655 ) ) ;
#11163=EDGE_LOOP ( 'NONE', ( #23026, #35625, #48356, #2067 ) ) ;
#11167=VERTEX_POINT ( 'NONE', #4398 ) ;
#11170=DIRECTION ( 'NONE',  ( 1.000000000000000000, -0.000000000000000000, -0.000000000000000000 ) ) ;
#11184=EDGE_LOOP ( 'NONE', ( #63193, #6323, #8830, #38578 ) ) ;
#11185=ORIENTED_EDGE ( 'NONE', *, *, #39817, .F. ) ;
#11188=ORIENTED_EDGE ( 'NONE', *, *, #28444, .T. ) ;
#11189=AXIS2_PLACEMENT_3D ( 'NONE', #62771, #50710, #51086 ) ;
#11193=EDGE_CURVE ( 'NONE', #45315, #63075, #13174, .T. ) ;
#11199=VERTEX_POINT ( 'NONE', #40443 ) ;
#11201=VERTEX_POINT ( 'NONE', #21667 ) ;
#11227=CARTESIAN_POINT ( 'NONE',  ( 11.99999999999999822, 81.90746397400394585, -3.894527615416972566 ) ) ;
#11228=EDGE_CURVE ( 'NONE', #66160, #52399, #26427, .T. ) ;
#11231=EDGE_CURVE ( 'NONE', #17107, #16098, #27670, .T. ) ;
#11232=DIRECTION ( 'NONE',  ( -1.000000000000000000, -0.000000000000000000, -0.000000000000000000 ) ) ;
#11236=DIRECTION ( 'NONE',  ( 0.000000000000000000, 0.000000000000000000, 1.000000000000000000 ) ) ;
#11238=CARTESIAN_POINT ( 'NONE',  ( 0.000000000000000000, -65.64334221924937651, 41.19522573413711797 ) ) ;
#11240=CARTESIAN_POINT ( 'NONE',  ( 11.99999999999999822, 0.000000000000000000, 0.000000000000000000 ) ) ;
#11245=CIRCLE ( 'NONE', #41235, 31.99999999999998934 ) ;
#11249=DIRECTION ( 'NONE',  ( 0.000000000000000000, 0.000000000000000000, 1.000000000000000000 ) ) ;
#11250=AXIS2_PLACEMENT_3D ( 'NONE', #61924, #22059, #10406 ) ;
#11253=DIRECTION ( 'NONE',  ( 0.000000000000000000, 0.000000000000000000, 1.000000000000000000 ) ) ;
#11256=CARTESIAN_POINT ( 'NONE',  ( 11.99999999999999822, 0.000000000000000000, 0.000000000000000000 ) ) ;
#11257=CARTESIAN_POINT ( 'NONE',  ( 0.000000000000000000, -5.256550761633393520, 77.32052557432838569 ) ) ;
#11260=CARTESIAN_POINT ( 'NONE',  ( 0.000000000000000000, 0.000000000000000000, 0.000000000000000000 ) ) ;
#11277=VERTEX_POINT ( 'NONE', #28416 ) ;
#11280=EDGE_CURVE ( 'NONE', #51135, #63042, #51349, .T. ) ;
#11282=CARTESIAN_POINT ( 'NONE',  ( 11.99999999999999822, 0.000000000000000000, 0.000000000000000000 ) ) ;
#11287=ORIENTED_EDGE ( 'NONE', *, *, #71770, .T. ) ;
#11288=ORIENTED_EDGE ( 'NONE', *, *, #52726, .F. ) ;
#11291=DIRECTION ( 'NONE',  ( -1.000000000000000000, 0.000000000000000000, -0.000000000000000000 ) ) ;
#11293=CARTESIAN_POINT ( 'NONE',  ( 11.99999999999999822, -78.73519480814969995, 22.90783923731599359 ) ) ;
#11294=ORIENTED_EDGE ( 'NONE', *, *, #35084, .F. ) ;
#11296=ORIENTED_EDGE ( 'NONE', *, *, #68606, .F. ) ;
#11298=CARTESIAN_POINT ( 'NONE',  ( 11.99999999999999822, -76.41127070299280888, 12.93880638057290788 ) ) ;
#11308=DIRECTION ( 'NONE',  ( -1.000000000000000000, 0.000000000000000000, -0.000000000000000000 ) ) ;
#11314=DIRECTION ( 'NONE',  ( 0.000000000000000000, 0.3826834323650840086, 0.9238795325112891810 ) ) ;
#11323=ORIENTED_EDGE ( 'NONE', *, *, #24020, .T. ) ;
#11333=AXIS2_PLACEMENT_3D ( 'NONE', #46515, #24327, #40885 ) ;
#11334=ORIENTED_EDGE ( 'NONE', *, *, #52049, .F. ) ;
#11338=AXIS2_PLACEMENT_3D ( 'NONE', #20758, #62105, #56087 ) ;
#11339=CIRCLE ( 'NONE', #7752, 31.99999999999998224 ) ;
#11344=CARTESIAN_POINT ( 'NONE',  ( 0.000000000000000000, -74.18225833017864090, -34.94270380257717790 ) ) ;
#11352=AXIS2_PLACEMENT_3D ( 'NONE', #5223, #68739, #29226 ) ;
#11353=EDGE_CURVE ( 'NONE', #2104, #12353, #70860, .T. ) ;
#11357=ORIENTED_EDGE ( 'NONE', *, *, #52746, .F. ) ;
#11369=CARTESIAN_POINT ( 'NONE',  ( 11.99999999999999822, 55.38113227695783536, 54.21277698773694453 ) ) ;
#11383=CYLINDRICAL_SURFACE ( 'NONE', #56456, 31.99999999999998579 ) ;
#11384=DIRECTION ( 'NONE',  ( 0.000000000000000000, 0.000000000000000000, 1.000000000000000000 ) ) ;
#11400=DIRECTION ( 'NONE',  ( -1.000000000000000000, 0.000000000000000000, -0.000000000000000000 ) ) ;
#11402=CYLINDRICAL_SURFACE ( 'NONE', #12158, 82.00000000000000000 ) ;
#11404=DIRECTION ( 'NONE',  ( 0.000000000000000000, 0.000000000000000000, 1.000000000000000000 ) ) ;
#11408=CARTESIAN_POINT ( 'NONE',  ( 11.99999999999999822, -31.46837873494930093, -68.27212725128309501 ) ) ;
#11409=LINE ( 'NONE', #6883, #38169 ) ;
#11414=VERTEX_POINT ( 'NONE', #2398 ) ;
#11416=VECTOR ( 'NONE', #67154, 1000.000000000000000 ) ;
#11418=CARTESIAN_POINT ( 'NONE',  ( 11.99999999999999822, -12.93880638057369659, 76.41127070299266677 ) ) ;
#11419=DIRECTION ( 'NONE',  ( -1.000000000000000000, 0.000000000000000000, 0.000000000000000000 ) ) ;
#11420=FACE_OUTER_BOUND ( 'NONE', #57743, .T. ) ;
#11424=AXIS2_PLACEMENT_3D ( 'NONE', #71706, #37149, #55169 ) ;
#11432=CARTESIAN_POINT ( 'NONE',  ( 0.000000000000000000, 8.840884882376133902, -74.65374052328640175 ) ) ;
#11440=ORIENTED_EDGE ( 'NONE', *, *, #31852, .F. ) ;
#11444=EDGE_LOOP ( 'NONE', ( #7661, #54568, #68630, #73101 ) ) ;
#11450=AXIS2_PLACEMENT_3D ( 'NONE', #34817, #23531, #5521 ) ;
#11454=VERTEX_POINT ( 'NONE', #9462 ) ;
#11459=CIRCLE ( 'NONE', #26912, 31.99999999999999289 ) ;
#11460=ORIENTED_EDGE ( 'NONE', *, *, #48377, .T. ) ;
#11463=VERTEX_POINT ( 'NONE', #4963 ) ;
#11475=EDGE_CURVE ( 'NONE', #45880, #46053, #55703, .T. ) ;
#11477=CYLINDRICAL_SURFACE ( 'NONE', #15866, 31.99999999999998579 ) ;
#11486=DIRECTION ( 'NONE',  ( 0.000000000000000000, 0.000000000000000000, 1.000000000000000000 ) ) ;
#11493=ORIENTED_EDGE ( 'NONE', *, *, #46879, .T. ) ;
#11499=ORIENTED_EDGE ( 'NONE', *, *, #10899, .T. ) ;
#11500=ORIENTED_EDGE ( 'NONE', *, *, #72401, .F. ) ;
#11504=DIRECTION ( 'NONE',  ( 0.000000000000000000, 0.000000000000000000, -1.000000000000000000 ) ) ;
#11507=CARTESIAN_POINT ( 'NONE',  ( 11.99999999999999822, -65.59268652807237743, 36.72794159290217664 ) ) ;
#11508=DIRECTION ( 'NONE',  ( -1.000000000000000000, -0.000000000000000000, -0.000000000000000000 ) ) ;
#11511=CARTESIAN_POINT ( 'NONE',  ( 6.000000000000000000, 3.894527615419050903, -81.90746397400384637 ) ) ;
#11515=AXIS2_PLACEMENT_3D ( 'NONE', #7255, #6876, #64034 ) ;
#11519=EDGE_LOOP ( 'NONE', ( #26173, #60326, #17755, #27328 ) ) ;
#11525=EDGE_CURVE ( 'NONE', #24794, #12008, #3478, .T. ) ;
#11527=DIRECTION ( 'NONE',  ( -1.000000000000000000, 0.000000000000000000, 0.000000000000000000 ) ) ;
#11529=PLANE ( 'NONE',  #40824 ) ;
#11531=CARTESIAN_POINT ( 'NONE',  ( 0.000000000000000000, 0.000000000000000000, 0.000000000000000000 ) ) ;
#11534=ORIENTED_EDGE ( 'NONE', *, *, #38642, .T. ) ;
#11537=CARTESIAN_POINT ( 'NONE',  ( 0.000000000000000000, 0.000000000000000000, 0.000000000000000000 ) ) ;
#11539=LINE ( 'NONE', #57420, #20683 ) ;
#11576=VERTEX_POINT ( 'NONE', #21858 ) ;
#11610=FILL_AREA_STYLE_COLOUR ( '', #38310 ) ;
#11613=DIRECTION ( 'NONE',  ( -1.000000000000000000, 0.000000000000000000, 0.000000000000000000 ) ) ;
#11621=ADVANCED_FACE ( 'NONE', ( #5333 ), #33880, .T. ) ;
#11630=EDGE_CURVE ( 'NONE', #23395, #55194, #45920, .T. ) ;
#11639=FACE_OUTER_BOUND ( 'NONE', #63348, .T. ) ;
#11642=CARTESIAN_POINT ( 'NONE',  ( 11.99999999999999822, 0.000000000000000000, 0.000000000000000000 ) ) ;
#11645=AXIS2_PLACEMENT_3D ( 'NONE', #44314, #66508, #38676 ) ;
#11646=ADVANCED_FACE ( 'NONE', ( #46644 ), #17700, .T. ) ;
#11649=PLANE ( 'NONE',  #63311 ) ;
#11650=DIRECTION ( 'NONE',  ( -1.000000000000000000, -0.000000000000000000, 0.000000000000000000 ) ) ;
#11651=ORIENTED_EDGE ( 'NONE', *, *, #27940, .T. ) ;
#11656=DIRECTION ( 'NONE',  ( 0.000000000000000000, 0.000000000000000000, 1.000000000000000000 ) ) ;
#11657=DIRECTION ( 'NONE',  ( 0.000000000000000000, 0.000000000000000000, 1.000000000000000000 ) ) ;
#11661=AXIS2_PLACEMENT_3D ( 'NONE', #57214, #41038, #29356 ) ;
#11663=ORIENTED_EDGE ( 'NONE', *, *, #46683, .T. ) ;
#11672=CARTESIAN_POINT ( 'NONE',  ( 11.99999999999999822, 39.47590169984944453, -71.87247863392373404 ) ) ;
#11681=ORIENTED_EDGE ( 'NONE', *, *, #50154, .F. ) ;
#11687=EDGE_CURVE ( 'NONE', #37410, #38445, #58293, .T. ) ;
#11693=LINE ( 'NONE', #23371, #8081 ) ;
#11694=ORIENTED_EDGE ( 'NONE', *, *, #42475, .T. ) ;
#11700=CARTESIAN_POINT ( 'NONE',  ( 11.99999999999999822, 75.11764819372149304, -2.946379043146603482 ) ) ;
#11702=CIRCLE ( 'NONE', #71705, 77.49899999999999523 ) ;
#11703=DIRECTION ( 'NONE',  ( 1.000000000000000000, 0.000000000000000000, 0.000000000000000000 ) ) ;
#11707=FACE_OUTER_BOUND ( 'NONE', #40806, .T. ) ;
#11712=DIRECTION ( 'NONE',  ( -1.000000000000000000, -0.000000000000000000, -0.000000000000000000 ) ) ;
#11713=ORIENTED_EDGE ( 'NONE', *, *, #32433, .F. ) ;
#11733=ORIENTED_EDGE ( 'NONE', *, *, #41079, .T. ) ;
#11736=CARTESIAN_POINT ( 'NONE',  ( 11.99999999999999822, 62.50329211542435104, 41.76937507738811917 ) ) ;
#11740=DIRECTION ( 'NONE',  ( 1.000000000000000000, -0.000000000000000000, -0.000000000000000000 ) ) ;
#11756=DIRECTION ( 'NONE',  ( -1.000000000000000000, 0.000000000000000000, -0.000000000000000000 ) ) ;
#11764=DIRECTION ( 'NONE',  ( 0.000000000000000000, -0.8910065241883723397, 0.4539904997395382003 ) ) ;
#11772=DIRECTION ( 'NONE',  ( 0.000000000000000000, -0.9945218953682742891, -0.1045284632676436315 ) ) ;
#11774=DIRECTION ( 'NONE',  ( 1.000000000000000000, -0.000000000000000000, -0.000000000000000000 ) ) ;
#11777=ADVANCED_FACE ( 'NONE', ( #13534 ), #48492, .T. ) ;
#11788=CYLINDRICAL_SURFACE ( 'NONE', #15814, 77.49899999999999523 ) ;
#11805=EDGE_CURVE ( 'NONE', #42720, #24576, #26488, .T. ) ;
#11809=EDGE_LOOP ( 'NONE', ( #28088, #18874, #71463, #14028 ) ) ;
#11819=ORIENTED_EDGE ( 'NONE', *, *, #41908, .T. ) ;
#11823=CIRCLE ( 'NONE', #53863, 31.99999999999998579 ) ;
#11831=CARTESIAN_POINT ( 'NONE',  ( 5.999999999999999112, -55.16347631942998930, -60.67117009219195722 ) ) ;
#11837=ORIENTED_EDGE ( 'NONE', *, *, #24751, .T. ) ;
#11840=VECTOR ( 'NONE', #3245, 1000.000000000000000 ) ;
#11843=DIRECTION ( 'NONE',  ( 0.000000000000000000, 0.8090169943749498938, 0.5877852522924696954 ) ) ;
#11848=ORIENTED_EDGE ( 'NONE', *, *, #61730, .T. ) ;
#11851=DIRECTION ( 'NONE',  ( -1.000000000000000000, 0.000000000000000000, -0.000000000000000000 ) ) ;
#11855=EDGE_CURVE ( 'NONE', #15073, #69736, #68518, .T. ) ;
#11865=EDGE_CURVE ( 'NONE', #60856, #22572, #37951, .T. ) ;
#11869=CARTESIAN_POINT ( 'NONE',  ( 0.000000000000000000, -74.74816331893404708, -33.71516098798818462 ) ) ;
#11877=CARTESIAN_POINT ( 'NONE',  ( -10.00000000000000000, 0.000000000000000000, 0.000000000000000000 ) ) ;
#11883=DIRECTION ( 'NONE',  ( 0.000000000000000000, -1.000000000000000000, -1.047444401652940007E-14 ) ) ;
#11896=AXIS2_PLACEMENT_3D ( 'NONE', #21703, #67574, #39008 ) ;
#11899=EDGE_CURVE ( 'NONE', #34985, #56906, #27396, .T. ) ;
#11900=CARTESIAN_POINT ( 'NONE',  ( 15.00000000000000000, -22.67460108101774452, 6.353146135318220367 ) ) ;
#11901=CYLINDRICAL_SURFACE ( 'NONE', #17999, 82.00000000000000000 ) ;
#11912=CARTESIAN_POINT ( 'NONE',  ( 11.99999999999999822, -8.840884882375609877, 74.65374052328647281 ) ) ;
#11939=DIRECTION ( 'NONE',  ( 0.000000000000000000, 0.000000000000000000, 1.000000000000000000 ) ) ;
#11946=AXIS2_PLACEMENT_3D ( 'NONE', #41616, #59657, #29216 ) ;
#11950=DIRECTION ( 'NONE',  ( -0.000000000000000000, 0.000000000000000000, 1.000000000000000000 ) ) ;
#11953=EDGE_CURVE ( 'NONE', #63551, #54039, #37589, .T. ) ;
#11955=CARTESIAN_POINT ( 'NONE',  ( 0.000000000000000000, 81.50828551894240093, -8.966570791699810528 ) ) ;
#11961=DIRECTION ( 'NONE',  ( -1.000000000000000000, -0.000000000000000000, -0.000000000000000000 ) ) ;
#11963=VERTEX_POINT ( 'NONE', #49588 ) ;
#11966=ORIENTED_EDGE ( 'NONE', *, *, #45018, .F. ) ;
#11970=CARTESIAN_POINT ( 'NONE',  ( 6.000000000000000000, -78.73519480814971416, 22.90783923731599359 ) ) ;
#11972=CARTESIAN_POINT ( 'NONE',  ( 12.00000000000000000, -23.29833615347104470, 3.418703333116808629 ) ) ;
#11978=EDGE_CURVE ( 'NONE', #12324, #63432, #17615, .T. ) ;
#11991=CARTESIAN_POINT ( 'NONE',  ( 11.99999999999999822, 59.03961581697465277, -46.53671651293886669 ) ) ;
#11993=DIRECTION ( 'NONE',  ( -1.000000000000000000, -0.000000000000000000, 0.000000000000000000 ) ) ;
#11994=DIRECTION ( 'NONE',  ( 0.000000000000000000, 0.1045284632676459491, -0.9945218953682741780 ) ) ;
#11995=CIRCLE ( 'NONE', #44425, 82.00000000000000000 ) ;
#11997=VECTOR ( 'NONE', #11740, 1000.000000000000000 ) ;
#12007=DIRECTION ( 'NONE',  ( -1.000000000000000000, -0.000000000000000000, -0.000000000000000000 ) ) ;
#12008=VERTEX_POINT ( 'NONE', #28512 ) ;
#12013=ORIENTED_EDGE ( 'NONE', *, *, #1852, .F. ) ;
#12016=ORIENTED_EDGE ( 'NONE', *, *, #58938, .F. ) ;
#12027=EDGE_LOOP ( 'NONE', ( #65850, #23882, #58885, #40031 ) ) ;
#12037=DIRECTION ( 'NONE',  ( 0.000000000000000000, -0.1564344650402168801, -0.9876883405951399908 ) ) ;
#12049=DIRECTION ( 'NONE',  ( 0.000000000000000000, 1.000000000000000000, 3.491481338843133355E-15 ) ) ;
#12056=CIRCLE ( 'NONE', #46894, 31.99999999999999289 ) ;
#12059=AXIS2_PLACEMENT_3D ( 'NONE', #42609, #60284, #59534 ) ;
#12068=EDGE_CURVE ( 'NONE', #54039, #46823, #57779, .T. ) ;
#12091=ORIENTED_EDGE ( 'NONE', *, *, #52112, .F. ) ;
#12095=DIRECTION ( 'NONE',  ( -1.000000000000000000, 0.000000000000000000, -0.000000000000000000 ) ) ;
#12099=AXIS2_PLACEMENT_3D ( 'NONE', #32102, #48669, #9179 ) ;
#12101=VECTOR ( 'NONE', #1182, 1000.000000000000000 ) ;
#12102=ORIENTED_EDGE ( 'NONE', *, *, #23929, .F. ) ;
#12103=ORIENTED_EDGE ( 'NONE', *, *, #48145, .F. ) ;
#12104=AXIS2_PLACEMENT_3D ( 'NONE', #20944, #43168, #27319 ) ;
#12106=CARTESIAN_POINT ( 'NONE',  ( 0.000000000000000000, -70.53064760720297954, -26.01480285779911839 ) ) ;
#12108=ORIENTED_EDGE ( 'NONE', *, *, #27304, .T. ) ;
#12112=ADVANCED_FACE ( 'NONE', ( #7445 ), #30726, .T. ) ;
#12133=CARTESIAN_POINT ( 'NONE',  ( 6.000000000000000000, 68.55367621811204515, -44.99326035065983120 ) ) ;
#12134=LINE ( 'NONE', #74180, #22459 ) ;
#12136=CARTESIAN_POINT ( 'NONE',  ( 11.99999999999999822, 62.20884554314085335, -46.21855187248562657 ) ) ;
#12139=CARTESIAN_POINT ( 'NONE',  ( 11.99999999999999822, -75.16055320797043748, 18.89407956138231270 ) ) ;
#12153=CARTESIAN_POINT ( 'NONE',  ( 15.00000000000000000, 26.49999999999999645, 1.499999999999995781 ) ) ;
#12154=AXIS2_PLACEMENT_3D ( 'NONE', #48299, #32839, #56158 ) ;
#12158=AXIS2_PLACEMENT_3D ( 'NONE', #51250, #62944, #23073 ) ;
#12166=EDGE_CURVE ( 'NONE', #57064, #20511, #15351, .T. ) ;
#12172=VERTEX_POINT ( 'NONE', #20188 ) ;
#12182=ORIENTED_EDGE ( 'NONE', *, *, #16752, .T. ) ;
#12184=CARTESIAN_POINT ( 'NONE',  ( 12.00000000000000000, 23.49999999999999645, -1.500000000000003997 ) ) ;
#12191=VECTOR ( 'NONE', #34050, 1000.000000000000000 ) ;
#12192=ORIENTED_EDGE ( 'NONE', *, *, #67022, .F. ) ;
#12197=EDGE_LOOP ( 'NONE', ( #34593, #18579, #60758, #27088 ) ) ;
#12215=ORIENTED_EDGE ( 'NONE', *, *, #9675, .T. ) ;
#12217=ORIENTED_EDGE ( 'NONE', *, *, #30558, .F. ) ;
#12219=ORIENTED_EDGE ( 'NONE', *, *, #12280, .F. ) ;
#12226=DIRECTION ( 'NONE',  ( -1.000000000000000000, -0.000000000000000000, 0.000000000000000000 ) ) ;
#12229=ORIENTED_EDGE ( 'NONE', *, *, #40948, .T. ) ;
#12247=EDGE_CURVE ( 'NONE', #62825, #64440, #35741, .T. ) ;
#12256=CARTESIAN_POINT ( 'NONE',  ( 0.000000000000000000, 41.76937507738788469, 62.50329211542452157 ) ) ;
#12258=VECTOR ( 'NONE', #20827, 1000.000000000000000 ) ;
#12259=VECTOR ( 'NONE', #21637, 1000.000000000000000 ) ;
#12264=LINE ( 'NONE', #23552, #31613 ) ;
#12270=CARTESIAN_POINT ( 'NONE',  ( 0.000000000000000000, 80.28980883073758434, 16.65972982744962749 ) ) ;
#12271=ORIENTED_EDGE ( 'NONE', *, *, #30817, .T. ) ;
#12280=EDGE_CURVE ( 'NONE', #42081, #61582, #52551, .T. ) ;
#12281=CARTESIAN_POINT ( 'NONE',  ( 11.99999999999999822, 0.000000000000000000, 0.000000000000000000 ) ) ;
#12282=CARTESIAN_POINT ( 'NONE',  ( 0.000000000000000000, 0.000000000000000000, 0.000000000000000000 ) ) ;
#12304=ORIENTED_EDGE ( 'NONE', *, *, #53815, .T. ) ;
#12306=AXIS2_PLACEMENT_3D ( 'NONE', #29229, #41270, #35254 ) ;
#12312=CARTESIAN_POINT ( 'NONE',  ( 0.000000000000000000, -76.69515212746036070, 29.01471420065536932 ) ) ;
#12316=DIRECTION ( 'NONE',  ( 1.000000000000000000, -0.000000000000000000, -0.000000000000000000 ) ) ;
#12318=CIRCLE ( 'NONE', #38726, 82.00000000000000000 ) ;
#12320=ORIENTED_EDGE ( 'NONE', *, *, #16668, .F. ) ;
#12323=EDGE_CURVE ( 'NONE', #3905, #7045, #28055, .T. ) ;
#12324=VERTEX_POINT ( 'NONE', #34073 ) ;
#12325=ADVANCED_FACE ( 'NONE', ( #10401 ), #17522, .T. ) ;
#12342=LINE ( 'NONE', #46938, #41619 ) ;
#12351=ADVANCED_FACE ( 'NONE', ( #23178 ), #16040, .T. ) ;
#12353=VERTEX_POINT ( 'NONE', #62677 ) ;
#12355=CARTESIAN_POINT ( 'NONE',  ( 11.99999999999999822, 36.73666225445988687, -65.58780272294035285 ) ) ;
#12365=ORIENTED_EDGE ( 'NONE', *, *, #8936, .T. ) ;
#12373=EDGE_CURVE ( 'NONE', #42450, #53064, #4794, .T. ) ;
#12376=ORIENTED_EDGE ( 'NONE', *, *, #72075, .F. ) ;
#12380=VERTEX_POINT ( 'NONE', #16794 ) ;
#12385=DIRECTION ( 'NONE',  ( 0.000000000000000000, -0.07845909572783058006, -0.9969173337331290741 ) ) ;
#12388=VERTEX_POINT ( 'NONE', #51358 ) ;
#12389=EDGE_LOOP ( 'NONE', ( #67681, #59757, #41242, #11663 ) ) ;
#12390=DIRECTION ( 'NONE',  ( 0.000000000000000000, -0.7071067811865389130, -0.7071067811865561215 ) ) ;
#12392=VERTEX_POINT ( 'NONE', #63047 ) ;
#12396=ORIENTED_EDGE ( 'NONE', *, *, #21450, .F. ) ;
#12398=CARTESIAN_POINT ( 'NONE',  ( 0.000000000000000000, 0.000000000000000000, 0.000000000000000000 ) ) ;
#12399=VERTEX_POINT ( 'NONE', #11869 ) ;
#12400=CIRCLE ( 'NONE', #31601, 31.99999999999998579 ) ;
#12401=VERTEX_POINT ( 'NONE', #57757 ) ;
#12403=DIRECTION ( 'NONE',  ( 0.000000000000000000, 0.5224985647159500202, -0.8526401643540915121 ) ) ;
#12405=EDGE_CURVE ( 'NONE', #6672, #18572, #33323, .T. ) ;
#12407=EDGE_CURVE ( 'NONE', #65728, #61974, #58564, .T. ) ;
#12411=ORIENTED_EDGE ( 'NONE', *, *, #19614, .F. ) ;
#12419=CARTESIAN_POINT ( 'NONE',  ( 15.00000000000000000, 0.000000000000000000, 0.000000000000000000 ) ) ;
#12432=ORIENTED_EDGE ( 'NONE', *, *, #17815, .T. ) ;
#12444=CARTESIAN_POINT ( 'NONE',  ( 0.000000000000000000, 0.000000000000000000, 0.000000000000000000 ) ) ;
#12447=FACE_BOUND ( 'NONE', #69296, .T. ) ;
#12450=EDGE_CURVE ( 'NONE', #12353, #27755, #59230, .T. ) ;
#12457=CIRCLE ( 'NONE', #55665, 77.49900000000002365 ) ;
#12461=ORIENTED_EDGE ( 'NONE', *, *, #21923, .F. ) ;
#12465=AXIS2_PLACEMENT_3D ( 'NONE', #50149, #5071, #9942 ) ;
#12467=ORIENTED_EDGE ( 'NONE', *, *, #35205, .F. ) ;
#12470=ORIENTED_EDGE ( 'NONE', *, *, #18350, .F. ) ;
#12473=ORIENTED_EDGE ( 'NONE', *, *, #42427, .F. ) ;
#12474=CARTESIAN_POINT ( 'NONE',  ( 11.99999999999999822, 0.000000000000000000, 0.000000000000000000 ) ) ;
#12475=DIRECTION ( 'NONE',  ( 0.000000000000000000, 0.000000000000000000, -1.000000000000000000 ) ) ;
#12479=ORIENTED_EDGE ( 'NONE', *, *, #59881, .T. ) ;
#12497=VERTEX_POINT ( 'NONE', #53966 ) ;
#12498=ADVANCED_FACE ( 'NONE', ( #53220 ), #46468, .T. ) ;
#12499=AXIS2_PLACEMENT_3D ( 'NONE', #69473, #24722, #25088 ) ;
#12506=CARTESIAN_POINT ( 'NONE',  ( 6.000000000000000000, -22.90783923731685334, 78.73519480814945837 ) ) ;
#12510=CARTESIAN_POINT ( 'NONE',  ( 11.99999999999999822, 41.76937507738788469, 62.50329211542452157 ) ) ;
#12511=CARTESIAN_POINT ( 'NONE',  ( 11.99999999999999822, 41.76106447765489094, 62.50884508063442269 ) ) ;
#12513=CIRCLE ( 'NONE', #52119, 31.99999999999998934 ) ;
#12521=DIRECTION ( 'NONE',  ( 0.000000000000000000, 0.000000000000000000, 1.000000000000000000 ) ) ;
#12523=ORIENTED_EDGE ( 'NONE', *, *, #21666, .T. ) ;
#12536=AXIS2_PLACEMENT_3D ( 'NONE', #23603, #17959, #57449 ) ;
#12539=DIRECTION ( 'NONE',  ( 0.000000000000000000, 0.07845909572784512398, -0.9969173337331279638 ) ) ;
#12541=CARTESIAN_POINT ( 'NONE',  ( -10.00000000000000000, 0.000000000000000000, 0.000000000000000000 ) ) ;
#12543=DIRECTION ( 'NONE',  ( 0.000000000000000000, 0.3090169943749560555, 0.9510565162951506446 ) ) ;
#12544=EDGE_CURVE ( 'NONE', #42337, #34606, #5830, .T. ) ;
#12555=VECTOR ( 'NONE', #49148, 1000.000000000000000 ) ;
#12556=VERTEX_POINT ( 'NONE', #58866 ) ;
#12558=CARTESIAN_POINT ( 'NONE',  ( 15.00000000000000000, 23.49999999999999645, -1.500000000000003997 ) ) ;
#12567=VECTOR ( 'NONE', #67290, 1000.000000000000000 ) ;
#12576=ADVANCED_FACE ( 'NONE', ( #48315 ), #65615, .T. ) ;
#12577=ORIENTED_EDGE ( 'NONE', *, *, #14231, .F. ) ;
#12583=CARTESIAN_POINT ( 'NONE',  ( 0.000000000000000000, -63.18004540532994184, -44.88180994100444821 ) ) ;
#12598=CARTESIAN_POINT ( 'NONE',  ( 11.99999999999999822, 0.000000000000000000, 0.000000000000000000 ) ) ;
#12599=DIRECTION ( 'NONE',  ( 0.000000000000000000, -0.8660254037844427044, -0.4999999999999931166 ) ) ;
#12600=ORIENTED_EDGE ( 'NONE', *, *, #36812, .F. ) ;
#12603=EDGE_LOOP ( 'NONE', ( #62496, #62040, #73006, #17716 ) ) ;
#12604=VERTEX_POINT ( 'NONE', #43443 ) ;
#12610=CARTESIAN_POINT ( 'NONE',  ( 11.99999999999999822, 36.72794159290241822, 65.59268652807223532 ) ) ;
#12612=CARTESIAN_POINT ( 'NONE',  ( 12.00000000000000000, 26.49999999999999645, 1.499999999999995781 ) ) ;
#12615=DIRECTION ( 'NONE',  ( 0.000000000000000000, 0.000000000000000000, 1.000000000000000000 ) ) ;
#12616=CARTESIAN_POINT ( 'NONE',  ( 11.99999999999999822, 0.000000000000000000, 0.000000000000000000 ) ) ;
#12617=FACE_OUTER_BOUND ( 'NONE', #73215, .T. ) ;
#12618=FACE_OUTER_BOUND ( 'NONE', #20234, .T. ) ;
#12622=VECTOR ( 'NONE', #64651, 1000.000000000000000 ) ;
#12629=EDGE_CURVE ( 'NONE', #58250, #48071, #54697, .T. ) ;
#12631=AXIS2_PLACEMENT_3D ( 'NONE', #60821, #4062, #26596 ) ;
#12635=EDGE_CURVE ( 'NONE', #7033, #69733, #58607, .T. ) ;
#12637=ORIENTED_EDGE ( 'NONE', *, *, #41917, .T. ) ;
#12640=CARTESIAN_POINT ( 'NONE',  ( 15.00000000000000000, 23.59884966291538078, 12.14883922797231008 ) ) ;
#12652=CARTESIAN_POINT ( 'NONE',  ( 11.99999999999999822, 71.87247863392413194, 39.47590169984869846 ) ) ;
#12664=CYLINDRICAL_SURFACE ( 'NONE', #17394, 21.00000000000000000 ) ;
#12669=ORIENTED_EDGE ( 'NONE', *, *, #46591, .T. ) ;
#12679=DIRECTION ( 'NONE',  ( 0.000000000000000000, 0.7071067811865486830, -0.7071067811865463515 ) ) ;
#12680=EDGE_LOOP ( 'NONE', ( #66462, #56336, #62526, #59386 ) ) ;
#12684=ORIENTED_EDGE ( 'NONE', *, *, #15418, .T. ) ;
#12690=AXIS2_PLACEMENT_3D ( 'NONE', #72235, #60964, #20740 ) ;
#12697=EDGE_LOOP ( 'NONE', ( #60715, #11733, #38784, #37649 ) ) ;
#12702=DIRECTION ( 'NONE',  ( -1.000000000000000000, -0.000000000000000000, -0.000000000000000000 ) ) ;
#12709=DIRECTION ( 'NONE',  ( 0.000000000000000000, 0.000000000000000000, 1.000000000000000000 ) ) ;
#12717=CARTESIAN_POINT ( 'NONE',  ( 11.99999999999999822, 73.73191006444551476, 14.66109333815590254 ) ) ;
#12728=AXIS2_PLACEMENT_3D ( 'NONE', #47942, #42674, #37033 ) ;
#12729=VERTEX_POINT ( 'NONE', #33610 ) ;
#12732=FACE_OUTER_BOUND ( 'NONE', #74105, .T. ) ;
#12733=VERTEX_POINT ( 'NONE', #39640 ) ;
#12735=CARTESIAN_POINT ( 'NONE',  ( 11.99999999999999822, 77.19088730480532945, -6.903761155836932062 ) ) ;
#12736=CIRCLE ( 'NONE', #22364, 82.00000000000000000 ) ;
#12742=ORIENTED_EDGE ( 'NONE', *, *, #68374, .T. ) ;
#12743=ORIENTED_EDGE ( 'NONE', *, *, #4810, .T. ) ;
#12744=DIRECTION ( 'NONE',  ( 0.000000000000000000, 1.000000000000000000, 3.491481338843133355E-15 ) ) ;
#12746=CIRCLE ( 'NONE', #21120, 31.99999999999998934 ) ;
#12759=VERTEX_POINT ( 'NONE', #22340 ) ;
#12763=ORIENTED_EDGE ( 'NONE', *, *, #65170, .F. ) ;
#12772=EDGE_LOOP ( 'NONE', ( #17866, #28213, #15911, #40684 ) ) ;
#12789=ADVANCED_FACE ( 'NONE', ( #55810 ), #10313, .T. ) ;
#12798=DIRECTION ( 'NONE',  ( -1.000000000000000000, -0.000000000000000000, 0.000000000000000000 ) ) ;
#12804=AXIS2_PLACEMENT_3D ( 'NONE', #42432, #14210, #26232 ) ;
#12805=DIRECTION ( 'NONE',  ( 1.000000000000000000, -0.000000000000000000, -0.000000000000000000 ) ) ;
#12809=ADVANCED_FACE ( 'NONE', ( #74207 ), #22723, .T. ) ;
#12817=ADVANCED_FACE ( 'NONE', ( #57293 ), #28713, .T. ) ;
#12828=AXIS2_PLACEMENT_3D ( 'NONE', #67690, #62440, #3812 ) ;
#12829=ORIENTED_EDGE ( 'NONE', *, *, #53221, .F. ) ;
#12835=FACE_OUTER_BOUND ( 'NONE', #52882, .T. ) ;
#12849=DIRECTION ( 'NONE',  ( 0.000000000000000000, 0.07845909572783793529, 0.9969173337331285190 ) ) ;
#12853=CYLINDRICAL_SURFACE ( 'NONE', #46146, 31.99999999999998579 ) ;
#12863=CARTESIAN_POINT ( 'NONE',  ( 12.00000000000000000, -0.9646360437375368635, -23.52805723605589705 ) ) ;
#12870=EDGE_CURVE ( 'NONE', #366, #25593, #35102, .T. ) ;
#12872=CYLINDRICAL_SURFACE ( 'NONE', #69117, 31.99999999999998579 ) ;
#12873=DIRECTION ( 'NONE',  ( 0.000000000000000000, 0.000000000000000000, 1.000000000000000000 ) ) ;
#12874=EDGE_LOOP ( 'NONE', ( #40916, #8253, #12993, #17468 ) ) ;
#12876=ADVANCED_FACE ( 'NONE', ( #24558 ), #35466, .T. ) ;
#12877=DIRECTION ( 'NONE',  ( -0.000000000000000000, 0.1045284632676437703, -0.9945218953682742891 ) ) ;
#12878=EDGE_CURVE ( 'NONE', #71894, #58524, #23844, .T. ) ;
#12884=DIRECTION ( 'NONE',  ( -1.000000000000000000, -0.000000000000000000, -0.000000000000000000 ) ) ;
#12889=EDGE_CURVE ( 'NONE', #21827, #26934, #12892, .T. ) ;
#12892=LINE ( 'NONE', #40747, #56266 ) ;
#12897=AXIS2_PLACEMENT_3D ( 'NONE', #8471, #20492, #49049 ) ;
#12898=FILL_AREA_STYLE_COLOUR ( '', #14550 ) ;
#12899=CARTESIAN_POINT ( 'NONE',  ( 0.000000000000000000, 0.000000000000000000, 0.000000000000000000 ) ) ;
#12900=EDGE_CURVE ( 'NONE', #60196, #10397, #37047, .T. ) ;
#12903=FACE_OUTER_BOUND ( 'NONE', #64721, .T. ) ;
#12905=LINE ( 'NONE', #29086, #37705 ) ;
#12910=VERTEX_POINT ( 'NONE', #47130 ) ;
#12916=CYLINDRICAL_SURFACE ( 'NONE', #387, 31.99999999999998579 ) ;
#12921=ORIENTED_EDGE ( 'NONE', *, *, #38636, .F. ) ;
#12942=DIRECTION ( 'NONE',  ( -1.000000000000000000, -0.000000000000000000, 0.000000000000000000 ) ) ;
#12945=CARTESIAN_POINT ( 'NONE',  ( 11.99999999999999822, 8.966570791700714693, 81.50828551894230145 ) ) ;
#12957=ORIENTED_EDGE ( 'NONE', *, *, #40479, .T. ) ;
#12967=CARTESIAN_POINT ( 'NONE',  ( 0.000000000000000000, 0.000000000000000000, 0.000000000000000000 ) ) ;
#12968=DIRECTION ( 'NONE',  ( -1.000000000000000000, 0.000000000000000000, 0.000000000000000000 ) ) ;
#12984=EDGE_CURVE ( 'NONE', #24796, #54007, #560, .T. ) ;
#12993=ORIENTED_EDGE ( 'NONE', *, *, #9275, .T. ) ;
#12998=AXIS2_PLACEMENT_3D ( 'NONE', #3945, #62183, #50891 ) ;
#13001=EDGE_LOOP ( 'NONE', ( #22021, #60424, #18945, #26340 ) ) ;
#13012=VERTEX_POINT ( 'NONE', #48948 ) ;
#13038=CIRCLE ( 'NONE', #51472, 82.00000000000000000 ) ;
#13042=AXIS2_PLACEMENT_3D ( 'NONE', #69678, #58396, #929 ) ;
#13044=CARTESIAN_POINT ( 'NONE',  ( 11.99999999999999822, -3.894527615418461153, 81.90746397400387480 ) ) ;
#13047=DIRECTION ( 'NONE',  ( -1.000000000000000000, 0.000000000000000000, -0.000000000000000000 ) ) ;
#13056=CARTESIAN_POINT ( 'NONE',  ( 11.99999999999999822, 0.000000000000000000, 0.000000000000000000 ) ) ;
#13060=CARTESIAN_POINT ( 'NONE',  ( 0.000000000000000000, 73.44644590900061587, 24.73286445877730699 ) ) ;
#13077=EDGE_CURVE ( 'NONE', #25431, #25593, #71856, .T. ) ;
#13081=DIRECTION ( 'NONE',  ( 0.000000000000000000, -0.07845909572785224328, 0.9969173337331274087 ) ) ;
#13082=DIRECTION ( 'NONE',  ( -1.000000000000000000, 0.000000000000000000, 0.000000000000000000 ) ) ;
#13089=DIRECTION ( 'NONE',  ( -1.000000000000000000, 0.000000000000000000, -0.000000000000000000 ) ) ;
#13095=VECTOR ( 'NONE', #70813, 1000.000000000000114 ) ;
#13096=VECTOR ( 'NONE', #13905, 1000.000000000000000 ) ;
#13098=CARTESIAN_POINT ( 'NONE',  ( 11.99999999999999822, -73.95703589263990807, 23.16143007188399139 ) ) ;
#13101=AXIS2_PLACEMENT_3D ( 'NONE', #56299, #55549, #4065 ) ;
#13119=ORIENTED_EDGE ( 'NONE', *, *, #10059, .T. ) ;
#13124=ORIENTED_EDGE ( 'NONE', *, *, #44652, .F. ) ;
#13127=ORIENTED_EDGE ( 'NONE', *, *, #22226, .T. ) ;
#13128=ORIENTED_EDGE ( 'NONE', *, *, #68405, .F. ) ;
#13132=EDGE_CURVE ( 'NONE', #28736, #20120, #48231, .T. ) ;
#13136=LINE ( 'NONE', #43863, #66671 ) ;
#13137=VERTEX_POINT ( 'NONE', #20398 ) ;
#13138=VERTEX_POINT ( 'NONE', #66271 ) ;
#13147=DIRECTION ( 'NONE',  ( 0.000000000000000000, 0.5224985647159440250, 0.8526401643540951758 ) ) ;
#13155=DIRECTION ( 'NONE',  ( -1.000000000000000000, -0.000000000000000000, 0.000000000000000000 ) ) ;
#13172=LINE ( 'NONE', #42135, #282 ) ;
#13174=CIRCLE ( 'NONE', #35981, 77.49899999999999523 ) ;
#13178=EDGE_CURVE ( 'NONE', #32525, #37548, #56860, .T. ) ;
#13185=CIRCLE ( 'NONE', #32388, 82.00000000000000000 ) ;
#13192=CARTESIAN_POINT ( 'NONE',  ( 0.000000000000000000, -54.21277698773713638, 55.38113227695764351 ) ) ;
#13212=EDGE_CURVE ( 'NONE', #56853, #35138, #32241, .T. ) ;
#13214=CARTESIAN_POINT ( 'NONE',  ( 0.000000000000000000, 67.80270845531956070, -46.11716303203111522 ) ) ;
#13215=EDGE_CURVE ( 'NONE', #60769, #69147, #28267, .T. ) ;
#13216=ORIENTED_EDGE ( 'NONE', *, *, #6471, .T. ) ;
#13227=AXIS2_PLACEMENT_3D ( 'NONE', #41655, #13082, #12709 ) ;
#13232=CARTESIAN_POINT ( 'NONE',  ( 11.99999999999999822, -35.91791733033428358, -68.67312586195033930 ) ) ;
#13237=FACE_OUTER_BOUND ( 'NONE', #35134, .T. ) ;
#13238=DIRECTION ( 'NONE',  ( -1.000000000000000000, -0.000000000000000000, -0.000000000000000000 ) ) ;
#13242=ORIENTED_EDGE ( 'NONE', *, *, #39213, .T. ) ;
#13249=CARTESIAN_POINT ( 'NONE',  ( 11.99999999999999822, 44.88180994100466847, -63.18004540532978552 ) ) ;
#13252=CARTESIAN_POINT ( 'NONE',  ( 6.000000000000000000, 71.21200624218852226, -40.65526001592539984 ) ) ;
#13257=ORIENTED_EDGE ( 'NONE', *, *, #46851, .F. ) ;
#13258=LINE ( 'NONE', #24541, #67489 ) ;
#13263=CARTESIAN_POINT ( 'NONE',  ( 11.99999999999999822, -71.21200624218766961, -40.65526001592688488 ) ) ;
#13264=CYLINDRICAL_SURFACE ( 'NONE', #32581, 31.99999999999998579 ) ;
#13267=ORIENTED_EDGE ( 'NONE', *, *, #69323, .F. ) ;
#13281=VERTEX_POINT ( 'NONE', #46314 ) ;
#13285=AXIS2_PLACEMENT_3D ( 'NONE', #42195, #25994, #69998 ) ;
#13287=CIRCLE ( 'NONE', #12059, 82.00000000000000000 ) ;
#13294=ORIENTED_EDGE ( 'NONE', *, *, #32642, .T. ) ;
#13300=EDGE_CURVE ( 'NONE', #15455, #37544, #51944, .T. ) ;
#13303=ADVANCED_FACE ( 'NONE', ( #63623 ), #25961, .T. ) ;
#13304=ORIENTED_EDGE ( 'NONE', *, *, #29714, .F. ) ;
#13318=EDGE_LOOP ( 'NONE', ( #70335, #53626, #35354, #36132 ) ) ;
#13327=CARTESIAN_POINT ( 'NONE',  ( 6.000000000000000000, 39.47590169984846398, 71.87247863392427405 ) ) ;
#13333=DIRECTION ( 'NONE',  ( 0.000000000000000000, 0.5877852522924696954, -0.8090169943749498938 ) ) ;
#13337=PLANE ( 'NONE',  #41412 ) ;
#13341=CARTESIAN_POINT ( 'NONE',  ( 15.00000000000000000, 8.688484142254226938, 21.88630264137359305 ) ) ;
#13345=CIRCLE ( 'NONE', #66172, 31.99999999999998934 ) ;
#13348=DIRECTION ( 'NONE',  ( -1.000000000000000000, 0.000000000000000000, 0.000000000000000000 ) ) ;
#13353=ADVANCED_FACE ( 'NONE', ( #72736 ), #26885, .T. ) ;
#13356=CARTESIAN_POINT ( 'NONE',  ( 12.00000000000000000, -22.67460108101774452, 6.353146135318220367 ) ) ;
#13382=VECTOR ( 'NONE', #23072, 1000.000000000000000 ) ;
#13387=VECTOR ( 'NONE', #40853, 999.9999999999998863 ) ;
#13395=DIRECTION ( 'NONE',  ( -1.000000000000000000, 0.000000000000000000, -0.000000000000000000 ) ) ;
#13397=DIRECTION ( 'NONE',  ( 0.000000000000000000, 0.9723699203976773342, -0.2334453638559024213 ) ) ;
#13411=DIRECTION ( 'NONE',  ( 0.000000000000000000, 0.000000000000000000, 1.000000000000000000 ) ) ;
#13427=DIRECTION ( 'NONE',  ( -1.000000000000000000, 0.000000000000000000, -0.000000000000000000 ) ) ;
#13430=ORIENTED_EDGE ( 'NONE', *, *, #59532, .T. ) ;
#13438=VECTOR ( 'NONE', #72392, 1000.000000000000000 ) ;
#13447=DIRECTION ( 'NONE',  ( 1.000000000000000000, 0.000000000000000000, 0.000000000000000000 ) ) ;
#13450=CIRCLE ( 'NONE', #55471, 77.49900000000000944 ) ;
#13456=CARTESIAN_POINT ( 'NONE',  ( 11.99999999999999822, 34.44570377933598593, 69.42325613327452061 ) ) ;
#13458=CARTESIAN_POINT ( 'NONE',  ( 5.999999999999999112, -67.80270845531855173, -46.11716303203260736 ) ) ;
#13459=ORIENTED_EDGE ( 'NONE', *, *, #47109, .T. ) ;
#13461=DIRECTION ( 'NONE',  ( -1.000000000000000000, 0.000000000000000000, 0.000000000000000000 ) ) ;
#13465=DIRECTION ( 'NONE',  ( 0.000000000000000000, -0.1564344650402170744, -0.9876883405951399908 ) ) ;
#13476=ORIENTED_EDGE ( 'NONE', *, *, #47444, .T. ) ;
#13483=EDGE_CURVE ( 'NONE', #27765, #16367, #52712, .T. ) ;
#13488=ORIENTED_EDGE ( 'NONE', *, *, #5144, .T. ) ;
#13490=ORIENTED_EDGE ( 'NONE', *, *, #23709, .F. ) ;
#13491=AXIS2_PLACEMENT_3D ( 'NONE', #15325, #33742, #22468 ) ;
#13493=CYLINDRICAL_SURFACE ( 'NONE', #15348, 77.49899999999999523 ) ;
#13496=ORIENTED_EDGE ( 'NONE', *, *, #50920, .F. ) ;
#13503=ORIENTED_EDGE ( 'NONE', *, *, #52611, .F. ) ;
#13504=VERTEX_POINT ( 'NONE', #41509 ) ;
#13511=CARTESIAN_POINT ( 'NONE',  ( 11.99999999999999822, 0.000000000000000000, 0.000000000000000000 ) ) ;
#13515=ORIENTED_EDGE ( 'NONE', *, *, #11855, .T. ) ;
#13516=VERTEX_POINT ( 'NONE', #58809 ) ;
#13518=DIRECTION ( 'NONE',  ( -1.000000000000000000, -0.000000000000000000, 0.000000000000000000 ) ) ;
#13527=EDGE_LOOP ( 'NONE', ( #43473, #50398, #72933, #69546 ) ) ;
#13529=FACE_OUTER_BOUND ( 'NONE', #59311, .T. ) ;
#13534=FACE_OUTER_BOUND ( 'NONE', #15831, .T. ) ;
#13542=VECTOR ( 'NONE', #51030, 1000.000000000000000 ) ;
#13545=DIRECTION ( 'NONE',  ( 0.000000000000000000, 0.4067366430757989870, 0.9135454576426015327 ) ) ;
#13548=CARTESIAN_POINT ( 'NONE',  ( 11.99999999999999822, -81.96053171279903893, 2.543863470248101333 ) ) ;
#13549=LINE ( 'NONE', #54521, #35220 ) ;
#13552=ORIENTED_EDGE ( 'NONE', *, *, #9921, .T. ) ;
#13555=PLANE ( 'NONE',  #14202 ) ;
#13573=VECTOR ( 'NONE', #60475, 1000.000000000000000 ) ;
#13574=VERTEX_POINT ( 'NONE', #48988 ) ;
#13575=ORIENTED_EDGE ( 'NONE', *, *, #56899, .T. ) ;
#13579=LINE ( 'NONE', #20335, #53623 ) ;
#13581=EDGE_CURVE ( 'NONE', #38472, #7584, #49363, .T. ) ;
#13585=ORIENTED_EDGE ( 'NONE', *, *, #65187, .F. ) ;
#13591=AXIS2_PLACEMENT_3D ( 'NONE', #30361, #12702, #53307 ) ;
#13604=LINE ( 'NONE', #48193, #51724 ) ;
#13611=DIRECTION ( 'NONE',  ( 0.000000000000000000, -0.9781476007338070211, -0.2079116908177532363 ) ) ;
#13614=CARTESIAN_POINT ( 'NONE',  ( 15.00000000000000000, 9.615535125379096826, 24.73947219025905042 ) ) ;
#13622=DIRECTION ( 'NONE',  ( 0.000000000000000000, 0.000000000000000000, -1.000000000000000000 ) ) ;
#13623=DIRECTION ( 'NONE',  ( -1.000000000000000000, 0.000000000000000000, 0.000000000000000000 ) ) ;
#13631=ORIENTED_EDGE ( 'NONE', *, *, #6248, .T. ) ;
#13633=CARTESIAN_POINT ( 'NONE',  ( 15.00000000000000000, 14.60985201121729737, 18.46759930825687235 ) ) ;
#13641=CIRCLE ( 'NONE', #55668, 82.00000000000000000 ) ;
#13642=DIRECTION ( 'NONE',  ( -0.000000000000000000, 0.1045284632676437703, -0.9945218953682742891 ) ) ;
#13655=ADVANCED_FACE ( 'NONE', ( #25336 ), #59930, .T. ) ;
#13657=CARTESIAN_POINT ( 'NONE',  ( 0.000000000000000000, 34.94270380257741238, -74.18225833017852722 ) ) ;
#13664=CARTESIAN_POINT ( 'NONE',  ( 11.99999999999999822, 14.67089635893713684, 73.72996012237443608 ) ) ;
#13673=ORIENTED_EDGE ( 'NONE', *, *, #20403, .F. ) ;
#13681=VERTEX_POINT ( 'NONE', #64825 ) ;
#13683=DIRECTION ( 'NONE',  ( 0.000000000000000000, 0.000000000000000000, 1.000000000000000000 ) ) ;
#13686=CARTESIAN_POINT ( 'NONE',  ( 11.99999999999999822, 30.41916302227114599, 71.27951684758035356 ) ) ;
#13697=CARTESIAN_POINT ( 'NONE',  ( -10.00000000000000000, 0.000000000000000000, 0.000000000000000000 ) ) ;
#13709=DIRECTION ( 'NONE',  ( -1.000000000000000000, -0.000000000000000000, 0.000000000000000000 ) ) ;
#13715=CARTESIAN_POINT ( 'NONE',  ( 12.00000000000000000, 14.60985201121703980, -18.46759930825707841 ) ) ;
#13716=ORIENTED_EDGE ( 'NONE', *, *, #24856, .F. ) ;
#13719=CYLINDRICAL_SURFACE ( 'NONE', #22357, 82.00000000000000000 ) ;
#13722=DIRECTION ( 'NONE',  ( 0.000000000000000000, 0.000000000000000000, 1.000000000000000000 ) ) ;
#13725=EDGE_CURVE ( 'NONE', #69920, #63641, #22730, .T. ) ;
#13732=ADVANCED_FACE ( 'NONE', ( #11002 ), #5011, .T. ) ;
#13735=ORIENTED_EDGE ( 'NONE', *, *, #30918, .T. ) ;
#13749=DIRECTION ( 'NONE',  ( -1.000000000000000000, -0.000000000000000000, 0.000000000000000000 ) ) ;
#13756=EDGE_CURVE ( 'NONE', #70963, #23395, #65991, .T. ) ;
#13757=CIRCLE ( 'NONE', #55801, 21.00000000000000000 ) ;
#13760=LINE ( 'NONE', #54732, #50688 ) ;
#13766=ORIENTED_EDGE ( 'NONE', *, *, #8450, .T. ) ;
#13786=DIRECTION ( 'NONE',  ( -1.000000000000000000, 0.000000000000000000, 0.000000000000000000 ) ) ;
#13789=ORIENTED_EDGE ( 'NONE', *, *, #32218, .F. ) ;
#13797=DIRECTION ( 'NONE',  ( -1.000000000000000000, -0.000000000000000000, -0.000000000000000000 ) ) ;
#13807=ADVANCED_FACE ( 'NONE', ( #39579 ), #50844, .T. ) ;
#13810=CARTESIAN_POINT ( 'NONE',  ( 11.99999999999999822, 41.19522573413733113, 65.64334221924924861 ) ) ;
#13814=VECTOR ( 'NONE', #10005, 1000.000000000000000 ) ;
#13817=VERTEX_POINT ( 'NONE', #38463 ) ;
#13820=AXIS2_PLACEMENT_3D ( 'NONE', #57292, #17794, #29076 ) ;
#13836=CYLINDRICAL_SURFACE ( 'NONE', #31743, 31.99999999999998579 ) ;
#13837=DIRECTION ( 'NONE',  ( 0.000000000000000000, -0.3090169943749548342, 0.9510565162951510887 ) ) ;
#13839=ORIENTED_EDGE ( 'NONE', *, *, #24140, .T. ) ;
#13849=CYLINDRICAL_SURFACE ( 'NONE', #46076, 82.00000000000000000 ) ;
#13883=VERTEX_POINT ( 'NONE', #21525 ) ;
#13885=CARTESIAN_POINT ( 'NONE',  ( 11.99999999999999822, -67.80270845531855173, -46.11716303203260736 ) ) ;
#13887=LINE ( 'NONE', #65781, #26627 ) ;
#13899=FACE_OUTER_BOUND ( 'NONE', #59553, .T. ) ;
#13905=DIRECTION ( 'NONE',  ( -1.000000000000000000, 0.000000000000000000, 0.000000000000000000 ) ) ;
#13907=CARTESIAN_POINT ( 'NONE',  ( 11.99999999999999822, 31.46837873494978055, 68.27212725128286763 ) ) ;
#13910=DIRECTION ( 'NONE',  ( 1.000000000000000000, 0.000000000000000000, 0.000000000000000000 ) ) ;
#13912=AXIS2_PLACEMENT_3D ( 'NONE', #11408, #74195, #62182 ) ;
#13913=EDGE_CURVE ( 'NONE', #15161, #10181, #32038, .T. ) ;
#13914=CIRCLE ( 'NONE', #2006, 82.00000000000000000 ) ;
#13917=EDGE_CURVE ( 'NONE', #66576, #71829, #7215, .T. ) ;
#13918=CYLINDRICAL_SURFACE ( 'NONE', #58195, 31.99999999999998579 ) ;
#13921=AXIS2_PLACEMENT_3D ( 'NONE', #66563, #55274, #38358 ) ;
#13922=VERTEX_POINT ( 'NONE', #23036 ) ;
#13923=CARTESIAN_POINT ( 'NONE',  ( 0.000000000000000000, -76.41127070299262414, -12.93880638057396304 ) ) ;
#13933=EDGE_LOOP ( 'NONE', ( #72142, #68001, #54103, #10058 ) ) ;
#13940=ORIENTED_EDGE ( 'NONE', *, *, #24352, .T. ) ;
#13946=CARTESIAN_POINT ( 'NONE',  ( 15.00000000000000000, 18.84667830672579569, -18.68964196561269375 ) ) ;
#13947=CIRCLE ( 'NONE', #19962, 31.99999999999998579 ) ;
#13954=CARTESIAN_POINT ( 'NONE',  ( 11.99999999999999822, -51.02545421589285723, -55.20638768913812555 ) ) ;
#13955=ORIENTED_EDGE ( 'NONE', *, *, #2828, .T. ) ;
#13956=CARTESIAN_POINT ( 'NONE',  ( 15.00000000000000000, 6.762365576493647445, 25.66652317338391498 ) ) ;
#13959=DIRECTION ( 'NONE',  ( -1.000000000000000000, 0.000000000000000000, 0.000000000000000000 ) ) ;
#13961=CIRCLE ( 'NONE', #43986, 31.99999999999998579 ) ;
#13963=LINE ( 'NONE', #65864, #51523 ) ;
#13974=CARTESIAN_POINT ( 'NONE',  ( 5.999999999999999112, 44.99326035066149387, -68.55367621811095091 ) ) ;
#13975=DIRECTION ( 'NONE',  ( 1.000000000000000000, 0.000000000000000000, -0.000000000000000000 ) ) ;
#13981=VERTEX_POINT ( 'NONE', #39952 ) ;
#13986=EDGE_CURVE ( 'NONE', #28379, #42337, #46327, .T. ) ;
#13996=CARTESIAN_POINT ( 'NONE',  ( 11.99999999999999822, 0.000000000000000000, 0.000000000000000000 ) ) ;
#13998=CARTESIAN_POINT ( 'NONE',  ( 0.000000000000000000, 0.000000000000000000, 0.000000000000000000 ) ) ;
#14005=DIRECTION ( 'NONE',  ( -1.000000000000000000, -0.000000000000000000, -0.000000000000000000 ) ) ;
#14006=CIRCLE ( 'NONE', #47668, 77.49900000000000944 ) ;
#14013=CYLINDRICAL_SURFACE ( 'NONE', #43148, 31.99999999999998579 ) ;
#14015=EDGE_CURVE ( 'NONE', #232, #61944, #41657, .T. ) ;
#14017=AXIS2_PLACEMENT_3D ( 'NONE', #2013, #47828, #65508 ) ;
#14019=CARTESIAN_POINT ( 'NONE',  ( 11.99999999999999822, -58.39081064771786345, 50.95692526931308919 ) ) ;
#14026=DIRECTION ( 'NONE',  ( -1.000000000000000000, 0.000000000000000000, 0.000000000000000000 ) ) ;
#14028=ORIENTED_EDGE ( 'NONE', *, *, #10898, .F. ) ;
#14032=ORIENTED_EDGE ( 'NONE', *, *, #49389, .F. ) ;
#14043=ORIENTED_EDGE ( 'NONE', *, *, #24020, .F. ) ;
#14044=DIRECTION ( 'NONE',  ( -1.000000000000000000, -0.000000000000000000, 0.000000000000000000 ) ) ;
#14052=CARTESIAN_POINT ( 'NONE',  ( 0.000000000000000000, 14.66109333815460225, 73.73191006444577056 ) ) ;
#14063=EDGE_CURVE ( 'NONE', #5078, #61762, #18836, .T. ) ;
#14064=DIRECTION ( 'NONE',  ( -1.000000000000000000, -0.000000000000000000, 0.000000000000000000 ) ) ;
#14068=DIRECTION ( 'NONE',  ( 1.000000000000000000, 0.000000000000000000, -0.000000000000000000 ) ) ;
#14071=CIRCLE ( 'NONE', #50070, 31.99999999999997868 ) ;
#14075=EDGE_CURVE ( 'NONE', #31904, #52407, #13579, .T. ) ;
#14081=CARTESIAN_POINT ( 'NONE',  ( 11.99999999999999822, 20.41045688087824317, 72.35160999960824313 ) ) ;
#14085=VERTEX_POINT ( 'NONE', #37276 ) ;
#14095=AXIS2_PLACEMENT_3D ( 'NONE', #67028, #16271, #55759 ) ;
#14110=ORIENTED_EDGE ( 'NONE', *, *, #71380, .F. ) ;
#14120=CARTESIAN_POINT ( 'NONE',  ( 0.000000000000000000, 64.81221759200342092, 50.23322058963371006 ) ) ;
#14127=ORIENTED_EDGE ( 'NONE', *, *, #5009, .F. ) ;
#14128=ORIENTED_EDGE ( 'NONE', *, *, #49895, .F. ) ;
#14137=CARTESIAN_POINT ( 'NONE',  ( 11.99999999999999822, 77.19088730480532945, -6.903761155836932062 ) ) ;
#14139=CIRCLE ( 'NONE', #53938, 31.99999999999998579 ) ;
#14145=ORIENTED_EDGE ( 'NONE', *, *, #48147, .T. ) ;
#14160=FACE_OUTER_BOUND ( 'NONE', #62375, .T. ) ;
#14165=CARTESIAN_POINT ( 'NONE',  ( 0.000000000000000000, 77.49459641780886443, -0.8261519478433960728 ) ) ;
#14167=CARTESIAN_POINT ( 'NONE',  ( 15.00000000000000000, -19.89357724624986545, 12.59942793731086219 ) ) ;
#14171=VECTOR ( 'NONE', #43571, 1000.000000000000000 ) ;
#14174=AXIS2_PLACEMENT_3D ( 'NONE', #44540, #62965, #5806 ) ;
#14177=CARTESIAN_POINT ( 'NONE',  ( 5.999999999999999112, -55.16347631943085617, 60.67117009219117563 ) ) ;
#14185=DIRECTION ( 'NONE',  ( -1.000000000000000000, 0.000000000000000000, 0.000000000000000000 ) ) ;
#14190=EDGE_CURVE ( 'NONE', #64128, #20120, #71643, .T. ) ;
#14200=DIRECTION ( 'NONE',  ( -1.000000000000000000, 0.000000000000000000, -0.000000000000000000 ) ) ;
#14201=ORIENTED_EDGE ( 'NONE', *, *, #20686, .F. ) ;
#14202=AXIS2_PLACEMENT_3D ( 'NONE', #23378, #64340, #40664 ) ;
#14204=DIRECTION ( 'NONE',  ( 0.000000000000000000, -0.1564344650402170744, -0.9876883405951398798 ) ) ;
#14207=VERTEX_POINT ( 'NONE', #15061 ) ;
#14208=ORIENTED_EDGE ( 'NONE', *, *, #1495, .F. ) ;
#14210=DIRECTION ( 'NONE',  ( -1.000000000000000000, -0.000000000000000000, -0.000000000000000000 ) ) ;
#14224=CARTESIAN_POINT ( 'NONE',  ( 0.000000000000000000, 14.67089635893819377, -73.72996012237423713 ) ) ;
#14225=AXIS2_PLACEMENT_3D ( 'NONE', #12444, #41759, #52673 ) ;
#14226=ADVANCED_FACE ( 'NONE', ( #9423 ), #60933, .T. ) ;
#14231=EDGE_CURVE ( 'NONE', #3457, #11454, #45281, .T. ) ;
#14243=EDGE_CURVE ( 'NONE', #24697, #13883, #6890, .T. ) ;
#14249=ORIENTED_EDGE ( 'NONE', *, *, #12323, .T. ) ;
#14265=ADVANCED_FACE ( 'NONE', ( #49276 ), #32348, .T. ) ;
#14267=CYLINDRICAL_SURFACE ( 'NONE', #30857, 31.99999999999998579 ) ;
#14268=FACE_OUTER_BOUND ( 'NONE', #53732, .T. ) ;
#14271=CARTESIAN_POINT ( 'NONE',  ( 11.99999999999999822, 71.91182617369230456, -28.89263327155667938 ) ) ;
#14273=DIRECTION ( 'NONE',  ( 0.000000000000000000, 0.000000000000000000, 1.000000000000000000 ) ) ;
#14282=AXIS2_PLACEMENT_3D ( 'NONE', #63728, #35510, #18218 ) ;
#14284=LINE ( 'NONE', #8655, #73647 ) ;
#14288=CARTESIAN_POINT ( 'NONE',  ( 11.99999999999999822, 51.02545421589324803, 55.20638768913779870 ) ) ;
#14294=LINE ( 'NONE', #3411, #64992 ) ;
#14295=ORIENTED_EDGE ( 'NONE', *, *, #13077, .T. ) ;
#14300=DIRECTION ( 'NONE',  ( 1.000000000000000000, -0.000000000000000000, -0.000000000000000000 ) ) ;
#14302=VECTOR ( 'NONE', #2337, 1000.000000000000000 ) ;
#14313=VERTEX_POINT ( 'NONE', #61326 ) ;
#14322=DIRECTION ( 'NONE',  ( 1.000000000000000000, 0.000000000000000000, 0.000000000000000000 ) ) ;
#14323=EDGE_CURVE ( 'NONE', #1097, #72747, #23681, .T. ) ;
#14324=ORIENTED_EDGE ( 'NONE', *, *, #73736, .F. ) ;
#14327=ORIENTED_EDGE ( 'NONE', *, *, #44243, .T. ) ;
#14352=ADVANCED_FACE ( 'NONE', ( #57539 ), #11649, .F. ) ;
#14354=ORIENTED_EDGE ( 'NONE', *, *, #39567, .F. ) ;
#14356=LINE ( 'NONE', #14720, #52779 ) ;
#14360=DIRECTION ( 'NONE',  ( -1.000000000000000000, -0.000000000000000000, -0.000000000000000000 ) ) ;
#14367=CIRCLE ( 'NONE', #39594, 31.99999999999999289 ) ;
#14378=ORIENTED_EDGE ( 'NONE', *, *, #24875, .T. ) ;
#14386=FACE_OUTER_BOUND ( 'NONE', #57156, .T. ) ;
#14398=LINE ( 'NONE', #14019, #3708 ) ;
#14400=ORIENTED_EDGE ( 'NONE', *, *, #52524, .F. ) ;
#14401=DIRECTION ( 'NONE',  ( 0.000000000000000000, 0.3090169943749461745, -0.9510565162951539753 ) ) ;
#14418=ORIENTED_EDGE ( 'NONE', *, *, #30918, .F. ) ;
#14420=ADVANCED_FACE ( 'NONE', ( #63925 ), #18049, .T. ) ;
#14426=VERTEX_POINT ( 'NONE', #7140 ) ;
#14427=DIRECTION ( 'NONE',  ( 0.000000000000000000, 0.9781476007338065770, 0.2079116908177544853 ) ) ;
#14435=DIRECTION ( 'NONE',  ( -0.000000000000000000, 0.5877852522924796874, 0.8090169943749426773 ) ) ;
#14437=DIRECTION ( 'NONE',  ( -1.000000000000000000, -0.000000000000000000, -0.000000000000000000 ) ) ;
#14438=ORIENTED_EDGE ( 'NONE', *, *, #38173, .T. ) ;
#14443=DIRECTION ( 'NONE',  ( 0.000000000000000000, 0.000000000000000000, 1.000000000000000000 ) ) ;
#14446=DIRECTION ( 'NONE',  ( -1.000000000000000000, 0.000000000000000000, 0.000000000000000000 ) ) ;
#14448=AXIS2_PLACEMENT_3D ( 'NONE', #20581, #60442, #32950 ) ;
#14450=DIRECTION ( 'NONE',  ( 0.000000000000000000, 0.000000000000000000, 1.000000000000000000 ) ) ;
#14464=EDGE_LOOP ( 'NONE', ( #51956, #8044, #6990, #43743 ) ) ;
#14466=DIRECTION ( 'NONE',  ( 0.000000000000000000, 0.000000000000000000, 1.000000000000000000 ) ) ;
#14468=AXIS2_PLACEMENT_3D ( 'NONE', #25175, #30426, #71019 ) ;
#14469=CARTESIAN_POINT ( 'NONE',  ( 11.99999999999999822, 0.000000000000000000, 0.000000000000000000 ) ) ;
#14470=CARTESIAN_POINT ( 'NONE',  ( 0.000000000000000000, -2.956366410621191765, 75.11725578898467859 ) ) ;
#14471=DIRECTION ( 'NONE',  ( -1.000000000000000000, 0.000000000000000000, 0.000000000000000000 ) ) ;
#14476=CIRCLE ( 'NONE', #34870, 77.49899999999999523 ) ;
#14481=ORIENTED_EDGE ( 'NONE', *, *, #63107, .F. ) ;
#14486=EDGE_LOOP ( 'NONE', ( #46630, #51730, #45149, #3351 ) ) ;
#14490=CIRCLE ( 'NONE', #68563, 77.49899999999999523 ) ;
#14491=DIRECTION ( 'NONE',  ( 1.000000000000000000, -0.000000000000000000, -0.000000000000000000 ) ) ;
#14493=EDGE_CURVE ( 'NONE', #48711, #41355, #17674, .T. ) ;
#14494=ORIENTED_EDGE ( 'NONE', *, *, #55798, .T. ) ;
#14495=EDGE_CURVE ( 'NONE', #21534, #53485, #60920, .T. ) ;
#14506=ORIENTED_EDGE ( 'NONE', *, *, #24464, .F. ) ;
#14510=AXIS2_PLACEMENT_3D ( 'NONE', #27288, #33683, #17140 ) ;
#14517=CARTESIAN_POINT ( 'NONE',  ( 15.00000000000000000, 16.83928648764945635, 16.46020748918027010 ) ) ;
#14522=ORIENTED_EDGE ( 'NONE', *, *, #51676, .T. ) ;
#14538=ADVANCED_FACE ( 'NONE', ( #3008 ), #53366, .T. ) ;
#14539=CARTESIAN_POINT ( 'NONE',  ( 0.000000000000000000, 65.58780272294076497, 36.73666225445916211 ) ) ;
#14542=DIRECTION ( 'NONE',  ( 0.000000000000000000, -0.9876883405951359940, -0.1564344650402420822 ) ) ;
#14548=LINE ( 'NONE', #15288, #65711 ) ;
#14550=COLOUR_RGB ( '', 0.40784314, 0.44705882, 0.49803922) ;
#14553=DIRECTION ( 'NONE',  ( -1.000000000000000000, -0.000000000000000000, -0.000000000000000000 ) ) ;
#14554=VECTOR ( 'NONE', #60975, 1000.000000000000000 ) ;
#14558=FACE_OUTER_BOUND ( 'NONE', #43845, .T. ) ;
#14560=FACE_OUTER_BOUND ( 'NONE', #14897, .T. ) ;
#14564=PRODUCT_DEFINITION_CONTEXT ( 'detailed design', #63796, 'design' ) ;
#14565=CARTESIAN_POINT ( 'NONE',  ( 11.99999999999999822, 0.000000000000000000, 0.000000000000000000 ) ) ;
#14573=DIRECTION ( 'NONE',  ( 0.000000000000000000, -0.9945218953682742891, -0.1045284632676449360 ) ) ;
#14574=EDGE_CURVE ( 'NONE', #13012, #49856, #42097, .T. ) ;
#14585=ADVANCED_FACE ( 'NONE', ( #37932 ), #66866, .T. ) ;
#14588=DIRECTION ( 'NONE',  ( 0.000000000000000000, 0.000000000000000000, -1.000000000000000000 ) ) ;
#14589=EDGE_CURVE ( 'NONE', #13574, #23135, #35686, .T. ) ;
#14593=VECTOR ( 'NONE', #60605, 1000.000000000000000 ) ;
#14596=DIRECTION ( 'NONE',  ( -1.000000000000000000, 0.000000000000000000, 0.000000000000000000 ) ) ;
#14599=FACE_OUTER_BOUND ( 'NONE', #10074, .T. ) ;
#14608=CARTESIAN_POINT ( 'NONE',  ( 11.99999999999999822, 0.000000000000000000, 0.000000000000000000 ) ) ;
#14609=VECTOR ( 'NONE', #10004, 1000.000000000000227 ) ;
#14640=LINE ( 'NONE', #32663, #1508 ) ;
#14649=CARTESIAN_POINT ( 'NONE',  ( 11.99999999999999822, 0.000000000000000000, 0.000000000000000000 ) ) ;
#14651=EDGE_CURVE ( 'NONE', #9220, #33472, #16109, .T. ) ;
#14660=EDGE_CURVE ( 'NONE', #63551, #55642, #70505, .T. ) ;
#14667=CARTESIAN_POINT ( 'NONE',  ( 0.000000000000000000, 0.000000000000000000, 0.000000000000000000 ) ) ;
#14669=ADVANCED_FACE ( 'NONE', ( #44700 ), #39049, .T. ) ;
#14671=VECTOR ( 'NONE', #36324, 1000.000000000000000 ) ;
#14680=EDGE_CURVE ( 'NONE', #56976, #71434, #24855, .T. ) ;
#14683=ORIENTED_EDGE ( 'NONE', *, *, #32683, .F. ) ;
#14687=ORIENTED_EDGE ( 'NONE', *, *, #73907, .F. ) ;
#14689=FACE_OUTER_BOUND ( 'NONE', #13318, .T. ) ;
#14693=EDGE_CURVE ( 'NONE', #16267, #11059, #61608, .T. ) ;
#14698=DIRECTION ( 'NONE',  ( -1.000000000000000000, 0.000000000000000000, 0.000000000000000000 ) ) ;
#14708=VERTEX_POINT ( 'NONE', #14989 ) ;
#14714=AXIS2_PLACEMENT_3D ( 'NONE', #9563, #71215, #49035 ) ;
#14720=CARTESIAN_POINT ( 'NONE',  ( 12.00000000000000000, -0.9646360437372099028, 23.52805723605590771 ) ) ;
#14725=LINE ( 'NONE', #59871, #34972 ) ;
#14728=CARTESIAN_POINT ( 'NONE',  ( 11.99999999999999822, -14.67089635893764665, 73.72996012237435082 ) ) ;
#14733=LINE ( 'NONE', #66618, #60371 ) ;
#14734=CARTESIAN_POINT ( 'NONE',  ( 11.99999999999999822, 77.32052557432849937, -5.256550761632002633 ) ) ;
#14739=DIRECTION ( 'NONE',  ( 0.000000000000000000, 0.000000000000000000, -1.000000000000000000 ) ) ;
#14740=EDGE_CURVE ( 'NONE', #19443, #34985, #66309, .T. ) ;
#14750=EDGE_CURVE ( 'NONE', #52748, #47732, #23982, .T. ) ;
#14753=FACE_OUTER_BOUND ( 'NONE', #62720, .T. ) ;
#14754=DIRECTION ( 'NONE',  ( 0.000000000000000000, 0.000000000000000000, 1.000000000000000000 ) ) ;
#14756=ORIENTED_EDGE ( 'NONE', *, *, #35303, .F. ) ;
#14763=CARTESIAN_POINT ( 'NONE',  ( 0.000000000000000000, 0.000000000000000000, 0.000000000000000000 ) ) ;
#14773=ORIENTED_EDGE ( 'NONE', *, *, #64593, .F. ) ;
#14776=CARTESIAN_POINT ( 'NONE',  ( 11.99999999999999822, -71.91182617369207719, 28.89263327155721228 ) ) ;
#14778=ORIENTED_EDGE ( 'NONE', *, *, #45680, .F. ) ;
#14783=EDGE_CURVE ( 'NONE', #51571, #42708, #17226, .T. ) ;
#14788=CARTESIAN_POINT ( 'NONE',  ( 11.99999999999999822, 0.000000000000000000, 0.000000000000000000 ) ) ;
#14803=DIRECTION ( 'NONE',  ( 0.000000000000000000, -0.8090169943749426773, 0.5877852522924796874 ) ) ;
#14811=ORIENTED_EDGE ( 'NONE', *, *, #10296, .T. ) ;
#14819=LINE ( 'NONE', #42662, #196 ) ;
#14829=DIRECTION ( 'NONE',  ( 1.000000000000000000, 0.000000000000000000, 0.000000000000000000 ) ) ;
#14830=AXIS2_PLACEMENT_3D ( 'NONE', #51374, #60542, #17173 ) ;
#14836=CIRCLE ( 'NONE', #19601, 31.99999999999998579 ) ;
#14839=EDGE_CURVE ( 'NONE', #46085, #15234, #63958, .T. ) ;
#14842=EDGE_CURVE ( 'NONE', #63432, #52407, #69108, .T. ) ;
#14854=ADVANCED_FACE ( 'NONE', ( #5595 ), #62747, .F. ) ;
#14857=CARTESIAN_POINT ( 'NONE',  ( 0.000000000000000000, -41.76937507738831812, 62.50329211542423025 ) ) ;
#14863=ORIENTED_EDGE ( 'NONE', *, *, #56899, .F. ) ;
#14868=EDGE_CURVE ( 'NONE', #16620, #68748, #57452, .T. ) ;
#14874=ADVANCED_FACE ( 'NONE', ( #14160 ), #20169, .T. ) ;
#14879=CIRCLE ( 'NONE', #22079, 31.99999999999998934 ) ;
#14884=ORIENTED_EDGE ( 'NONE', *, *, #42050, .T. ) ;
#14897=EDGE_LOOP ( 'NONE', ( #31899, #46392, #30500, #48536 ) ) ;
#14898=DIRECTION ( 'NONE',  ( -1.000000000000000000, -0.000000000000000000, -0.000000000000000000 ) ) ;
#14899=ORIENTED_EDGE ( 'NONE', *, *, #3344, .T. ) ;
#14901=ORIENTED_EDGE ( 'NONE', *, *, #10877, .T. ) ;
#14905=AXIS2_PLACEMENT_3D ( 'NONE', #45626, #68548, #17033 ) ;
#14913=ORIENTED_EDGE ( 'NONE', *, *, #57134, .T. ) ;
#14917=CYLINDRICAL_SURFACE ( 'NONE', #2932, 77.49899999999999523 ) ;
#14922=EDGE_CURVE ( 'NONE', #10184, #14708, #69940, .T. ) ;
#14923=CARTESIAN_POINT ( 'NONE',  ( 11.99999999999999822, -75.16055320797043748, 18.89407956138231270 ) ) ;
#14924=AXIS2_PLACEMENT_3D ( 'NONE', #34122, #57069, #50292 ) ;
#14932=DIRECTION ( 'NONE',  ( 0.000000000000000000, 0.000000000000000000, 1.000000000000000000 ) ) ;
#14938=VECTOR ( 'NONE', #14300, 1000.000000000000000 ) ;
#14939=CARTESIAN_POINT ( 'NONE',  ( 0.000000000000000000, -80.28980883073747066, -16.65972982745017461 ) ) ;
#14941=ORIENTED_EDGE ( 'NONE', *, *, #389, .T. ) ;
#14942=CIRCLE ( 'NONE', #28145, 82.00000000000000000 ) ;
#14945=DIRECTION ( 'NONE',  ( 0.000000000000000000, 0.000000000000000000, 1.000000000000000000 ) ) ;
#14947=AXIS2_PLACEMENT_3D ( 'NONE', #62100, #57202, #29347 ) ;
#14948=ADVANCED_FACE ( 'NONE', ( #31454 ), #47283, .F. ) ;
#14949=CARTESIAN_POINT ( 'NONE',  ( 11.99999999999999822, 30.41916302227216562, -71.27951684757994144 ) ) ;
#14951=VERTEX_POINT ( 'NONE', #37110 ) ;
#14952=FACE_OUTER_BOUND ( 'NONE', #12874, .T. ) ;
#14955=AXIS2_PLACEMENT_3D ( 'NONE', #16106, #53459, #42192 ) ;
#14958=EDGE_CURVE ( 'NONE', #58250, #73508, #25818, .T. ) ;
#14963=CARTESIAN_POINT ( 'NONE',  ( 0.000000000000000000, 0.000000000000000000, 0.000000000000000000 ) ) ;
#14987=CYLINDRICAL_SURFACE ( 'NONE', #25246, 82.00000000000000000 ) ;
#14988=ORIENTED_EDGE ( 'NONE', *, *, #66407, .F. ) ;
#14989=CARTESIAN_POINT ( 'NONE',  ( 11.99999999999999822, -80.28980883073745645, -16.65972982745018172 ) ) ;
#14993=CARTESIAN_POINT ( 'NONE',  ( 6.000000000000000000, -21.60688246758530795, -79.10210256391388839 ) ) ;
#14997=ORIENTED_EDGE ( 'NONE', *, *, #21278, .T. ) ;
#15002=DIRECTION ( 'NONE',  ( -1.000000000000000000, 0.000000000000000000, 0.000000000000000000 ) ) ;
#15003=DIRECTION ( 'NONE',  ( -1.000000000000000000, 0.000000000000000000, 0.000000000000000000 ) ) ;
#15005=CIRCLE ( 'NONE', #29478, 77.49900000000000944 ) ;
#15018=CYLINDRICAL_SURFACE ( 'NONE', #21856, 31.99999999999998579 ) ;
#15022=FACE_OUTER_BOUND ( 'NONE', #66511, .T. ) ;
#15023=AXIS2_PLACEMENT_3D ( 'NONE', #59281, #59653, #8136 ) ;
#15025=DIRECTION ( 'NONE',  ( -1.000000000000000000, -0.000000000000000000, -0.000000000000000000 ) ) ;
#15032=PLANE ( 'NONE',  #63545 ) ;
#15033=CIRCLE ( 'NONE', #10212, 82.00000000000000000 ) ;
#15037=AXIS2_PLACEMENT_3D ( 'NONE', #39752, #11527, #23197 ) ;
#15038=EDGE_CURVE ( 'NONE', #40774, #4927, #42325, .T. ) ;
#15040=ORIENTED_EDGE ( 'NONE', *, *, #55273, .F. ) ;
#15042=ORIENTED_EDGE ( 'NONE', *, *, #45187, .T. ) ;
#15052=DIRECTION ( 'NONE',  ( 0.000000000000000000, 0.000000000000000000, 1.000000000000000000 ) ) ;
#15055=ORIENTED_EDGE ( 'NONE', *, *, #63915, .F. ) ;
#15061=CARTESIAN_POINT ( 'NONE',  ( 11.99999999999999822, 58.39081064771822582, -50.95692526931267707 ) ) ;
#15069=ORIENTED_EDGE ( 'NONE', *, *, #50238, .F. ) ;
#15072=DIRECTION ( 'NONE',  ( -1.000000000000000000, 0.000000000000000000, 0.000000000000000000 ) ) ;
#15073=VERTEX_POINT ( 'NONE', #44232 ) ;
#15092=CARTESIAN_POINT ( 'NONE',  ( 11.99999999999999822, 5.256550761633951296, -77.32052557432835727 ) ) ;
#15095=FACE_OUTER_BOUND ( 'NONE', #38859, .T. ) ;
#15097=CIRCLE ( 'NONE', #58355, 31.99999999999998579 ) ;
#15102=LINE ( 'NONE', #26015, #60792 ) ;
#15109=ORIENTED_EDGE ( 'NONE', *, *, #46280, .F. ) ;
#15110=DIRECTION ( 'NONE',  ( -1.000000000000000000, 0.000000000000000000, 0.000000000000000000 ) ) ;
#15111=CARTESIAN_POINT ( 'NONE',  ( 11.99999999999999822, 0.000000000000000000, 0.000000000000000000 ) ) ;
#15118=EDGE_CURVE ( 'NONE', #56648, #21247, #67158, .T. ) ;
#15123=LINE ( 'NONE', #15497, #40599 ) ;
#15133=ORIENTED_EDGE ( 'NONE', *, *, #64593, .T. ) ;
#15134=LINE ( 'NONE', #73008, #29186 ) ;
#15140=DIRECTION ( 'NONE',  ( -1.000000000000000000, 0.000000000000000000, 0.000000000000000000 ) ) ;
#15149=VERTEX_POINT ( 'NONE', #34418 ) ;
#15152=CIRCLE ( 'NONE', #27162, 31.99999999999998579 ) ;
#15160=DIRECTION ( 'NONE',  ( -1.000000000000000000, -0.000000000000000000, -0.000000000000000000 ) ) ;
#15161=VERTEX_POINT ( 'NONE', #68279 ) ;
#15164=CARTESIAN_POINT ( 'NONE',  ( 0.000000000000000000, 0.000000000000000000, 0.000000000000000000 ) ) ;
#15174=CARTESIAN_POINT ( 'NONE',  ( 11.99999999999999822, 0.000000000000000000, 0.000000000000000000 ) ) ;
#15191=EDGE_LOOP ( 'NONE', ( #677, #14438, #15664, #45445 ) ) ;
#15195=DIRECTION ( 'NONE',  ( -1.000000000000000000, -0.000000000000000000, -0.000000000000000000 ) ) ;
#15197=CARTESIAN_POINT ( 'NONE',  ( 0.000000000000000000, 59.75363087400076267, 56.15606465354979093 ) ) ;
#15202=ORIENTED_EDGE ( 'NONE', *, *, #31482, .F. ) ;
#15208=VECTOR ( 'NONE', #58980, 1000.000000000000227 ) ;
#15222=VERTEX_POINT ( 'NONE', #33682 ) ;
#15229=VERTEX_POINT ( 'NONE', #45734 ) ;
#15234=VERTEX_POINT ( 'NONE', #34802 ) ;
#15239=DIRECTION ( 'NONE',  ( -1.000000000000000000, 0.000000000000000000, 0.000000000000000000 ) ) ;
#15259=VECTOR ( 'NONE', #5491, 1000.000000000000000 ) ;
#15263=CARTESIAN_POINT ( 'NONE',  ( 0.000000000000000000, -33.71516098798793593, 74.74816331893418919 ) ) ;
#15274=DIRECTION ( 'NONE',  ( 0.000000000000000000, 0.000000000000000000, -1.000000000000000000 ) ) ;
#15282=VECTOR ( 'NONE', #8227, 1000.000000000000000 ) ;
#15283=DIRECTION ( 'NONE',  ( 0.000000000000000000, 0.7431448254773878048, -0.6691306063588654540 ) ) ;
#15288=CARTESIAN_POINT ( 'NONE',  ( 11.99999999999999822, 55.38113227695858143, -54.21277698773617715 ) ) ;
#15297=CARTESIAN_POINT ( 'NONE',  ( 0.000000000000000000, 0.000000000000000000, 0.000000000000000000 ) ) ;
#15307=ORIENTED_EDGE ( 'NONE', *, *, #48566, .F. ) ;
#15316=DIRECTION ( 'NONE',  ( 0.000000000000000000, 0.000000000000000000, 1.000000000000000000 ) ) ;
#15322=DIRECTION ( 'NONE',  ( 0.000000000000000000, 0.000000000000000000, 1.000000000000000000 ) ) ;
#15325=CARTESIAN_POINT ( 'NONE',  ( 0.000000000000000000, -41.76106447765533147, 62.50884508063410294 ) ) ;
#15331=ORIENTED_EDGE ( 'NONE', *, *, #31230, .F. ) ;
#15336=ORIENTED_EDGE ( 'NONE', *, *, #70410, .T. ) ;
#15343=ORIENTED_EDGE ( 'NONE', *, *, #10033, .F. ) ;
#15344=CARTESIAN_POINT ( 'NONE',  ( 11.99999999999999822, 29.01471420065673712, -76.69515212745983490 ) ) ;
#15348=AXIS2_PLACEMENT_3D ( 'NONE', #30766, #8599, #31883 ) ;
#15351=CIRCLE ( 'NONE', #36939, 31.99999999999998579 ) ;
#15352=FACE_OUTER_BOUND ( 'NONE', #12603, .T. ) ;
#15353=CARTESIAN_POINT ( 'NONE',  ( -10.00000000000000000, 0.000000000000000000, 0.000000000000000000 ) ) ;
#15361=ADVANCED_FACE ( 'NONE', ( #73759 ), #66655, .T. ) ;
#15369=DIRECTION ( 'NONE',  ( 0.000000000000000000, 0.000000000000000000, -1.000000000000000000 ) ) ;
#15370=DIRECTION ( 'NONE',  ( 0.000000000000000000, 0.000000000000000000, 1.000000000000000000 ) ) ;
#15372=CARTESIAN_POINT ( 'NONE',  ( 11.99999999999999822, 62.50884508063427347, 41.76106447765511831 ) ) ;
#15374=EDGE_CURVE ( 'NONE', #24130, #11963, #26781, .T. ) ;
#15381=DIRECTION ( 'NONE',  ( -1.000000000000000000, 0.000000000000000000, -0.000000000000000000 ) ) ;
#15389=ADVANCED_FACE ( 'NONE', ( #27727 ), #33350, .T. ) ;
#15392=CARTESIAN_POINT ( 'NONE',  ( 6.000000000000000000, -34.94270380257692921, 74.18225833017875459 ) ) ;
#15393=PLANE ( 'NONE',  #48532 ) ;
#15416=CIRCLE ( 'NONE', #71814, 77.49900000000000944 ) ;
#15418=EDGE_CURVE ( 'NONE', #13981, #1170, #5190, .T. ) ;
#15422=AXIS2_PLACEMENT_3D ( 'NONE', #9803, #71828, #32713 ) ;
#15429=LINE ( 'NONE', #4179, #50932 ) ;
#15434=CARTESIAN_POINT ( 'NONE',  ( 5.999999999999999112, -33.71516098798793593, 74.74816331893417498 ) ) ;
#15437=CARTESIAN_POINT ( 'NONE',  ( 15.00000000000000000, -0.9646360437372099028, 23.52805723605590771 ) ) ;
#15438=EDGE_CURVE ( 'NONE', #27488, #61944, #3963, .T. ) ;
#15440=ORIENTED_EDGE ( 'NONE', *, *, #26738, .T. ) ;
#15455=VERTEX_POINT ( 'NONE', #16449 ) ;
#15470=ADVANCED_FACE ( 'NONE', ( #4825 ), #34474, .T. ) ;
#15486=CARTESIAN_POINT ( 'NONE',  ( 11.99999999999999822, 0.000000000000000000, 0.000000000000000000 ) ) ;
#15487=AXIS2_PLACEMENT_3D ( 'NONE', #34963, #23316, #16552 ) ;
#15494=AXIS2_PLACEMENT_3D ( 'NONE', #5089, #68970, #5460 ) ;
#15495=ORIENTED_EDGE ( 'NONE', *, *, #9675, .F. ) ;
#15497=CARTESIAN_POINT ( 'NONE',  ( 12.00000000000000000, -22.67460108101774452, 6.353146135318220367 ) ) ;
#15510=EDGE_CURVE ( 'NONE', #61033, #20162, #48372, .T. ) ;
#15521=CIRCLE ( 'NONE', #9511, 31.99999999999998224 ) ;
#15526=EDGE_LOOP ( 'NONE', ( #65933, #46709, #45689, #38836 ) ) ;
#15537=EDGE_LOOP ( 'NONE', ( #40879, #5569, #18061, #57615 ) ) ;
#15539=ORIENTED_EDGE ( 'NONE', *, *, #12878, .T. ) ;
#15541=AXIS2_PLACEMENT_3D ( 'NONE', #38192, #44212, #61135 ) ;
#15556=ORIENTED_EDGE ( 'NONE', *, *, #59683, .T. ) ;
#15559=EDGE_LOOP ( 'NONE', ( #5756, #34890, #29455, #15133 ) ) ;
#15561=CARTESIAN_POINT ( 'NONE',  ( 11.99999999999999822, -41.76106447765533147, 62.50884508063410294 ) ) ;
#15567=CARTESIAN_POINT ( 'NONE',  ( 0.000000000000000000, 73.95703589263973754, 23.16143007188452430 ) ) ;
#15574=CARTESIAN_POINT ( 'NONE',  ( 11.99999999999999822, 31.47745569255140552, 68.26794271651274926 ) ) ;
#15578=CIRCLE ( 'NONE', #68403, 82.00000000000000000 ) ;
#15581=AXIS2_PLACEMENT_3D ( 'NONE', #39242, #4304, #10657 ) ;
#15591=CYLINDRICAL_SURFACE ( 'NONE', #49680, 31.99999999999998579 ) ;
#15600=CARTESIAN_POINT ( 'NONE',  ( 0.000000000000000000, 2.956366410621684260, -75.11725578898465017 ) ) ;
#15612=ORIENTED_EDGE ( 'NONE', *, *, #48583, .F. ) ;
#15617=LINE ( 'NONE', #51298, #1167 ) ;
#15633=VERTEX_POINT ( 'NONE', #17556 ) ;
#15645=VERTEX_POINT ( 'NONE', #41979 ) ;
#15657=DIRECTION ( 'NONE',  ( 0.000000000000000000, 0.000000000000000000, 1.000000000000000000 ) ) ;
#15658=CARTESIAN_POINT ( 'NONE',  ( 0.000000000000000000, -74.65374052328654386, 8.840884882374837161 ) ) ;
#15664=ORIENTED_EDGE ( 'NONE', *, *, #49219, .T. ) ;
#15669=DIRECTION ( 'NONE',  ( -1.000000000000000000, -0.000000000000000000, -0.000000000000000000 ) ) ;
#15670=DIRECTION ( 'NONE',  ( 0.000000000000000000, -0.9238795325112821866, -0.3826834323651008285 ) ) ;
#15676=CARTESIAN_POINT ( 'NONE',  ( 0.000000000000000000, 8.840884882375075193, 74.65374052328651544 ) ) ;
#15679=CARTESIAN_POINT ( 'NONE',  ( 0.000000000000000000, 76.66974797899835892, 11.30684508768366570 ) ) ;
#15691=DIRECTION ( 'NONE',  ( -1.000000000000000000, -0.000000000000000000, -0.000000000000000000 ) ) ;
#15701=CIRCLE ( 'NONE', #31312, 82.00000000000000000 ) ;
#15704=CIRCLE ( 'NONE', #25319, 82.00000000000000000 ) ;
#15711=DIRECTION ( 'NONE',  ( -1.000000000000000000, 0.000000000000000000, -0.000000000000000000 ) ) ;
#15713=LINE ( 'NONE', #28463, #30879 ) ;
#15716=VERTEX_POINT ( 'NONE', #59635 ) ;
#15717=CARTESIAN_POINT ( 'NONE',  ( 15.00000000000000000, -23.29833615347109088, -3.418703333116486665 ) ) ;
#15721=DIRECTION ( 'NONE',  ( 0.000000000000000000, 0.000000000000000000, -1.000000000000000000 ) ) ;
#15723=ORIENTED_EDGE ( 'NONE', *, *, #56825, .F. ) ;
#15724=CARTESIAN_POINT ( 'NONE',  ( 0.000000000000000000, -49.70050353004846500, -59.46389618802017907 ) ) ;
#15732=VERTEX_POINT ( 'NONE', #32528 ) ;
#15736=ORIENTED_EDGE ( 'NONE', *, *, #69416, .F. ) ;
#15741=CARTESIAN_POINT ( 'NONE',  ( 5.999999999999999112, 71.21200624218795383, 40.65526001592638039 ) ) ;
#15753=DIRECTION ( 'NONE',  ( -1.000000000000000000, 0.000000000000000000, 0.000000000000000000 ) ) ;
#15754=LINE ( 'NONE', #46190, #70457 ) ;
#15767=DIRECTION ( 'NONE',  ( -0.000000000000000000, 0.9781476007338067991, 0.2079116908177533474 ) ) ;
#15778=EDGE_CURVE ( 'NONE', #56906, #9702, #60459, .T. ) ;
#15780=DIRECTION ( 'NONE',  ( 0.000000000000000000, 0.000000000000000000, 1.000000000000000000 ) ) ;
#15784=CARTESIAN_POINT ( 'NONE',  ( 15.00000000000000000, -13.04903810567646971, 19.60159698893442481 ) ) ;
#15785=CARTESIAN_POINT ( 'NONE',  ( 0.000000000000000000, -65.58780272294048075, -36.73666225445966660 ) ) ;
#15787=DIRECTION ( 'NONE',  ( -1.000000000000000000, -0.000000000000000000, 0.000000000000000000 ) ) ;
#15793=VERTEX_POINT ( 'NONE', #31423 ) ;
#15795=DIRECTION ( 'NONE',  ( -1.000000000000000000, 0.000000000000000000, 0.000000000000000000 ) ) ;
#15813=DIRECTION ( 'NONE',  ( 1.000000000000000000, 0.000000000000000000, 0.000000000000000000 ) ) ;
#15814=AXIS2_PLACEMENT_3D ( 'NONE', #4711, #22733, #23462 ) ;
#15815=ORIENTED_EDGE ( 'NONE', *, *, #14958, .T. ) ;
#15830=ORIENTED_EDGE ( 'NONE', *, *, #23785, .F. ) ;
#15831=EDGE_LOOP ( 'NONE', ( #57361, #24133, #27987, #64346 ) ) ;
#15834=CARTESIAN_POINT ( 'NONE',  ( 5.999999999999999112, 56.15606465355041621, -59.75363087400017292 ) ) ;
#15836=ORIENTED_EDGE ( 'NONE', *, *, #24508, .F. ) ;
#15840=DIRECTION ( 'NONE',  ( 0.000000000000000000, -0.1045284632676449221, 0.9945218953682741780 ) ) ;
#15844=CARTESIAN_POINT ( 'NONE',  ( 11.99999999999999822, 0.000000000000000000, 0.000000000000000000 ) ) ;
#15852=VERTEX_POINT ( 'NONE', #14120 ) ;
#15853=CARTESIAN_POINT ( 'NONE',  ( 5.999999999999999112, 74.74816331893477184, -33.71516098798660011 ) ) ;
#15854=DIRECTION ( 'NONE',  ( 1.000000000000000000, 0.000000000000000000, -0.000000000000000000 ) ) ;
#15859=DIRECTION ( 'NONE',  ( -1.000000000000000000, 0.000000000000000000, 0.000000000000000000 ) ) ;
#15865=CARTESIAN_POINT ( 'NONE',  ( 6.000000000000000000, 71.87247863392413194, 39.47590169984871267 ) ) ;
#15866=AXIS2_PLACEMENT_3D ( 'NONE', #62639, #4376, #34039 ) ;
#15867=EDGE_CURVE ( 'NONE', #12556, #65739, #70042, .T. ) ;
#15868=DIRECTION ( 'NONE',  ( 0.000000000000000000, 0.000000000000000000, 1.000000000000000000 ) ) ;
#15873=DIRECTION ( 'NONE',  ( 0.000000000000000000, 0.000000000000000000, 1.000000000000000000 ) ) ;
#15874=VERTEX_POINT ( 'NONE', #73117 ) ;
#15880=DIRECTION ( 'NONE',  ( 0.000000000000000000, -0.9876883405951394357, 0.1564344650402203496 ) ) ;
#15888=VERTEX_POINT ( 'NONE', #16740 ) ;
#15890=VERTEX_POINT ( 'NONE', #45696 ) ;
#15901=AXIS2_PLACEMENT_3D ( 'NONE', #1823, #65681, #30342 ) ;
#15902=ORIENTED_EDGE ( 'NONE', *, *, #45678, .T. ) ;
#15904=DIRECTION ( 'NONE',  ( -1.000000000000000000, -0.000000000000000000, -0.000000000000000000 ) ) ;
#15909=CARTESIAN_POINT ( 'NONE',  ( -10.00000000000000000, 0.000000000000000000, 0.000000000000000000 ) ) ;
#15911=ORIENTED_EDGE ( 'NONE', *, *, #23338, .T. ) ;
#15913=VECTOR ( 'NONE', #27868, 1000.000000000000114 ) ;
#15917=PLANE ( 'NONE',  #62970 ) ;
#15920=CARTESIAN_POINT ( 'NONE',  ( 15.00000000000000000, 16.61724383029361718, -20.69703378468926402 ) ) ;
#15928=CYLINDRICAL_SURFACE ( 'NONE', #9724, 31.99999999999998579 ) ;
#15937=DIRECTION ( 'NONE',  ( -1.000000000000000000, 0.000000000000000000, 0.000000000000000000 ) ) ;
#15938=LINE ( 'NONE', #38878, #6994 ) ;
#15939=FACE_OUTER_BOUND ( 'NONE', #66034, .T. ) ;
#15940=DIRECTION ( 'NONE',  ( 0.000000000000000000, 0.6494480483301849905, -0.7604059656000298206 ) ) ;
#15944=ORIENTED_EDGE ( 'NONE', *, *, #19674, .T. ) ;
#15950=DIRECTION ( 'NONE',  ( -1.000000000000000000, 0.000000000000000000, -0.000000000000000000 ) ) ;
#15951=CARTESIAN_POINT ( 'NONE',  ( 11.99999999999999822, 14.67089635893819377, -73.72996012237423713 ) ) ;
#15952=EDGE_CURVE ( 'NONE', #52714, #12392, #73639, .T. ) ;
#15984=AXIS2_PLACEMENT_3D ( 'NONE', #12256, #62683, #5164 ) ;
#15991=ORIENTED_EDGE ( 'NONE', *, *, #20632, .F. ) ;
#16023=CIRCLE ( 'NONE', #49648, 77.49899999999999523 ) ;
#16028=EDGE_CURVE ( 'NONE', #26970, #5289, #29193, .T. ) ;
#16034=DIRECTION ( 'NONE',  ( -1.000000000000000000, -0.000000000000000000, 0.000000000000000000 ) ) ;
#16040=CYLINDRICAL_SURFACE ( 'NONE', #70561, 31.99999999999998579 ) ;
#16042=CARTESIAN_POINT ( 'NONE',  ( 11.99999999999999822, 0.000000000000000000, 0.000000000000000000 ) ) ;
#16044=DIRECTION ( 'NONE',  ( -1.000000000000000000, -0.000000000000000000, -0.000000000000000000 ) ) ;
#16047=PLANE ( 'NONE',  #25134 ) ;
#16048=VECTOR ( 'NONE', #32502, 1000.000000000000000 ) ;
#16049=EDGE_CURVE ( 'NONE', #12729, #66558, #18844, .T. ) ;
#16050=CARTESIAN_POINT ( 'NONE',  ( 11.99999999999999822, 73.72996012237440766, 14.67089635893739619 ) ) ;
#16051=LINE ( 'NONE', #65803, #70643 ) ;
#16056=VERTEX_POINT ( 'NONE', #52701 ) ;
#16060=DIRECTION ( 'NONE',  ( -1.000000000000000000, 0.000000000000000000, 0.000000000000000000 ) ) ;
#16069=CARTESIAN_POINT ( 'NONE',  ( 11.99999999999999822, -2.946379043146863719, 75.11764819372146462 ) ) ;
#16070=VECTOR ( 'NONE', #45000, 1000.000000000000000 ) ;
#16074=ORIENTED_EDGE ( 'NONE', *, *, #42713, .T. ) ;
#16097=VECTOR ( 'NONE', #8912, 1000.000000000000000 ) ;
#16098=VERTEX_POINT ( 'NONE', #65476 ) ;
#16103=CYLINDRICAL_SURFACE ( 'NONE', #62197, 77.49899999999999523 ) ;
#16106=CARTESIAN_POINT ( 'NONE',  ( 11.99999999999999822, -73.72996012237429397, -14.67089635893794508 ) ) ;
#16109=LINE ( 'NONE', #27375, #51309 ) ;
#16120=CARTESIAN_POINT ( 'NONE',  ( 15.00000000000000000, 20.85821328998741109, -10.92862929874522671 ) ) ;
#16128=ADVANCED_FACE ( 'NONE', ( #12835 ), #35762, .T. ) ;
#16137=DIRECTION ( 'NONE',  ( -1.000000000000000000, 0.000000000000000000, 0.000000000000000000 ) ) ;
#16141=DIRECTION ( 'NONE',  ( -1.000000000000000000, -0.000000000000000000, 0.000000000000000000 ) ) ;
#16142=VECTOR ( 'NONE', #65001, 1000.000000000000000 ) ;
#16144=EDGE_CURVE ( 'NONE', #66576, #15455, #41298, .T. ) ;
#16146=AXIS2_PLACEMENT_3D ( 'NONE', #6498, #29398, #52342 ) ;
#16149=CARTESIAN_POINT ( 'NONE',  ( 0.000000000000000000, 0.000000000000000000, 0.000000000000000000 ) ) ;
#16157=CARTESIAN_POINT ( 'NONE',  ( 15.00000000000000000, 23.59884966291521380, -12.14883922797262805 ) ) ;
#16172=VECTOR ( 'NONE', #20414, 1000.000000000000000 ) ;
#16176=ORIENTED_EDGE ( 'NONE', *, *, #10612, .T. ) ;
#16189=ORIENTED_EDGE ( 'NONE', *, *, #73983, .F. ) ;
#16192=EDGE_LOOP ( 'NONE', ( #34149, #29203, #2548, #33777 ) ) ;
#16198=CARTESIAN_POINT ( 'NONE',  ( 11.99999999999999822, -77.49459641780886443, 0.8261519478428549501 ) ) ;
#16203=CYLINDRICAL_SURFACE ( 'NONE', #43175, 82.00000000000000000 ) ;
#16205=VERTEX_POINT ( 'NONE', #61312 ) ;
#16212=CARTESIAN_POINT ( 'NONE',  ( 11.99999999999999822, -75.11764819372145041, -2.946379043147127064 ) ) ;
#16223=AXIS2_PLACEMENT_3D ( 'NONE', #21896, #30666, #26785 ) ;
#16228=EDGE_CURVE ( 'NONE', #4971, #49355, #5302, .T. ) ;
#16235=CIRCLE ( 'NONE', #35450, 31.99999999999997868 ) ;
#16237=ADVANCED_FACE ( 'NONE', ( #14689 ), #48898, .T. ) ;
#16240=CARTESIAN_POINT ( 'NONE',  ( 11.99999999999999822, -74.65491531819111515, -8.830959090343204920 ) ) ;
#16245=EDGE_CURVE ( 'NONE', #49792, #6124, #12457, .T. ) ;
#16251=DIRECTION ( 'NONE',  ( 0.000000000000000000, 0.000000000000000000, 1.000000000000000000 ) ) ;
#16256=DIRECTION ( 'NONE',  ( 0.000000000000000000, -0.9723699203976740035, -0.2334453638559160216 ) ) ;
#16267=VERTEX_POINT ( 'NONE', #71823 ) ;
#16269=LINE ( 'NONE', #73023, #47969 ) ;
#16271=DIRECTION ( 'NONE',  ( -1.000000000000000000, -0.000000000000000000, -0.000000000000000000 ) ) ;
#16281=DIRECTION ( 'NONE',  ( 0.000000000000000000, 0.000000000000000000, 1.000000000000000000 ) ) ;
#16289=DIRECTION ( 'NONE',  ( -1.000000000000000000, -0.000000000000000000, -0.000000000000000000 ) ) ;
#16290=EDGE_CURVE ( 'NONE', #30983, #48336, #56858, .T. ) ;
#16293=ORIENTED_EDGE ( 'NONE', *, *, #2511, .T. ) ;
#16294=CIRCLE ( 'NONE', #58314, 31.99999999999998224 ) ;
#16299=ORIENTED_EDGE ( 'NONE', *, *, #27899, .T. ) ;
#16301=DIRECTION ( 'NONE',  ( -1.000000000000000000, 0.000000000000000000, -0.000000000000000000 ) ) ;
#16317=CARTESIAN_POINT ( 'NONE',  ( 11.99999999999999822, 0.000000000000000000, 0.000000000000000000 ) ) ;
#16326=CARTESIAN_POINT ( 'NONE',  ( 11.99999999999999822, -59.75363087400113926, 56.15606465354937171 ) ) ;
#16329=DIRECTION ( 'NONE',  ( 0.000000000000000000, 0.000000000000000000, 1.000000000000000000 ) ) ;
#16356=ORIENTED_EDGE ( 'NONE', *, *, #33885, .F. ) ;
#16366=EDGE_CURVE ( 'NONE', #47354, #40774, #46238, .T. ) ;
#16367=VERTEX_POINT ( 'NONE', #69173 ) ;
#16371=DIRECTION ( 'NONE',  ( -1.000000000000000000, -0.000000000000000000, 0.000000000000000000 ) ) ;
#16381=DIRECTION ( 'NONE',  ( 0.000000000000000000, -0.5224985647159380298, -0.8526401643540988395 ) ) ;
#16399=VECTOR ( 'NONE', #40331, 999.9999999999998863 ) ;
#16400=ORIENTED_EDGE ( 'NONE', *, *, #4442, .F. ) ;
#16401=AXIS2_PLACEMENT_3D ( 'NONE', #39830, #22159, #44347 ) ;
#16415=DIRECTION ( 'NONE',  ( -1.000000000000000000, 0.000000000000000000, 0.000000000000000000 ) ) ;
#16417=DIRECTION ( 'NONE',  ( -1.000000000000000000, -0.000000000000000000, -0.000000000000000000 ) ) ;
#16419=LINE ( 'NONE', #22433, #55672 ) ;
#16424=CYLINDRICAL_SURFACE ( 'NONE', #44355, 31.99999999999998579 ) ;
#16434=DIRECTION ( 'NONE',  ( 0.000000000000000000, 0.000000000000000000, -1.000000000000000000 ) ) ;
#16437=DIRECTION ( 'NONE',  ( 1.000000000000000000, 0.000000000000000000, -0.000000000000000000 ) ) ;
#16441=ORIENTED_EDGE ( 'NONE', *, *, #61084, .T. ) ;
#16442=EDGE_CURVE ( 'NONE', #11963, #8256, #29295, .T. ) ;
#16445=EDGE_CURVE ( 'NONE', #15716, #61582, #16546, .T. ) ;
#16449=CARTESIAN_POINT ( 'NONE',  ( 11.99999999999999822, 18.89407956138257205, 75.16055320797038064 ) ) ;
#16450=EDGE_CURVE ( 'NONE', #57513, #58250, #62437, .T. ) ;
#16452=DIRECTION ( 'NONE',  ( 0.000000000000000000, 0.07845909572784530439, -0.9969173337331279638 ) ) ;
#16469=ORIENTED_EDGE ( 'NONE', *, *, #17080, .T. ) ;
#16478=ORIENTED_EDGE ( 'NONE', *, *, #53163, .F. ) ;
#16482=CARTESIAN_POINT ( 'NONE',  ( 11.99999999999999822, -75.16055320797016748, -18.89407956138335365 ) ) ;
#16489=ADVANCED_FACE ( 'NONE', ( #48082 ), #13849, .T. ) ;
#16491=ADVANCED_FACE ( 'NONE', ( #25513 ), #40974, .T. ) ;
#16493=CARTESIAN_POINT ( 'NONE',  ( 0.000000000000000000, -46.54456581323762521, -59.03342792756313884 ) ) ;
#16498=FACE_OUTER_BOUND ( 'NONE', #66733, .T. ) ;
#16503=VECTOR ( 'NONE', #29078, 1000.000000000000000 ) ;
#16506=CARTESIAN_POINT ( 'NONE',  ( 11.99999999999999822, -30.41916302227164337, 71.27951684758015460 ) ) ;
#16514=CARTESIAN_POINT ( 'NONE',  ( 0.000000000000000000, 29.01471420065563933, 76.69515212746026123 ) ) ;
#16521=ORIENTED_EDGE ( 'NONE', *, *, #47397, .T. ) ;
#16522=CARTESIAN_POINT ( 'NONE',  ( 11.99999999999999822, -73.73191006444582740, 14.66109333815435889 ) ) ;
#16525=DIRECTION ( 'NONE',  ( 0.000000000000000000, 0.000000000000000000, 1.000000000000000000 ) ) ;
#16528=EDGE_CURVE ( 'NONE', #64295, #143, #67746, .T. ) ;
#16533=CARTESIAN_POINT ( 'NONE',  ( 11.99999999999999822, 63.18004540533030422, 44.88180994100399346 ) ) ;
#16538=EDGE_CURVE ( 'NONE', #61399, #46926, #54534, .T. ) ;
#16539=EDGE_CURVE ( 'NONE', #32269, #40792, #24547, .T. ) ;
#16545=VECTOR ( 'NONE', #15003, 1000.000000000000000 ) ;
#16546=LINE ( 'NONE', #39493, #62889 ) ;
#16552=DIRECTION ( 'NONE',  ( 0.000000000000000000, 0.000000000000000000, 1.000000000000000000 ) ) ;
#16565=ORIENTED_EDGE ( 'NONE', *, *, #37335, .T. ) ;
#16579=EDGE_CURVE ( 'NONE', #15229, #50948, #59326, .T. ) ;
#16599=DIRECTION ( 'NONE',  ( 0.000000000000000000, 0.2079116908177555123, -0.9781476007338064660 ) ) ;
#16602=FACE_OUTER_BOUND ( 'NONE', #63883, .T. ) ;
#16606=DIRECTION ( 'NONE',  ( -1.000000000000000000, 0.000000000000000000, 0.000000000000000000 ) ) ;
#16617=EDGE_CURVE ( 'NONE', #31218, #36914, #1726, .T. ) ;
#16619=CARTESIAN_POINT ( 'NONE',  ( 6.000000000000000000, 81.50828551894240093, -8.966570791699810528 ) ) ;
#16620=VERTEX_POINT ( 'NONE', #47704 ) ;
#16622=CARTESIAN_POINT ( 'NONE',  ( 11.99999999999999822, 75.11725578898467859, 2.956366410620910656 ) ) ;
#16623=CARTESIAN_POINT ( 'NONE',  ( 11.99999999999999822, -2.956366410621191765, 75.11725578898467859 ) ) ;
#16632=DIRECTION ( 'NONE',  ( -1.000000000000000000, 0.000000000000000000, 0.000000000000000000 ) ) ;
#16633=ORIENTED_EDGE ( 'NONE', *, *, #34539, .T. ) ;
#16641=VERTEX_POINT ( 'NONE', #61589 ) ;
#16647=EDGE_CURVE ( 'NONE', #69147, #67241, #18530, .T. ) ;
#16659=VECTOR ( 'NONE', #3852, 1000.000000000000000 ) ;
#16660=DIRECTION ( 'NONE',  ( 0.000000000000000000, -0.5877852522924803536, 0.8090169943749422332 ) ) ;
#16661=FACE_OUTER_BOUND ( 'NONE', #45902, .T. ) ;
#16664=CARTESIAN_POINT ( 'NONE',  ( 6.000000000000000000, -2.543863470248951320, 81.96053171279901051 ) ) ;
#16665=CARTESIAN_POINT ( 'NONE',  ( 0.000000000000000000, 81.96053171279902472, 2.543863470248677316 ) ) ;
#16668=EDGE_CURVE ( 'NONE', #28318, #63927, #26984, .T. ) ;
#16669=ORIENTED_EDGE ( 'NONE', *, *, #21278, .F. ) ;
#16676=CARTESIAN_POINT ( 'NONE',  ( 0.000000000000000000, 55.38113227695858143, -54.21277698773617715 ) ) ;
#16684=ORIENTED_EDGE ( 'NONE', *, *, #62980, .F. ) ;
#16687=VECTOR ( 'NONE', #47427, 1000.000000000000114 ) ;
#16695=DIRECTION ( 'NONE',  ( -1.000000000000000000, 0.000000000000000000, 0.000000000000000000 ) ) ;
#16697=ORIENTED_EDGE ( 'NONE', *, *, #58049, .T. ) ;
#16703=DIRECTION ( 'NONE',  ( -1.000000000000000000, -0.000000000000000000, -0.000000000000000000 ) ) ;
#16706=AXIS2_PLACEMENT_3D ( 'NONE', #44505, #62927, #11384 ) ;
#16732=CARTESIAN_POINT ( 'NONE',  ( -10.00000000000000000, 0.000000000000000000, 0.000000000000000000 ) ) ;
#16735=ORIENTED_EDGE ( 'NONE', *, *, #31137, .F. ) ;
#16736=VECTOR ( 'NONE', #31143, 1000.000000000000000 ) ;
#16737=ORIENTED_EDGE ( 'NONE', *, *, #43425, .F. ) ;
#16740=CARTESIAN_POINT ( 'NONE',  ( 11.99999999999999822, 74.74816331893428867, 33.71516098798767302 ) ) ;
#16747=EDGE_LOOP ( 'NONE', ( #10902, #4611, #34494, #13552 ) ) ;
#16749=ORIENTED_EDGE ( 'NONE', *, *, #36938, .T. ) ;
#16752=EDGE_CURVE ( 'NONE', #4754, #42720, #58139, .T. ) ;
#16755=CYLINDRICAL_SURFACE ( 'NONE', #4216, 31.99999999999998579 ) ;
#16757=DIRECTION ( 'NONE',  ( -1.000000000000000000, -0.000000000000000000, 0.000000000000000000 ) ) ;
#16760=ORIENTED_EDGE ( 'NONE', *, *, #4001, .F. ) ;
#16766=AXIS2_PLACEMENT_3D ( 'NONE', #17321, #28589, #52640 ) ;
#16770=DIRECTION ( 'NONE',  ( -1.000000000000000000, 0.000000000000000000, 0.000000000000000000 ) ) ;
#16772=CARTESIAN_POINT ( 'NONE',  ( 11.99999999999999822, 0.000000000000000000, 0.000000000000000000 ) ) ;
#16781=AXIS2_PLACEMENT_3D ( 'NONE', #24577, #42251, #36222 ) ;
#16789=ORIENTED_EDGE ( 'NONE', *, *, #25986, .T. ) ;
#16790=AXIS2_PLACEMENT_3D ( 'NONE', #725, #59679, #30714 ) ;
#16793=DIRECTION ( 'NONE',  ( -1.000000000000000000, -0.000000000000000000, 0.000000000000000000 ) ) ;
#16794=CARTESIAN_POINT ( 'NONE',  ( 11.99999999999999822, 59.46389618801966037, 49.70050353004911159 ) ) ;
#16796=CARTESIAN_POINT ( 'NONE',  ( 12.00000000000000000, 6.762365576493649222, 25.66652317338391853 ) ) ;
#16800=VECTOR ( 'NONE', #32607, 1000.000000000000000 ) ;
#16805=CYLINDRICAL_SURFACE ( 'NONE', #40998, 31.99999999999998579 ) ;
#16811=DIRECTION ( 'NONE',  ( -1.000000000000000000, -0.000000000000000000, 0.000000000000000000 ) ) ;
#16815=FACE_OUTER_BOUND ( 'NONE', #21738, .T. ) ;
#16819=DIRECTION ( 'NONE',  ( -1.000000000000000000, -0.000000000000000000, 0.000000000000000000 ) ) ;
#16827=DIRECTION ( 'NONE',  ( 0.000000000000000000, 0.000000000000000000, 1.000000000000000000 ) ) ;
#16828=LINE ( 'NONE', #73578, #37697 ) ;
#16836=ORIENTED_EDGE ( 'NONE', *, *, #71758, .T. ) ;
#16840=AXIS2_PLACEMENT_3D ( 'NONE', #17400, #40333, #29045 ) ;
#16845=CIRCLE ( 'NONE', #56461, 31.99999999999998934 ) ;
#16854=LINE ( 'NONE', #4849, #54250 ) ;
#16861=DIRECTION ( 'NONE',  ( 0.000000000000000000, 0.000000000000000000, 1.000000000000000000 ) ) ;
#16869=CARTESIAN_POINT ( 'NONE',  ( 0.000000000000000000, -55.16347631943085617, 60.67117009219117563 ) ) ;
#16876=DIRECTION ( 'NONE',  ( 1.000000000000000000, -0.000000000000000000, -0.000000000000000000 ) ) ;
#16878=DIRECTION ( 'NONE',  ( -1.000000000000000000, 0.000000000000000000, 0.000000000000000000 ) ) ;
#16879=DIRECTION ( 'NONE',  ( -1.000000000000000000, 0.000000000000000000, 0.000000000000000000 ) ) ;
#16880=CIRCLE ( 'NONE', #22899, 31.99999999999998934 ) ;
#16890=CARTESIAN_POINT ( 'NONE',  ( 6.000000000000000000, -78.73519480814938731, -22.90783923731713045 ) ) ;
#16898=DIRECTION ( 'NONE',  ( -1.000000000000000000, -0.000000000000000000, -0.000000000000000000 ) ) ;
#16900=FACE_OUTER_BOUND ( 'NONE', #71378, .T. ) ;
#16902=ADVANCED_FACE ( 'NONE', ( #33363 ), #28855, .T. ) ;
#16909=DIRECTION ( 'NONE',  ( 0.000000000000000000, -0.8090169943749426773, 0.5877852522924797984 ) ) ;
#16938=DIRECTION ( 'NONE',  ( 0.000000000000000000, -0.1045284632676449221, 0.9945218953682741780 ) ) ;
#16940=AXIS2_PLACEMENT_3D ( 'NONE', #32666, #67268, #21016 ) ;
#16941=EDGE_LOOP ( 'NONE', ( #60123, #50855, #27226, #30536 ) ) ;
#16942=ORIENTED_EDGE ( 'NONE', *, *, #26124, .F. ) ;
#16944=FACE_OUTER_BOUND ( 'NONE', #12697, .T. ) ;
#16950=VECTOR ( 'NONE', #36382, 1000.000000000000000 ) ;
#16951=CARTESIAN_POINT ( 'NONE',  ( 11.99999999999999822, 41.76106447765489094, 62.50884508063442269 ) ) ;
#16957=CARTESIAN_POINT ( 'NONE',  ( 12.00000000000000000, 8.688484142254226938, 21.88630264137359305 ) ) ;
#16960=CARTESIAN_POINT ( 'NONE',  ( 11.99999999999999822, -46.11716303203233736, 67.80270845531873647 ) ) ;
#16965=CARTESIAN_POINT ( 'NONE',  ( 15.00000000000000000, -20.55727247249726020, 16.78983467731313084 ) ) ;
#16971=CARTESIAN_POINT ( 'NONE',  ( 11.99999999999999822, -23.16143007188479430, 73.95703589263968070 ) ) ;
#16979=AXIS2_PLACEMENT_3D ( 'NONE', #60243, #30894, #53839 ) ;
#16983=CARTESIAN_POINT ( 'NONE',  ( 0.000000000000000000, -20.40083707022935400, 72.35432306680478121 ) ) ;
#16987=AXIS2_PLACEMENT_3D ( 'NONE', #16772, #57000, #44227 ) ;
#16989=ORIENTED_EDGE ( 'NONE', *, *, #11193, .F. ) ;
#16994=DIRECTION ( 'NONE',  ( -1.000000000000000000, 0.000000000000000000, 0.000000000000000000 ) ) ;
#16995=DIRECTION ( 'NONE',  ( -1.000000000000000000, -0.000000000000000000, 0.000000000000000000 ) ) ;
#16996=AXIS2_PLACEMENT_3D ( 'NONE', #39245, #33965, #9918 ) ;
#17006=DIRECTION ( 'NONE',  ( -1.000000000000000000, 0.000000000000000000, 0.000000000000000000 ) ) ;
#17009=DIRECTION ( 'NONE',  ( -1.000000000000000000, 0.000000000000000000, 0.000000000000000000 ) ) ;
#17012=ORIENTED_EDGE ( 'NONE', *, *, #35721, .F. ) ;
#17013=CARTESIAN_POINT ( 'NONE',  ( 0.000000000000000000, -11.30684508768393570, 76.66974797899831628 ) ) ;
#17014=ORIENTED_EDGE ( 'NONE', *, *, #31129, .T. ) ;
#17015=LINE ( 'NONE', #55473, #54935 ) ;
#17020=ORIENTED_EDGE ( 'NONE', *, *, #18098, .F. ) ;
#17023=VERTEX_POINT ( 'NONE', #52149 ) ;
#17031=AXIS2_PLACEMENT_3D ( 'NONE', #57573, #45928, #6082 ) ;
#17033=DIRECTION ( 'NONE',  ( 0.000000000000000000, 0.3826834323650841752, 0.9238795325112891810 ) ) ;
#17036=CARTESIAN_POINT ( 'NONE',  ( 0.000000000000000000, 0.000000000000000000, 0.000000000000000000 ) ) ;
#17048=LINE ( 'NONE', #12506, #5631 ) ;
#17055=FACE_OUTER_BOUND ( 'NONE', #6423, .T. ) ;
#17057=CIRCLE ( 'NONE', #37503, 82.00000000000000000 ) ;
#17063=DIRECTION ( 'NONE',  ( 0.000000000000000000, 0.000000000000000000, 1.000000000000000000 ) ) ;
#17066=DIRECTION ( 'NONE',  ( -1.000000000000000000, -0.000000000000000000, -0.000000000000000000 ) ) ;
#17072=FACE_OUTER_BOUND ( 'NONE', #1082, .T. ) ;
#17073=CARTESIAN_POINT ( 'NONE',  ( 11.99999999999999822, 73.73191006444572793, -14.66109333815486515 ) ) ;
#17074=CARTESIAN_POINT ( 'NONE',  ( 11.99999999999999822, 70.52718814184260054, 26.02418014898334420 ) ) ;
#17078=( LENGTH_UNIT ( ) NAMED_UNIT ( * ) SI_UNIT ( .MILLI., .METRE. ) );
#17079=ADVANCED_FACE ( 'NONE', ( #35965 ), #58166, .T. ) ;
#17080=EDGE_CURVE ( 'NONE', #56648, #18566, #64189, .T. ) ;
#17089=CIRCLE ( 'NONE', #26674, 31.99999999999998934 ) ;
#17093=CIRCLE ( 'NONE', #36295, 82.00000000000000000 ) ;
#17104=ORIENTED_EDGE ( 'NONE', *, *, #68679, .T. ) ;
#17105=VERTEX_POINT ( 'NONE', #1803 ) ;
#17107=VERTEX_POINT ( 'NONE', #24690 ) ;
#17112=ORIENTED_EDGE ( 'NONE', *, *, #63996, .F. ) ;
#17113=ORIENTED_EDGE ( 'NONE', *, *, #62108, .F. ) ;
#17121=DIRECTION ( 'NONE',  ( -1.000000000000000000, 0.000000000000000000, 0.000000000000000000 ) ) ;
#17133=DIRECTION ( 'NONE',  ( 0.000000000000000000, 0.3090169943749480064, -0.9510565162951534202 ) ) ;
#17134=EDGE_CURVE ( 'NONE', #26057, #73333, #4002, .T. ) ;
#17135=CARTESIAN_POINT ( 'NONE',  ( 11.99999999999999822, -30.41916302227164337, 71.27951684758015460 ) ) ;
#17140=DIRECTION ( 'NONE',  ( 0.000000000000000000, 0.3826834323650904479, -0.9238795325112865164 ) ) ;
#17147=AXIS2_PLACEMENT_3D ( 'NONE', #39163, #27116, #62098 ) ;
#17148=CARTESIAN_POINT ( 'NONE',  ( 15.00000000000000000, -1.278221433540507546, -26.51162292216071492 ) ) ;
#17149=LINE ( 'NONE', #34429, #10258 ) ;
#17151=AXIS2_PLACEMENT_3D ( 'NONE', #68709, #319, #39765 ) ;
#17154=VERTEX_POINT ( 'NONE', #26159 ) ;
#17157=VECTOR ( 'NONE', #61821, 1000.000000000000000 ) ;
#17163=CARTESIAN_POINT ( 'NONE',  ( 0.000000000000000000, -33.71516098798685590, -74.74816331893465815 ) ) ;
#17166=FACE_OUTER_BOUND ( 'NONE', #67513, .T. ) ;
#17172=ORIENTED_EDGE ( 'NONE', *, *, #21030, .T. ) ;
#17173=DIRECTION ( 'NONE',  ( 0.000000000000000000, 0.2334453638559058908, -0.9723699203976765570 ) ) ;
#17176=EDGE_CURVE ( 'NONE', #56792, #15793, #61483, .T. ) ;
#17177=DIRECTION ( 'NONE',  ( -1.000000000000000000, 0.000000000000000000, 0.000000000000000000 ) ) ;
#17181=FACE_OUTER_BOUND ( 'NONE', #40222, .T. ) ;
#17183=CARTESIAN_POINT ( 'NONE',  ( -10.00000000000000000, 0.000000000000000000, 0.000000000000000000 ) ) ;
#17188=CIRCLE ( 'NONE', #65234, 31.99999999999998579 ) ;
#17208=DIRECTION ( 'NONE',  ( -1.000000000000000000, -0.000000000000000000, -0.000000000000000000 ) ) ;
#17211=ORIENTED_EDGE ( 'NONE', *, *, #13913, .F. ) ;
#17220=CYLINDRICAL_SURFACE ( 'NONE', #51385, 31.99999999999998579 ) ;
#17221=CARTESIAN_POINT ( 'NONE',  ( 11.99999999999999822, -71.27951684758005513, -30.41916302227188851 ) ) ;
#17226=LINE ( 'NONE', #22882, #56715 ) ;
#17229=EDGE_CURVE ( 'NONE', #32135, #71894, #21250, .T. ) ;
#17233=EDGE_CURVE ( 'NONE', #39724, #66486, #49445, .T. ) ;
#17238=CARTESIAN_POINT ( 'NONE',  ( 0.000000000000000000, -44.99326035066007279, -68.55367621811190304 ) ) ;
#17241=ORIENTED_EDGE ( 'NONE', *, *, #55692, .F. ) ;
#17258=CARTESIAN_POINT ( 'NONE',  ( 11.99999999999999822, -5.256550761632340141, -77.32052557432847095 ) ) ;
#17266=DIRECTION ( 'NONE',  ( 0.000000000000000000, 0.000000000000000000, 1.000000000000000000 ) ) ;
#17267=CARTESIAN_POINT ( 'NONE',  ( 11.99999999999999822, 0.000000000000000000, 0.000000000000000000 ) ) ;
#17275=ORIENTED_EDGE ( 'NONE', *, *, #9989, .F. ) ;
#17279=AXIS2_PLACEMENT_3D ( 'NONE', #56356, #57099, #10474 ) ;
#17287=ORIENTED_EDGE ( 'NONE', *, *, #44259, .F. ) ;
#17289=AXIS2_PLACEMENT_3D ( 'NONE', #20706, #3443, #26346 ) ;
#17290=DIRECTION ( 'NONE',  ( -0.000000000000000000, 0.9781476007338042455, -0.2079116908177663092 ) ) ;
#17297=ORIENTED_EDGE ( 'NONE', *, *, #66105, .T. ) ;
#17305=ORIENTED_EDGE ( 'NONE', *, *, #2741, .T. ) ;
#17306=DIRECTION ( 'NONE',  ( -1.000000000000000000, -0.000000000000000000, 0.000000000000000000 ) ) ;
#17307=CIRCLE ( 'NONE', #29266, 31.99999999999998934 ) ;
#17310=EDGE_LOOP ( 'NONE', ( #36534, #36142, #19118, #39578 ) ) ;
#17317=ORIENTED_EDGE ( 'NONE', *, *, #70232, .F. ) ;
#17321=CARTESIAN_POINT ( 'NONE',  ( 0.000000000000000000, 59.03342792756328095, -46.54456581323744757 ) ) ;
#17326=DIRECTION ( 'NONE',  ( -1.000000000000000000, 0.000000000000000000, 0.000000000000000000 ) ) ;
#17341=CARTESIAN_POINT ( 'NONE',  ( 0.000000000000000000, 46.54456581323805153, 59.03342792756280488 ) ) ;
#17344=EDGE_CURVE ( 'NONE', #25482, #61033, #26631, .T. ) ;
#17350=LINE ( 'NONE', #27885, #40489 ) ;
#17354=DIRECTION ( 'NONE',  ( 0.000000000000000000, 0.000000000000000000, 1.000000000000000000 ) ) ;
#17368=DIRECTION ( 'NONE',  ( -1.000000000000000000, 0.000000000000000000, -0.000000000000000000 ) ) ;
#17370=EDGE_CURVE ( 'NONE', #39963, #10633, #60306, .T. ) ;
#17375=CARTESIAN_POINT ( 'NONE',  ( 0.000000000000000000, 0.000000000000000000, 0.000000000000000000 ) ) ;
#17383=ORIENTED_EDGE ( 'NONE', *, *, #29092, .F. ) ;
#17384=EDGE_CURVE ( 'NONE', #1863, #21262, #46065, .T. ) ;
#17394=AXIS2_PLACEMENT_3D ( 'NONE', #58919, #64551, #35234 ) ;
#17398=DIRECTION ( 'NONE',  ( 0.000000000000000000, 0.5877852522924685852, 0.8090169943749506709 ) ) ;
#17399=CARTESIAN_POINT ( 'NONE',  ( 12.00000000000000000, -26.23277895567245466, 4.042438405570107918 ) ) ;
#17400=CARTESIAN_POINT ( 'NONE',  ( 0.000000000000000000, -20.41045688087876897, 72.35160999960810102 ) ) ;
#17404=ORIENTED_EDGE ( 'NONE', *, *, #38347, .F. ) ;
#17408=LINE ( 'NONE', #12863, #43122 ) ;
#17411=DIRECTION ( 'NONE',  ( 0.000000000000000000, 0.000000000000000000, 1.000000000000000000 ) ) ;
#17421=ORIENTED_EDGE ( 'NONE', *, *, #14660, .F. ) ;
#17432=DIRECTION ( 'NONE',  ( 0.000000000000000000, 0.000000000000000000, 1.000000000000000000 ) ) ;
#17440=DIRECTION ( 'NONE',  ( 0.000000000000000000, 0.000000000000000000, 1.000000000000000000 ) ) ;
#17460=AXIS2_PLACEMENT_3D ( 'NONE', #34795, #69015, #40431 ) ;
#17465=ORIENTED_EDGE ( 'NONE', *, *, #903, .F. ) ;
#17467=CIRCLE ( 'NONE', #59500, 82.00000000000000000 ) ;
#17468=ORIENTED_EDGE ( 'NONE', *, *, #66198, .T. ) ;
#17472=ORIENTED_EDGE ( 'NONE', *, *, #19373, .F. ) ;
#17485=DIRECTION ( 'NONE',  ( 1.000000000000000000, 0.000000000000000000, 0.000000000000000000 ) ) ;
#17490=ORIENTED_EDGE ( 'NONE', *, *, #37594, .F. ) ;
#17494=VERTEX_POINT ( 'NONE', #7685 ) ;
#17512=CARTESIAN_POINT ( 'NONE',  ( 0.000000000000000000, 0.000000000000000000, 0.000000000000000000 ) ) ;
#17518=EDGE_LOOP ( 'NONE', ( #18409, #21807, #70706, #3177 ) ) ;
#17522=CYLINDRICAL_SURFACE ( 'NONE', #63353, 31.99999999999998579 ) ;
#17524=FACE_OUTER_BOUND ( 'NONE', #73466, .T. ) ;
#17528=LINE ( 'NONE', #11511, #36461 ) ;
#17541=EDGE_CURVE ( 'NONE', #67241, #51687, #46033, .T. ) ;
#17556=CARTESIAN_POINT ( 'NONE',  ( 0.000000000000000000, -51.29473840253177030, -63.97538442413482329 ) ) ;
#17564=ORIENTED_EDGE ( 'NONE', *, *, #13215, .T. ) ;
#17566=ORIENTED_EDGE ( 'NONE', *, *, #52866, .T. ) ;
#17569=AXIS2_PLACEMENT_3D ( 'NONE', #50865, #26817, #44117 ) ;
#17575=ORIENTED_EDGE ( 'NONE', *, *, #61828, .T. ) ;
#17592=ORIENTED_EDGE ( 'NONE', *, *, #23202, .T. ) ;
#17593=DIRECTION ( 'NONE',  ( 0.000000000000000000, -0.4067366430757908269, 0.9135454576426049744 ) ) ;
#17594=EDGE_CURVE ( 'NONE', #19214, #73443, #66327, .T. ) ;
#17599=FACE_OUTER_BOUND ( 'NONE', #56125, .T. ) ;
#17604=ORIENTED_EDGE ( 'NONE', *, *, #69501, .F. ) ;
#17613=ORIENTED_EDGE ( 'NONE', *, *, #70345, .T. ) ;
#17615=LINE ( 'NONE', #29249, #70904 ) ;
#17620=CARTESIAN_POINT ( 'NONE',  ( 11.99999999999999822, -75.11764819372145041, 29.05362095685286050 ) ) ;
#17622=CARTESIAN_POINT ( 'NONE',  ( 11.99999999999999822, 56.15606465355041621, -59.75363087400016582 ) ) ;
#17623=CYLINDRICAL_SURFACE ( 'NONE', #72288, 77.49899999999999523 ) ;
#17627=LINE ( 'NONE', #45479, #55361 ) ;
#17628=CARTESIAN_POINT ( 'NONE',  ( 11.99999999999999822, 59.03342792756328095, -46.54456581323744757 ) ) ;
#17635=EDGE_LOOP ( 'NONE', ( #43641, #6474, #62671, #8317 ) ) ;
#17638=CARTESIAN_POINT ( 'NONE',  ( 0.000000000000000000, 23.16143007188426850, 73.95703589263983702 ) ) ;
#17639=CARTESIAN_POINT ( 'NONE',  ( 11.99999999999999822, 51.02545421589324803, 55.20638768913779870 ) ) ;
#17654=ORIENTED_EDGE ( 'NONE', *, *, #24386, .F. ) ;
#17663=CYLINDRICAL_SURFACE ( 'NONE', #71310, 31.99999999999998579 ) ;
#17674=LINE ( 'NONE', #52254, #5725 ) ;
#17677=FACE_OUTER_BOUND ( 'NONE', #9469, .T. ) ;
#17678=ORIENTED_EDGE ( 'NONE', *, *, #62211, .F. ) ;
#17681=ORIENTED_EDGE ( 'NONE', *, *, #34531, .T. ) ;
#17683=CYLINDRICAL_SURFACE ( 'NONE', #32492, 77.49899999999999523 ) ;
#17687=ADVANCED_FACE ( 'NONE', ( #32819 ), #15917, .F. ) ;
#17698=DIRECTION ( 'NONE',  ( 1.000000000000000000, 0.000000000000000000, -0.000000000000000000 ) ) ;
#17700=CYLINDRICAL_SURFACE ( 'NONE', #40939, 77.49899999999999523 ) ;
#17701=CARTESIAN_POINT ( 'NONE',  ( 11.99999999999999822, 77.16300072079661732, 27.74655509720698277 ) ) ;
#17716=ORIENTED_EDGE ( 'NONE', *, *, #11865, .T. ) ;
#17724=DIRECTION ( 'NONE',  ( 0.000000000000000000, 0.000000000000000000, -1.000000000000000000 ) ) ;
#17744=DIRECTION ( 'NONE',  ( 0.000000000000000000, -0.5224985647159561264, 0.8526401643540878483 ) ) ;
#17755=ORIENTED_EDGE ( 'NONE', *, *, #59865, .F. ) ;
#17758=ADVANCED_FACE ( 'NONE', ( #16661 ), #73419, .F. ) ;
#17765=CARTESIAN_POINT ( 'NONE',  ( 11.99999999999999822, 0.000000000000000000, 0.000000000000000000 ) ) ;
#17771=DIRECTION ( 'NONE',  ( 0.000000000000000000, 0.9135454576426055295, 0.4067366430757899387 ) ) ;
#17779=LINE ( 'NONE', #46001, #13382 ) ;
#17787=CARTESIAN_POINT ( 'NONE',  ( 0.000000000000000000, -59.03342792756231461, -46.54456581323868392 ) ) ;
#17789=LINE ( 'NONE', #47124, #32579 ) ;
#17794=DIRECTION ( 'NONE',  ( -1.000000000000000000, -0.000000000000000000, 0.000000000000000000 ) ) ;
#17798=CARTESIAN_POINT ( 'NONE',  ( 11.99999999999999822, 68.55367621811204515, -44.99326035065983120 ) ) ;
#17800=EDGE_CURVE ( 'NONE', #29971, #47446, #50494, .T. ) ;
#17801=CIRCLE ( 'NONE', #22590, 31.99999999999998224 ) ;
#17803=EDGE_CURVE ( 'NONE', #10768, #57809, #32922, .T. ) ;
#17811=ORIENTED_EDGE ( 'NONE', *, *, #7025, .F. ) ;
#17815=EDGE_CURVE ( 'NONE', #37548, #4632, #29333, .T. ) ;
#17818=ORIENTED_EDGE ( 'NONE', *, *, #25911, .T. ) ;
#17820=ORIENTED_EDGE ( 'NONE', *, *, #6123, .F. ) ;
#17825=ORIENTED_EDGE ( 'NONE', *, *, #8586, .F. ) ;
#17831=ORIENTED_EDGE ( 'NONE', *, *, #45168, .T. ) ;
#17834=DIRECTION ( 'NONE',  ( -1.000000000000000000, 0.000000000000000000, 0.000000000000000000 ) ) ;
#17836=EDGE_CURVE ( 'NONE', #58803, #52520, #49714, .T. ) ;
#17847=CIRCLE ( 'NONE', #35871, 77.49899999999999523 ) ;
#17850=DIRECTION ( 'NONE',  ( -1.000000000000000000, 0.000000000000000000, -0.000000000000000000 ) ) ;
#17853=DIRECTION ( 'NONE',  ( 0.000000000000000000, 0.000000000000000000, 1.000000000000000000 ) ) ;
#17860=ORIENTED_EDGE ( 'NONE', *, *, #74106, .T. ) ;
#17866=ORIENTED_EDGE ( 'NONE', *, *, #16668, .T. ) ;
#17868=CARTESIAN_POINT ( 'NONE',  ( 11.99999999999999822, 23.16143007188530589, -73.95703589263951017 ) ) ;
#17871=LINE ( 'NONE', #52082, #22203 ) ;
#17874=DIRECTION ( 'NONE',  ( -1.000000000000000000, -0.000000000000000000, -0.000000000000000000 ) ) ;
#17879=EDGE_CURVE ( 'NONE', #38198, #25988, #58157, .T. ) ;
#17886=DIRECTION ( 'NONE',  ( -1.000000000000000000, 0.000000000000000000, 0.000000000000000000 ) ) ;
#17888=VECTOR ( 'NONE', #5254, 1000.000000000000000 ) ;
#17889=CARTESIAN_POINT ( 'NONE',  ( 11.99999999999999822, 68.26794271651262136, 31.47745569255165066 ) ) ;
#17893=DIRECTION ( 'NONE',  ( -1.000000000000000000, -0.000000000000000000, -0.000000000000000000 ) ) ;
#17896=CYLINDRICAL_SURFACE ( 'NONE', #30444, 31.99999999999998579 ) ;
#17899=FACE_OUTER_BOUND ( 'NONE', #7847, .T. ) ;
#17902=EDGE_CURVE ( 'NONE', #68616, #55213, #48549, .T. ) ;
#17906=EDGE_LOOP ( 'NONE', ( #51175, #56031, #72921, #17915 ) ) ;
#17907=ADVANCED_FACE ( 'NONE', ( #63651 ), #12853, .T. ) ;
#17915=ORIENTED_EDGE ( 'NONE', *, *, #68375, .T. ) ;
#17923=EDGE_LOOP ( 'NONE', ( #7855, #4616, #48390, #11288 ) ) ;
#17934=AXIS2_PLACEMENT_3D ( 'NONE', #55002, #71547, #65196 ) ;
#17939=VERTEX_POINT ( 'NONE', #24160 ) ;
#17940=ORIENTED_EDGE ( 'NONE', *, *, #51458, .F. ) ;
#17944=CARTESIAN_POINT ( 'NONE',  ( 15.00000000000000000, -10.45096189432344502, -21.10159698893425784 ) ) ;
#17959=DIRECTION ( 'NONE',  ( -1.000000000000000000, 0.000000000000000000, 0.000000000000000000 ) ) ;
#17960=DIRECTION ( 'NONE',  ( -1.000000000000000000, 0.000000000000000000, -0.000000000000000000 ) ) ;
#17962=DIRECTION ( 'NONE',  ( -1.000000000000000000, 0.000000000000000000, 0.000000000000000000 ) ) ;
#17964=AXIS2_PLACEMENT_3D ( 'NONE', #14539, #8904, #63032 ) ;
#17966=ORIENTED_EDGE ( 'NONE', *, *, #43968, .F. ) ;
#17968=FACE_BOUND ( 'NONE', #36519, .T. ) ;
#17972=CARTESIAN_POINT ( 'NONE',  ( 0.000000000000000000, 0.000000000000000000, 0.000000000000000000 ) ) ;
#17974=ORIENTED_EDGE ( 'NONE', *, *, #63035, .T. ) ;
#17978=CARTESIAN_POINT ( 'NONE',  ( 11.99999999999999822, 0.000000000000000000, 0.000000000000000000 ) ) ;
#17987=FACE_OUTER_BOUND ( 'NONE', #35152, .T. ) ;
#17989=DIRECTION ( 'NONE',  ( 0.000000000000000000, 0.9238795325112851842, 0.3826834323650938341 ) ) ;
#17999=AXIS2_PLACEMENT_3D ( 'NONE', #17183, #69061, #40116 ) ;
#18000=DIRECTION ( 'NONE',  ( 1.000000000000000000, 0.000000000000000000, 0.000000000000000000 ) ) ;
#18005=ADVANCED_FACE ( 'NONE', ( #65858 ), #30513, .T. ) ;
#18007=CARTESIAN_POINT ( 'NONE',  ( 11.99999999999999822, 35.91791733033476675, 68.67312586195008350 ) ) ;
#18013=VECTOR ( 'NONE', #40352, 1000.000000000000000 ) ;
#18015=ORIENTED_EDGE ( 'NONE', *, *, #31999, .T. ) ;
#18026=EDGE_LOOP ( 'NONE', ( #43464, #59454, #31055, #1335 ) ) ;
#18049=CYLINDRICAL_SURFACE ( 'NONE', #47719, 31.99999999999998579 ) ;
#18051=LINE ( 'NONE', #63926, #57082 ) ;
#18055=ORIENTED_EDGE ( 'NONE', *, *, #35237, .F. ) ;
#18061=ORIENTED_EDGE ( 'NONE', *, *, #20866, .F. ) ;
#18066=LINE ( 'NONE', #28593, #47610 ) ;
#18069=EDGE_CURVE ( 'NONE', #55521, #10549, #8948, .T. ) ;
#18073=AXIS2_PLACEMENT_3D ( 'NONE', #59853, #19243, #30883 ) ;
#18076=EDGE_CURVE ( 'NONE', #57242, #52714, #29377, .T. ) ;
#18079=ADVANCED_FACE ( 'NONE', ( #25991 ), #59851, .T. ) ;
#18081=DIRECTION ( 'NONE',  ( 0.000000000000000000, 0.000000000000000000, 1.000000000000000000 ) ) ;
#18086=ORIENTED_EDGE ( 'NONE', *, *, #50570, .T. ) ;
#18088=ADVANCED_FACE ( 'NONE', ( #31262 ), #33014, .T. ) ;
#18089=DIRECTION ( 'NONE',  ( 0.000000000000000000, 0.9969173337331276308, 0.07845909572784874608 ) ) ;
#18097=CARTESIAN_POINT ( 'NONE',  ( 11.99999999999999822, 0.000000000000000000, 0.000000000000000000 ) ) ;
#18098=EDGE_CURVE ( 'NONE', #38802, #42705, #48918, .T. ) ;
#18107=ORIENTED_EDGE ( 'NONE', *, *, #6731, .T. ) ;
#18122=VERTEX_POINT ( 'NONE', #4857 ) ;
#18131=LINE ( 'NONE', #64004, #6019 ) ;
#18132=ORIENTED_EDGE ( 'NONE', *, *, #70498, .F. ) ;
#18143=VERTEX_POINT ( 'NONE', #33766 ) ;
#18152=CARTESIAN_POINT ( 'NONE',  ( 15.00000000000000000, 16.83928648764945635, 16.46020748918027010 ) ) ;
#18154=EDGE_CURVE ( 'NONE', #42672, #32448, #59404, .T. ) ;
#18156=CARTESIAN_POINT ( 'NONE',  ( 0.000000000000000000, 68.26794271651262136, 31.47745569255165066 ) ) ;
#18162=EDGE_CURVE ( 'NONE', #37377, #232, #51802, .T. ) ;
#18175=AXIS2_PLACEMENT_3D ( 'NONE', #43518, #70553, #3297 ) ;
#18177=LINE ( 'NONE', #42234, #16503 ) ;
#18180=PRESENTATION_STYLE_ASSIGNMENT (( #52384 ) ) ;
#18181=VECTOR ( 'NONE', #73555, 1000.000000000000000 ) ;
#18186=DIRECTION ( 'NONE',  ( -1.000000000000000000, 0.000000000000000000, -0.000000000000000000 ) ) ;
#18188=DIRECTION ( 'NONE',  ( 0.000000000000000000, 0.000000000000000000, 1.000000000000000000 ) ) ;
#18189=PLANE ( 'NONE',  #10597 ) ;
#18192=ADVANCED_FACE ( 'NONE', ( #69461 ), #5965, .T. ) ;
#18197=ORIENTED_EDGE ( 'NONE', *, *, #29100, .F. ) ;
#18198=DIRECTION ( 'NONE',  ( 0.000000000000000000, 0.07845909572783797692, 0.9969173337331285190 ) ) ;
#18218=DIRECTION ( 'NONE',  ( 0.000000000000000000, 0.000000000000000000, 1.000000000000000000 ) ) ;
#18221=AXIS2_PLACEMENT_3D ( 'NONE', #45806, #33370, #68730 ) ;
#18233=EDGE_LOOP ( 'NONE', ( #20652, #2980, #73029, #35326 ) ) ;
#18242=CARTESIAN_POINT ( 'NONE',  ( 11.99999999999999822, 6.903761155838878061, -77.19088730480517313 ) ) ;
#18252=CARTESIAN_POINT ( 'NONE',  ( 0.000000000000000000, 0.000000000000000000, 0.000000000000000000 ) ) ;
#18256=AXIS2_PLACEMENT_3D ( 'NONE', #65421, #59772, #18787 ) ;
#18275=DIRECTION ( 'NONE',  ( 0.000000000000000000, 0.000000000000000000, -1.000000000000000000 ) ) ;
#18283=ORIENTED_EDGE ( 'NONE', *, *, #34360, .F. ) ;
#18299=ORIENTED_EDGE ( 'NONE', *, *, #33440, .F. ) ;
#18312=VERTEX_POINT ( 'NONE', #31076 ) ;
#18321=DIRECTION ( 'NONE',  ( -1.000000000000000000, -0.000000000000000000, -0.000000000000000000 ) ) ;
#18323=CARTESIAN_POINT ( 'NONE',  ( 15.00000000000000000, -18.13022148937263012, -15.02647892043543898 ) ) ;
#18326=ORIENTED_EDGE ( 'NONE', *, *, #69684, .T. ) ;
#18331=ORIENTED_EDGE ( 'NONE', *, *, #38217, .F. ) ;
#18339=EDGE_CURVE ( 'NONE', #45327, #24118, #52203, .T. ) ;
#18345=CARTESIAN_POINT ( 'NONE',  ( 11.99999999999999822, 75.11764819372142199, 2.946379043147685728 ) ) ;
#18350=EDGE_CURVE ( 'NONE', #36873, #27913, #43800, .T. ) ;
#18361=CARTESIAN_POINT ( 'NONE',  ( 5.999999999999999112, -21.60688246758642705, 79.10210256391358996 ) ) ;
#18369=VECTOR ( 'NONE', #1116, 1000.000000000000000 ) ;
#18372=ORIENTED_EDGE ( 'NONE', *, *, #48145, .T. ) ;
#18375=CARTESIAN_POINT ( 'NONE',  ( 15.00000000000000000, -10.45096189432314127, 21.10159698893440350 ) ) ;
#18384=DIRECTION ( 'NONE',  ( 0.000000000000000000, 0.9510565162951503115, -0.3090169943749573878 ) ) ;
#18392=ORIENTED_EDGE ( 'NONE', *, *, #6123, .T. ) ;
#18398=DIRECTION ( 'NONE',  ( 0.000000000000000000, 0.000000000000000000, 1.000000000000000000 ) ) ;
#18403=ORIENTED_EDGE ( 'NONE', *, *, #13483, .F. ) ;
#18409=ORIENTED_EDGE ( 'NONE', *, *, #59924, .T. ) ;
#18412=ORIENTED_EDGE ( 'NONE', *, *, #63922, .T. ) ;
#18419=DIRECTION ( 'NONE',  ( -1.000000000000000000, 0.000000000000000000, 0.000000000000000000 ) ) ;
#18421=LINE ( 'NONE', #31544, #52826 ) ;
#18426=EDGE_CURVE ( 'NONE', #42081, #15645, #57043, .T. ) ;
#18428=CARTESIAN_POINT ( 'NONE',  ( 0.000000000000000000, -59.03961581697367933, -46.53671651294010303 ) ) ;
#18435=CYLINDRICAL_SURFACE ( 'NONE', #21638, 82.00000000000000000 ) ;
#18437=CARTESIAN_POINT ( 'NONE',  ( 0.000000000000000000, -49.70050353004931054, 59.46389618801946142 ) ) ;
#18443=DIRECTION ( 'NONE',  ( 0.000000000000000000, -0.9510565162951510887, 0.3090169943749551673 ) ) ;
#18444=CIRCLE ( 'NONE', #69833, 77.49899999999999523 ) ;
#18458=AXIS2_PLACEMENT_3D ( 'NONE', #45032, #44282, #51394 ) ;
#18472=DIRECTION ( 'NONE',  ( 0.000000000000000000, 0.000000000000000000, 1.000000000000000000 ) ) ;
#18480=ORIENTED_EDGE ( 'NONE', *, *, #20763, .T. ) ;
#18486=VERTEX_POINT ( 'NONE', #20166 ) ;
#18496=CARTESIAN_POINT ( 'NONE',  ( 6.000000000000000000, 15.33399622253482697, 80.55351364060595643 ) ) ;
#18505=AXIS2_PLACEMENT_3D ( 'NONE', #25826, #71679, #15670 ) ;
#18512=DIRECTION ( 'NONE',  ( -1.000000000000000000, -0.000000000000000000, 0.000000000000000000 ) ) ;
#18513=PLANE ( 'NONE',  #56048 ) ;
#18518=EDGE_CURVE ( 'NONE', #2055, #8165, #55127, .T. ) ;
#18525=ADVANCED_FACE ( 'NONE', ( #37107 ), #32559, .T. ) ;
#18527=DIRECTION ( 'NONE',  ( -1.000000000000000000, 0.000000000000000000, 0.000000000000000000 ) ) ;
#18528=CARTESIAN_POINT ( 'NONE',  ( 0.000000000000000000, -81.90746397400386059, -3.894527615418766242 ) ) ;
#18529=DIRECTION ( 'NONE',  ( -1.000000000000000000, -0.000000000000000000, -0.000000000000000000 ) ) ;
#18530=CIRCLE ( 'NONE', #48520, 31.99999999999998934 ) ;
#18531=CYLINDRICAL_SURFACE ( 'NONE', #67265, 31.99999999999998579 ) ;
#18537=AXIS2_PLACEMENT_3D ( 'NONE', #385, #16898, #23281 ) ;
#18538=DIRECTION ( 'NONE',  ( 0.000000000000000000, 0.7431448254773862505, -0.6691306063588671194 ) ) ;
#18540=DIRECTION ( 'NONE',  ( 0.000000000000000000, -0.9135454576426055295, -0.4067366430757899942 ) ) ;
#18543=SHAPE_REPRESENTATION_RELATIONSHIP ( 'NONE' , 'NONE' ,  #36835, #58845 ) ;
#18548=AXIS2_PLACEMENT_3D ( 'NONE', #1995, #13959, #20354 ) ;
#18550=DIRECTION ( 'NONE',  ( -1.000000000000000000, 0.000000000000000000, -0.000000000000000000 ) ) ;
#18551=ORIENTED_EDGE ( 'NONE', *, *, #19439, .T. ) ;
#18561=ORIENTED_EDGE ( 'NONE', *, *, #60726, .T. ) ;
#18566=VERTEX_POINT ( 'NONE', #60055 ) ;
#18568=EDGE_CURVE ( 'NONE', #19673, #41269, #38588, .T. ) ;
#18572=VERTEX_POINT ( 'NONE', #33294 ) ;
#18579=ORIENTED_EDGE ( 'NONE', *, *, #49535, .T. ) ;
#18581=CARTESIAN_POINT ( 'NONE',  ( 11.99999999999999822, -35.91791733033525702, 68.67312586194982771 ) ) ;
#18583=CIRCLE ( 'NONE', #6582, 31.99999999999998934 ) ;
#18587=EDGE_CURVE ( 'NONE', #40037, #40781, #71443, .T. ) ;
#18594=LINE ( 'NONE', #59199, #50690 ) ;
#18601=DIRECTION ( 'NONE',  ( 0.000000000000000000, -0.8526401643540970632, 0.5224985647159410274 ) ) ;
#18602=AXIS2_PLACEMENT_3D ( 'NONE', #29142, #22031, #74274 ) ;
#18604=DIRECTION ( 'NONE',  ( 0.000000000000000000, -0.5877852522924689183, 0.8090169943749504489 ) ) ;
#18609=FACE_OUTER_BOUND ( 'NONE', #62239, .T. ) ;
#18612=ORIENTED_EDGE ( 'NONE', *, *, #54268, .T. ) ;
#18614=CARTESIAN_POINT ( 'NONE',  ( 0.000000000000000000, 0.000000000000000000, 0.000000000000000000 ) ) ;
#18618=EDGE_LOOP ( 'NONE', ( #66123, #19249, #6820, #38831 ) ) ;
#18626=DIRECTION ( 'NONE',  ( 0.000000000000000000, 0.3090169943749480064, -0.9510565162951534202 ) ) ;
#18629=DIRECTION ( 'NONE',  ( 0.000000000000000000, 0.3090169943749480064, -0.9510565162951534202 ) ) ;
#18631=AXIS2_PLACEMENT_3D ( 'NONE', #10928, #1177, #40992 ) ;
#18634=DIRECTION ( 'NONE',  ( 1.000000000000000000, 0.000000000000000000, 0.000000000000000000 ) ) ;
#18641=ORIENTED_EDGE ( 'NONE', *, *, #30393, .T. ) ;
#18663=VERTEX_POINT ( 'NONE', #73896 ) ;
#18665=ORIENTED_EDGE ( 'NONE', *, *, #22497, .T. ) ;
#18666=CARTESIAN_POINT ( 'NONE',  ( 0.000000000000000000, 59.03961581697465277, -46.53671651293886669 ) ) ;
#18673=ORIENTED_EDGE ( 'NONE', *, *, #41249, .F. ) ;
#18681=AXIS2_PLACEMENT_3D ( 'NONE', #10002, #47554, #63377 ) ;
#18686=CARTESIAN_POINT ( 'NONE',  ( 11.99999999999999822, 26.02418014898310261, 70.52718814184268581 ) ) ;
#18689=AXIS2_PLACEMENT_3D ( 'NONE', #10357, #16371, #33275 ) ;
#18690=ADVANCED_FACE ( 'NONE', ( #6243 ), #33679, .T. ) ;
#18697=DIRECTION ( 'NONE',  ( 0.000000000000000000, -0.9969173337331287410, 0.07845909572783489605 ) ) ;
#18704=ORIENTED_EDGE ( 'NONE', *, *, #36170, .T. ) ;
#18706=VERTEX_POINT ( 'NONE', #5133 ) ;
#18718=CARTESIAN_POINT ( 'NONE',  ( 0.000000000000000000, 79.10210256391398786, -21.60688246758504505 ) ) ;
#18719=CARTESIAN_POINT ( 'NONE',  ( 11.99999999999999822, 55.20638768913831029, -51.02545421589267960 ) ) ;
#18727=EDGE_CURVE ( 'NONE', #53818, #359, #45085, .T. ) ;
#18729=FACE_OUTER_BOUND ( 'NONE', #52922, .T. ) ;
#18731=AXIS2_PLACEMENT_3D ( 'NONE', #51625, #23068, #1285 ) ;
#18747=EDGE_CURVE ( 'NONE', #32813, #21432, #17871, .T. ) ;
#18750=ORIENTED_EDGE ( 'NONE', *, *, #50263, .T. ) ;
#18751=DIRECTION ( 'NONE',  ( -1.000000000000000000, 0.000000000000000000, 0.000000000000000000 ) ) ;
#18756=CARTESIAN_POINT ( 'NONE',  ( 0.000000000000000000, 20.40083707022882820, 72.35432306680490910 ) ) ;
#18758=CARTESIAN_POINT ( 'NONE',  ( 11.99999999999999822, 70.53064760720316428, -26.01480285779861035 ) ) ;
#18762=EDGE_LOOP ( 'NONE', ( #60773, #52325, #48265, #64449 ) ) ;
#18766=ORIENTED_EDGE ( 'NONE', *, *, #14958, .F. ) ;
#18767=VERTEX_POINT ( 'NONE', #64857 ) ;
#18773=LINE ( 'NONE', #41713, #35441 ) ;
#18777=PLANE ( 'NONE',  #14468 ) ;
#18784=DIRECTION ( 'NONE',  ( -1.000000000000000000, 0.000000000000000000, -0.000000000000000000 ) ) ;
#18787=DIRECTION ( 'NONE',  ( 0.000000000000000000, 0.000000000000000000, -1.000000000000000000 ) ) ;
#18796=AXIS2_PLACEMENT_3D ( 'NONE', #2911, #26539, #49472 ) ;
#18797=CARTESIAN_POINT ( 'NONE',  ( 11.99999999999999822, -46.21855187248585395, -62.20884554314068993 ) ) ;
#18800=ADVANCED_FACE ( 'NONE', ( #36272 ), #13337, .F. ) ;
#18811=FACE_OUTER_BOUND ( 'NONE', #15537, .T. ) ;
#18814=AXIS2_PLACEMENT_3D ( 'NONE', #65572, #48268, #31702 ) ;
#18818=CARTESIAN_POINT ( 'NONE',  ( 0.000000000000000000, -69.42325613327466272, 34.44570377933573724 ) ) ;
#18824=AXIS2_PLACEMENT_3D ( 'NONE', #3858, #50437, #42963 ) ;
#18826=ORIENTED_EDGE ( 'NONE', *, *, #71341, .T. ) ;
#18832=EDGE_CURVE ( 'NONE', #11001, #70989, #58102, .T. ) ;
#18836=CIRCLE ( 'NONE', #48849, 31.99999999999998934 ) ;
#18844=LINE ( 'NONE', #25247, #38819 ) ;
#18847=CARTESIAN_POINT ( 'NONE',  ( 0.000000000000000000, 0.000000000000000000, 0.000000000000000000 ) ) ;
#18854=VERTEX_POINT ( 'NONE', #42300 ) ;
#18856=EDGE_CURVE ( 'NONE', #10445, #24628, #15005, .T. ) ;
#18857=ORIENTED_EDGE ( 'NONE', *, *, #41544, .F. ) ;
#18859=VERTEX_POINT ( 'NONE', #7343 ) ;
#18863=AXIS2_PLACEMENT_3D ( 'NONE', #43918, #66838, #15322 ) ;
#18874=ORIENTED_EDGE ( 'NONE', *, *, #24472, .T. ) ;
#18884=CARTESIAN_POINT ( 'NONE',  ( 11.99999999999999822, 56.15606465354957777, 59.75363087400094031 ) ) ;
#18886=ORIENTED_EDGE ( 'NONE', *, *, #59252, .T. ) ;
#18890=CARTESIAN_POINT ( 'NONE',  ( 11.99999999999999822, 75.54627589209970040, -17.28742895386005785 ) ) ;
#18891=DIRECTION ( 'NONE',  ( -1.000000000000000000, -0.000000000000000000, -0.000000000000000000 ) ) ;
#18894=AXIS2_PLACEMENT_3D ( 'NONE', #53666, #2204, #56264 ) ;
#18895=ORIENTED_EDGE ( 'NONE', *, *, #14922, .T. ) ;
#18896=DIRECTION ( 'NONE',  ( 0.000000000000000000, 0.000000000000000000, 1.000000000000000000 ) ) ;
#18899=EDGE_CURVE ( 'NONE', #2154, #19352, #46140, .T. ) ;
#18902=DIRECTION ( 'NONE',  ( 0.000000000000000000, -0.9510565162951543083, -0.3090169943749448977 ) ) ;
#18909=FACE_OUTER_BOUND ( 'NONE', #67697, .T. ) ;
#18913=EDGE_CURVE ( 'NONE', #26714, #10762, #40288, .T. ) ;
#18915=DIRECTION ( 'NONE',  ( -1.000000000000000000, 0.000000000000000000, 0.000000000000000000 ) ) ;
#18918=CARTESIAN_POINT ( 'NONE',  ( -10.00000000000000000, 0.000000000000000000, 0.000000000000000000 ) ) ;
#18929=PLANE ( 'NONE',  #45471 ) ;
#18933=ORIENTED_EDGE ( 'NONE', *, *, #42762, .F. ) ;
#18936=EDGE_LOOP ( 'NONE', ( #158, #8047, #50016, #58200 ) ) ;
#18945=ORIENTED_EDGE ( 'NONE', *, *, #48790, .F. ) ;
#18947=CARTESIAN_POINT ( 'NONE',  ( 0.000000000000000000, 0.000000000000000000, 0.000000000000000000 ) ) ;
#18948=EDGE_LOOP ( 'NONE', ( #30388, #71278, #47600, #37175 ) ) ;
#18951=VECTOR ( 'NONE', #31741, 1000.000000000000000 ) ;
#18968=CARTESIAN_POINT ( 'NONE',  ( 15.00000000000000000, -10.45096189432314127, 21.10159698893440350 ) ) ;
#18971=CARTESIAN_POINT ( 'NONE',  ( 11.99999999999999822, 34.94270380257639630, 74.18225833017902460 ) ) ;
#18977=CARTESIAN_POINT ( 'NONE',  ( 15.00000000000000000, 5.835314593368470248, -22.81335362449854642 ) ) ;
#18984=EDGE_CURVE ( 'NONE', #63724, #24340, #7867, .T. ) ;
#18993=CARTESIAN_POINT ( 'NONE',  ( 11.99999999999999822, -75.11764819372145041, -2.946379043147127064 ) ) ;
#19001=CIRCLE ( 'NONE', #25017, 31.99999999999998934 ) ;
#19010=CIRCLE ( 'NONE', #63475, 82.00000000000000000 ) ;
#19048=FACE_OUTER_BOUND ( 'NONE', #12197, .T. ) ;
#19051=VERTEX_POINT ( 'NONE', #51628 ) ;
#19053=AXIS2_PLACEMENT_3D ( 'NONE', #38493, #27187, #61432 ) ;
#19060=CARTESIAN_POINT ( 'NONE',  ( 11.99999999999999822, 0.000000000000000000, 0.000000000000000000 ) ) ;
#19074=ORIENTED_EDGE ( 'NONE', *, *, #44736, .F. ) ;
#19085=DIRECTION ( 'NONE',  ( 0.000000000000000000, 0.7604059656000322631, -0.6494480483301821039 ) ) ;
#19095=CIRCLE ( 'NONE', #46682, 77.49899999999999523 ) ;
#19104=EDGE_CURVE ( 'NONE', #54754, #7371, #11459, .T. ) ;
#19107=CARTESIAN_POINT ( 'NONE',  ( 15.00000000000000000, -23.29833615347104470, 3.418703333116808629 ) ) ;
#19111=CIRCLE ( 'NONE', #66099, 31.99999999999998579 ) ;
#19117=CIRCLE ( 'NONE', #35917, 82.00000000000000000 ) ;
#19118=ORIENTED_EDGE ( 'NONE', *, *, #20949, .F. ) ;
#19119=ORIENTED_EDGE ( 'NONE', *, *, #10951, .F. ) ;
#19120=DIRECTION ( 'NONE',  ( -1.000000000000000000, -0.000000000000000000, -0.000000000000000000 ) ) ;
#19121=ORIENTED_EDGE ( 'NONE', *, *, #20303, .F. ) ;
#19133=DIRECTION ( 'NONE',  ( -1.000000000000000000, -0.000000000000000000, -0.000000000000000000 ) ) ;
#19134=CIRCLE ( 'NONE', #7184, 82.00000000000000000 ) ;
#19139=AXIS2_PLACEMENT_3D ( 'NONE', #3053, #72897, #4523 ) ;
#19151=ORIENTED_EDGE ( 'NONE', *, *, #18587, .T. ) ;
#19152=EDGE_LOOP ( 'NONE', ( #32799, #27186, #16942, #65820 ) ) ;
#19168=CARTESIAN_POINT ( 'NONE',  ( 0.000000000000000000, -23.16143007188376757, -73.95703589263997912 ) ) ;
#19169=AXIS2_PLACEMENT_3D ( 'NONE', #72328, #3934, #20826 ) ;
#19170=EDGE_CURVE ( 'NONE', #237, #61251, #36685, .T. ) ;
#19172=DIRECTION ( 'NONE',  ( 0.000000000000000000, 0.000000000000000000, 1.000000000000000000 ) ) ;
#19183=DIRECTION ( 'NONE',  ( -1.000000000000000000, -0.000000000000000000, -0.000000000000000000 ) ) ;
#19188=CIRCLE ( 'NONE', #16840, 31.99999999999999289 ) ;
#19191=DIRECTION ( 'NONE',  ( 0.000000000000000000, 0.000000000000000000, -1.000000000000000000 ) ) ;
#19197=CARTESIAN_POINT ( 'NONE',  ( 11.99999999999999822, 55.16347631943042984, 60.67117009219156643 ) ) ;
#19208=AXIS2_PLACEMENT_3D ( 'NONE', #17375, #62523, #10618 ) ;
#19213=CIRCLE ( 'NONE', #37221, 82.00000000000000000 ) ;
#19214=VERTEX_POINT ( 'NONE', #24174 ) ;
#19222=EDGE_LOOP ( 'NONE', ( #44710, #66706, #14043, #53446 ) ) ;
#19235=DIRECTION ( 'NONE',  ( -1.000000000000000000, 0.000000000000000000, 0.000000000000000000 ) ) ;
#19242=EDGE_CURVE ( 'NONE', #18486, #64128, #52739, .T. ) ;
#19243=DIRECTION ( 'NONE',  ( -1.000000000000000000, -0.000000000000000000, -0.000000000000000000 ) ) ;
#19247=EDGE_CURVE ( 'NONE', #34378, #28286, #58374, .T. ) ;
#19249=ORIENTED_EDGE ( 'NONE', *, *, #68606, .T. ) ;
#19256=DIRECTION ( 'NONE',  ( -1.000000000000000000, 0.000000000000000000, -0.000000000000000000 ) ) ;
#19260=DIRECTION ( 'NONE',  ( 0.000000000000000000, 0.000000000000000000, 1.000000000000000000 ) ) ;
#19262=ORIENTED_EDGE ( 'NONE', *, *, #18832, .F. ) ;
#19266=LINE ( 'NONE', #65154, #71611 ) ;
#19270=DIRECTION ( 'NONE',  ( 0.000000000000000000, -0.3826834323650774583, -0.9238795325112919565 ) ) ;
#19273=ORIENTED_EDGE ( 'NONE', *, *, #65187, .T. ) ;
#19276=AXIS2_PLACEMENT_3D ( 'NONE', #51741, #11508, #5161 ) ;
#19297=AXIS2_PLACEMENT_3D ( 'NONE', #69545, #35337, #18398 ) ;
#19315=CARTESIAN_POINT ( 'NONE',  ( -10.00000000000000000, 0.000000000000000000, 0.000000000000000000 ) ) ;
#19316=ORIENTED_EDGE ( 'NONE', *, *, #58131, .F. ) ;
#19319=CIRCLE ( 'NONE', #73296, 77.49899999999999523 ) ;
#19321=CARTESIAN_POINT ( 'NONE',  ( 11.99999999999999822, 81.34940948281349904, -10.30890764327296161 ) ) ;
#19323=ORIENTED_EDGE ( 'NONE', *, *, #19872, .T. ) ;
#19325=FACE_OUTER_BOUND ( 'NONE', #7219, .T. ) ;
#19326=DIRECTION ( 'NONE',  ( 0.000000000000000000, 0.000000000000000000, 1.000000000000000000 ) ) ;
#19343=AXIS2_PLACEMENT_3D ( 'NONE', #30359, #35276, #53305 ) ;
#19348=AXIS2_PLACEMENT_3D ( 'NONE', #52629, #1181, #24080 ) ;
#19350=ORIENTED_EDGE ( 'NONE', *, *, #57531, .F. ) ;
#19351=AXIS2_PLACEMENT_3D ( 'NONE', #2198, #73439, #63296 ) ;
#19352=VERTEX_POINT ( 'NONE', #12136 ) ;
#19355=CARTESIAN_POINT ( 'NONE',  ( 11.99999999999999822, -41.19522573413780009, 65.64334221924896440 ) ) ;
#19361=CIRCLE ( 'NONE', #4997, 31.99999999999998579 ) ;
#19366=DIRECTION ( 'NONE',  ( 1.000000000000000000, -0.000000000000000000, 0.000000000000000000 ) ) ;
#19373=EDGE_CURVE ( 'NONE', #61374, #73431, #23795, .T. ) ;
#19379=DIRECTION ( 'NONE',  ( -1.000000000000000000, -0.000000000000000000, -0.000000000000000000 ) ) ;
#19380=VECTOR ( 'NONE', #68088, 1000.000000000000000 ) ;
#19388=PRESENTATION_STYLE_ASSIGNMENT (( #25413 ) ) ;
#19389=ORIENTED_EDGE ( 'NONE', *, *, #2828, .F. ) ;
#19390=ORIENTED_EDGE ( 'NONE', *, *, #73574, .F. ) ;
#19395=CIRCLE ( 'NONE', #24203, 31.99999999999998579 ) ;
#19406=VERTEX_POINT ( 'NONE', #33827 ) ;
#19408=ORIENTED_EDGE ( 'NONE', *, *, #63107, .T. ) ;
#19419=ORIENTED_EDGE ( 'NONE', *, *, #544, .F. ) ;
#19421=VERTEX_POINT ( 'NONE', #51485 ) ;
#19427=EDGE_CURVE ( 'NONE', #19829, #35960, #73665, .T. ) ;
#19434=EDGE_LOOP ( 'NONE', ( #73105, #4030, #2643, #30954 ) ) ;
#19439=EDGE_CURVE ( 'NONE', #6126, #6388, #69161, .T. ) ;
#19443=VERTEX_POINT ( 'NONE', #16533 ) ;
#19447=ORIENTED_EDGE ( 'NONE', *, *, #26738, .F. ) ;
#19475=CARTESIAN_POINT ( 'NONE',  ( 6.000000000000000000, 78.73519480814985627, -22.90783923731547489 ) ) ;
#19479=EDGE_LOOP ( 'NONE', ( #73778, #12108, #9920, #68868 ) ) ;
#19485=FACE_OUTER_BOUND ( 'NONE', #60642, .T. ) ;
#19486=ORIENTED_EDGE ( 'NONE', *, *, #42475, .F. ) ;
#19490=DIRECTION ( 'NONE',  ( -1.000000000000000000, -0.000000000000000000, 0.000000000000000000 ) ) ;
#19493=ORIENTED_EDGE ( 'NONE', *, *, #48397, .T. ) ;
#19497=DIRECTION ( 'NONE',  ( 0.000000000000000000, 0.9876883405951371042, 0.1564344650402346715 ) ) ;
#19499=DIRECTION ( 'NONE',  ( 0.000000000000000000, 0.000000000000000000, -1.000000000000000000 ) ) ;
#19521=CARTESIAN_POINT ( 'NONE',  ( 12.00000000000000000, -19.89357724624986545, 12.59942793731086219 ) ) ;
#19524=ORIENTED_EDGE ( 'NONE', *, *, #54561, .T. ) ;
#19526=DIRECTION ( 'NONE',  ( 0.000000000000000000, 0.9238795325112877377, -0.3826834323650873948 ) ) ;
#19532=CARTESIAN_POINT ( 'NONE',  ( 11.99999999999999822, 0.000000000000000000, 0.000000000000000000 ) ) ;
#19546=FACE_OUTER_BOUND ( 'NONE', #68857, .T. ) ;
#19556=CYLINDRICAL_SURFACE ( 'NONE', #68238, 31.99999999999998579 ) ;
#19560=ORIENTED_EDGE ( 'NONE', *, *, #8990, .F. ) ;
#19565=VERTEX_POINT ( 'NONE', #18375 ) ;
#19567=DIRECTION ( 'NONE',  ( 0.000000000000000000, -0.8526401643540860720, -0.5224985647159589019 ) ) ;
#19601=AXIS2_PLACEMENT_3D ( 'NONE', #20291, #25566, #72163 ) ;
#19604=VERTEX_POINT ( 'NONE', #48072 ) ;
#19614=EDGE_CURVE ( 'NONE', #25706, #57093, #1513, .T. ) ;
#19620=DIRECTION ( 'NONE',  ( -1.000000000000000000, 0.000000000000000000, -0.000000000000000000 ) ) ;
#19622=LINE ( 'NONE', #42568, #62069 ) ;
#19626=DIRECTION ( 'NONE',  ( 0.000000000000000000, 0.9945218953682730678, -0.1045284632676570791 ) ) ;
#19628=EDGE_CURVE ( 'NONE', #6829, #53064, #7479, .T. ) ;
#19632=LINE ( 'NONE', #58764, #73486 ) ;
#19633=CARTESIAN_POINT ( 'NONE',  ( 0.000000000000000000, 0.000000000000000000, 0.000000000000000000 ) ) ;
#19637=CARTESIAN_POINT ( 'NONE',  ( 6.000000000000000000, 81.90746397400393164, -3.894527615416979671 ) ) ;
#19638=EDGE_LOOP ( 'NONE', ( #23840, #17287, #5548, #29777 ) ) ;
#19642=AXIS2_PLACEMENT_3D ( 'NONE', #21239, #39303, #34019 ) ;
#19656=DIRECTION ( 'NONE',  ( 0.000000000000000000, 0.000000000000000000, 1.000000000000000000 ) ) ;
#19657=DIRECTION ( 'NONE',  ( 1.000000000000000000, 0.000000000000000000, 0.000000000000000000 ) ) ;
#19665=DIRECTION ( 'NONE',  ( -1.000000000000000000, -0.000000000000000000, -0.000000000000000000 ) ) ;
#19667=VERTEX_POINT ( 'NONE', #48433 ) ;
#19673=VERTEX_POINT ( 'NONE', #26234 ) ;
#19674=EDGE_CURVE ( 'NONE', #8287, #54048, #13757, .T. ) ;
#19676=ORIENTED_EDGE ( 'NONE', *, *, #21569, .F. ) ;
#19684=FACE_OUTER_BOUND ( 'NONE', #39852, .T. ) ;
#19705=ORIENTED_EDGE ( 'NONE', *, *, #51579, .F. ) ;
#19708=CARTESIAN_POINT ( 'NONE',  ( 11.99999999999999822, 0.000000000000000000, 0.000000000000000000 ) ) ;
#19718=ORIENTED_EDGE ( 'NONE', *, *, #54636, .T. ) ;
#19721=CARTESIAN_POINT ( 'NONE',  ( 11.99999999999999822, -59.03342792756297541, 46.54456581323783126 ) ) ;
#19722=DIRECTION ( 'NONE',  ( -1.000000000000000000, 0.000000000000000000, 0.000000000000000000 ) ) ;
#19729=DIRECTION ( 'NONE',  ( -1.000000000000000000, 0.000000000000000000, 0.000000000000000000 ) ) ;
#19735=DIRECTION ( 'NONE',  ( 1.000000000000000000, 0.000000000000000000, 0.000000000000000000 ) ) ;
#19736=CARTESIAN_POINT ( 'NONE',  ( 15.00000000000000000, -20.55727247249748402, -16.78983467731284307 ) ) ;
#19738=ADVANCED_FACE ( 'NONE', ( #65732 ), #13836, .T. ) ;
#19739=CIRCLE ( 'NONE', #71345, 82.00000000000000000 ) ;
#19756=ORIENTED_EDGE ( 'NONE', *, *, #66552, .T. ) ;
#19759=CARTESIAN_POINT ( 'NONE',  ( 11.99999999999999822, 21.60688246758586573, 79.10210256391376049 ) ) ;
#19760=CIRCLE ( 'NONE', #46235, 31.99999999999998934 ) ;
#19784=ADVANCED_FACE ( 'NONE', ( #2621 ), #9696, .T. ) ;
#19799=DIRECTION ( 'NONE',  ( 0.000000000000000000, -0.2334453638559126354, 0.9723699203976748917 ) ) ;
#19800=CARTESIAN_POINT ( 'NONE',  ( 11.99999999999999822, 28.89263327155746097, 71.91182617369197771 ) ) ;
#19802=ORIENTED_EDGE ( 'NONE', *, *, #43564, .T. ) ;
#19808=EDGE_LOOP ( 'NONE', ( #22587, #72818, #20330, #53340 ) ) ;
#19820=CARTESIAN_POINT ( 'NONE',  ( 11.99999999999999822, -71.27951684758005513, -30.41916302227188851 ) ) ;
#19827=AXIS2_PLACEMENT_3D ( 'NONE', #3654, #43865, #15657 ) ;
#19829=VERTEX_POINT ( 'NONE', #55770 ) ;
#19832=EDGE_CURVE ( 'NONE', #11576, #51303, #22199, .T. ) ;
#19833=CIRCLE ( 'NONE', #49832, 77.49899999999999523 ) ;
#19834=ADVANCED_FACE ( 'NONE', ( #67793 ), #27933, .T. ) ;
#19837=ORIENTED_EDGE ( 'NONE', *, *, #51335, .T. ) ;
#19846=CARTESIAN_POINT ( 'NONE',  ( 5.999999999999999112, -51.29473840253269401, 63.97538442413407012 ) ) ;
#19855=CARTESIAN_POINT ( 'NONE',  ( 11.99999999999999822, 0.000000000000000000, 0.000000000000000000 ) ) ;
#19859=VERTEX_POINT ( 'NONE', #43763 ) ;
#19862=ORIENTED_EDGE ( 'NONE', *, *, #50475, .F. ) ;
#19866=ORIENTED_EDGE ( 'NONE', *, *, #13725, .T. ) ;
#19872=EDGE_CURVE ( 'NONE', #72308, #67235, #42597, .T. ) ;
#19879=AXIS2_PLACEMENT_3D ( 'NONE', #26834, #72330, #65596 ) ;
#19881=DIRECTION ( 'NONE',  ( 0.000000000000000000, 0.3826834323650841752, 0.9238795325112891810 ) ) ;
#19884=EDGE_LOOP ( 'NONE', ( #51714, #23664, #38298, #16293 ) ) ;
#19889=DIRECTION ( 'NONE',  ( 0.000000000000000000, 0.000000000000000000, -1.000000000000000000 ) ) ;
#19895=CARTESIAN_POINT ( 'NONE',  ( -10.00000000000000000, 0.000000000000000000, 0.000000000000000000 ) ) ;
#19903=DIRECTION ( 'NONE',  ( 0.000000000000000000, 0.000000000000000000, 1.000000000000000000 ) ) ;
#19927=AXIS2_PLACEMENT_3D ( 'NONE', #62571, #15937, #45651 ) ;
#19931=DIRECTION ( 'NONE',  ( -1.000000000000000000, 0.000000000000000000, -0.000000000000000000 ) ) ;
#19937=CARTESIAN_POINT ( 'NONE',  ( 11.99999999999999822, 14.67089635893819377, -73.72996012237423713 ) ) ;
#19938=FACE_OUTER_BOUND ( 'NONE', #12680, .T. ) ;
#19944=VERTEX_POINT ( 'NONE', #52340 ) ;
#19945=DIRECTION ( 'NONE',  ( 0.000000000000000000, -0.9238795325112821866, -0.3826834323651006065 ) ) ;
#19953=CARTESIAN_POINT ( 'NONE',  ( 0.000000000000000000, 70.52718814184294160, -26.02418014898236720 ) ) ;
#19954=ORIENTED_EDGE ( 'NONE', *, *, #57680, .F. ) ;
#19960=ORIENTED_EDGE ( 'NONE', *, *, #26993, .T. ) ;
#19962=AXIS2_PLACEMENT_3D ( 'NONE', #68470, #817, #24091 ) ;
#19963=VERTEX_POINT ( 'NONE', #51233 ) ;
#19971=VERTEX_POINT ( 'NONE', #162 ) ;
#19975=ORIENTED_EDGE ( 'NONE', *, *, #73518, .F. ) ;
#19991=DIRECTION ( 'NONE',  ( 1.000000000000000000, -0.000000000000000000, -0.000000000000000000 ) ) ;
#20005=EDGE_CURVE ( 'NONE', #53485, #68824, #26863, .T. ) ;
#20006=FACE_OUTER_BOUND ( 'NONE', #54380, .T. ) ;
#20011=CARTESIAN_POINT ( 'NONE',  ( 11.99999999999999822, 67.80270845531889279, 46.11716303203210288 ) ) ;
#20015=CARTESIAN_POINT ( 'NONE',  ( 11.99999999999999822, 34.44570377933693806, -69.42325613327405165 ) ) ;
#20020=DIRECTION ( 'NONE',  ( 0.000000000000000000, 0.000000000000000000, 1.000000000000000000 ) ) ;
#20039=ORIENTED_EDGE ( 'NONE', *, *, #10496, .T. ) ;
#20042=EDGE_CURVE ( 'NONE', #62534, #64128, #23289, .T. ) ;
#20046=EDGE_LOOP ( 'NONE', ( #39010, #28819, #47071, #51243 ) ) ;
#20055=ORIENTED_EDGE ( 'NONE', *, *, #54491, .T. ) ;
#20061=CARTESIAN_POINT ( 'NONE',  ( 11.99999999999999822, -41.76937507738831812, 62.50329211542423025 ) ) ;
#20066=PLANE ( 'NONE',  #25064 ) ;
#20075=AXIS2_PLACEMENT_3D ( 'NONE', #39491, #33837, #27821 ) ;
#20076=FACE_OUTER_BOUND ( 'NONE', #5604, .T. ) ;
#20077=LINE ( 'NONE', #26464, #52290 ) ;
#20078=CARTESIAN_POINT ( 'NONE',  ( 0.000000000000000000, -77.19088730480518734, -6.903761155838607166 ) ) ;
#20080=AXIS2_PLACEMENT_3D ( 'NONE', #33097, #57171, #40612 ) ;
#20097=EDGE_CURVE ( 'NONE', #55952, #17105, #65314, .T. ) ;
#20098=FACE_OUTER_BOUND ( 'NONE', #41114, .T. ) ;
#20104=LINE ( 'NONE', #54699, #32901 ) ;
#20120=VERTEX_POINT ( 'NONE', #1633 ) ;
#20121=ADVANCED_FACE ( 'NONE', ( #15352 ), #36162, .F. ) ;
#20125=ORIENTED_EDGE ( 'NONE', *, *, #39907, .T. ) ;
#20127=CARTESIAN_POINT ( 'NONE',  ( 11.99999999999999822, 34.44570377933598593, 69.42325613327452061 ) ) ;
#20133=CARTESIAN_POINT ( 'NONE',  ( 0.000000000000000000, -77.49459641780886443, 0.8261519478428549501 ) ) ;
#20142=ORIENTED_EDGE ( 'NONE', *, *, #51109, .F. ) ;
#20162=VERTEX_POINT ( 'NONE', #9722 ) ;
#20165=DIRECTION ( 'NONE',  ( -1.000000000000000000, 0.000000000000000000, 0.000000000000000000 ) ) ;
#20166=CARTESIAN_POINT ( 'NONE',  ( 11.99999999999999822, -71.91182617369167929, -28.89263327155821059 ) ) ;
#20168=ORIENTED_EDGE ( 'NONE', *, *, #26603, .T. ) ;
#20169=CYLINDRICAL_SURFACE ( 'NONE', #57939, 31.99999999999998579 ) ;
#20170=DIRECTION ( 'NONE',  ( 0.000000000000000000, 0.000000000000000000, 1.000000000000000000 ) ) ;
#20180=AXIS2_PLACEMENT_3D ( 'NONE', #3997, #72389, #67878 ) ;
#20188=CARTESIAN_POINT ( 'NONE',  ( 0.000000000000000000, 74.18225833017888249, 34.94270380257665209 ) ) ;
#20192=DIRECTION ( 'NONE',  ( 0.000000000000000000, -0.2334453638558922628, -0.9723699203976798877 ) ) ;
#20195=DIRECTION ( 'NONE',  ( 0.000000000000000000, -0.9238795325112906243, 0.3826834323650805114 ) ) ;
#20210=DIRECTION ( 'NONE',  ( -1.000000000000000000, -0.000000000000000000, -0.000000000000000000 ) ) ;
#20216=ORIENTED_EDGE ( 'NONE', *, *, #32001, .T. ) ;
#20217=LINE ( 'NONE', #19846, #66807 ) ;
#20223=DIRECTION ( 'NONE',  ( 0.000000000000000000, 0.000000000000000000, 1.000000000000000000 ) ) ;
#20227=ORIENTED_EDGE ( 'NONE', *, *, #9436, .F. ) ;
#20234=EDGE_LOOP ( 'NONE', ( #13127, #36802, #48068, #39684 ) ) ;
#20235=DIRECTION ( 'NONE',  ( 1.000000000000000000, 0.000000000000000000, 0.000000000000000000 ) ) ;
#20240=LINE ( 'NONE', #31897, #28474 ) ;
#20241=EDGE_LOOP ( 'NONE', ( #26191, #25286, #61665, #42842 ) ) ;
#20248=CIRCLE ( 'NONE', #22699, 31.99999999999998579 ) ;
#20251=VERTEX_POINT ( 'NONE', #17221 ) ;
#20257=LINE ( 'NONE', #39336, #56566 ) ;
#20258=EDGE_CURVE ( 'NONE', #47563, #24844, #10066, .T. ) ;
#20266=STYLED_ITEM ( 'NONE', ( #19388 ), #37031 ) ;
#20273=CARTESIAN_POINT ( 'NONE',  ( 11.99999999999999822, -31.46837873495025306, 68.27212725128265447 ) ) ;
#20290=ADVANCED_FACE ( 'NONE', ( #51058 ), #62362, .F. ) ;
#20291=CARTESIAN_POINT ( 'NONE',  ( 0.000000000000000000, -68.27212725128298132, 31.46837873494953541 ) ) ;
#20303=EDGE_CURVE ( 'NONE', #35138, #33465, #35249, .T. ) ;
#20311=CIRCLE ( 'NONE', #52677, 31.99999999999999289 ) ;
#20324=ORIENTED_EDGE ( 'NONE', *, *, #26540, .T. ) ;
#20330=ORIENTED_EDGE ( 'NONE', *, *, #6247, .F. ) ;
#20333=VERTEX_POINT ( 'NONE', #61603 ) ;
#20335=CARTESIAN_POINT ( 'NONE',  ( 15.00000000000000000, 23.59884966291538078, 12.14883922797231008 ) ) ;
#20337=CARTESIAN_POINT ( 'NONE',  ( 0.000000000000000000, 49.70050353004975818, -59.46389618801909904 ) ) ;
#20339=DIRECTION ( 'NONE',  ( 0.000000000000000000, -0.7071067811865389130, -0.7071067811865562325 ) ) ;
#20352=ADVANCED_FACE ( 'NONE', ( #38673 ), #73239, .T. ) ;
#20353=ORIENTED_EDGE ( 'NONE', *, *, #28244, .T. ) ;
#20354=DIRECTION ( 'NONE',  ( 0.000000000000000000, -6.982962677686266711E-15, 1.000000000000000000 ) ) ;
#20356=EDGE_CURVE ( 'NONE', #36497, #45028, #50853, .T. ) ;
#20360=EDGE_CURVE ( 'NONE', #3632, #12392, #50304, .T. ) ;
#20368=FACE_OUTER_BOUND ( 'NONE', #73986, .T. ) ;
#20376=CARTESIAN_POINT ( 'NONE',  ( 15.00000000000000000, -0.9646360437375368635, -23.52805723605589705 ) ) ;
#20377=VERTEX_POINT ( 'NONE', #4856 ) ;
#20379=CIRCLE ( 'NONE', #17964, 31.99999999999998579 ) ;
#20385=DIRECTION ( 'NONE',  ( 1.000000000000000000, 0.000000000000000000, 0.000000000000000000 ) ) ;
#20396=ADVANCED_FACE ( 'NONE', ( #30703 ), #29225, .T. ) ;
#20397=DIRECTION ( 'NONE',  ( -1.000000000000000000, 0.000000000000000000, -0.000000000000000000 ) ) ;
#20398=CARTESIAN_POINT ( 'NONE',  ( 0.000000000000000000, 71.27951684758068041, -30.41916302227036439 ) ) ;
#20403=EDGE_CURVE ( 'NONE', #30983, #9893, #18444, .T. ) ;
#20404=AXIS2_PLACEMENT_3D ( 'NONE', #14052, #43767, #9542 ) ;
#20414=DIRECTION ( 'NONE',  ( 0.000000000000000000, -0.2079116908177532363, 0.9781476007338069101 ) ) ;
#20415=AXIS2_PLACEMENT_3D ( 'NONE', #3006, #25899, #19881 ) ;
#20416=DIRECTION ( 'NONE',  ( 0.000000000000000000, 0.000000000000000000, 1.000000000000000000 ) ) ;
#20417=ORIENTED_EDGE ( 'NONE', *, *, #47358, .T. ) ;
#20423=AXIS2_PLACEMENT_3D ( 'NONE', #39344, #34427, #5145 ) ;
#20432=CIRCLE ( 'NONE', #61281, 31.99999999999998579 ) ;
#20436=VERTEX_POINT ( 'NONE', #13044 ) ;
#20438=CARTESIAN_POINT ( 'NONE',  ( 6.000000000000000000, 22.90783923731740401, -78.73519480814930205 ) ) ;
#20449=EDGE_CURVE ( 'NONE', #6916, #39794, #7041, .T. ) ;
#20464=CARTESIAN_POINT ( 'NONE',  ( 11.99999999999999822, -81.34940948281328588, -10.30890764327469356 ) ) ;
#20467=CARTESIAN_POINT ( 'NONE',  ( 11.99999999999999822, -75.54627589209931671, -17.28742895386162814 ) ) ;
#20492=DIRECTION ( 'NONE',  ( -1.000000000000000000, 0.000000000000000000, 0.000000000000000000 ) ) ;
#20510=CARTESIAN_POINT ( 'NONE',  ( 15.00000000000000000, -13.04903810567675393, -19.60159698893424718 ) ) ;
#20511=VERTEX_POINT ( 'NONE', #12312 ) ;
#20518=FACE_OUTER_BOUND ( 'NONE', #64196, .T. ) ;
#20526=ORIENTED_EDGE ( 'NONE', *, *, #7732, .F. ) ;
#20532=AXIS2_PLACEMENT_3D ( 'NONE', #5974, #40528, #11950 ) ;
#20552=LINE ( 'NONE', #43506, #30176 ) ;
#20554=LINE ( 'NONE', #60783, #42103 ) ;
#20558=VERTEX_POINT ( 'NONE', #2921 ) ;
#20567=DIRECTION ( 'NONE',  ( 0.000000000000000000, 0.000000000000000000, 1.000000000000000000 ) ) ;
#20571=LINE ( 'NONE', #14177, #7813 ) ;
#20575=DIRECTION ( 'NONE',  ( 0.000000000000000000, 0.000000000000000000, 1.000000000000000000 ) ) ;
#20579=DIRECTION ( 'NONE',  ( -1.000000000000000000, -0.000000000000000000, -0.000000000000000000 ) ) ;
#20581=CARTESIAN_POINT ( 'NONE',  ( 11.99999999999999822, -26.01480285779785362, -70.53064760720343429 ) ) ;
#20584=FACE_OUTER_BOUND ( 'NONE', #66943, .T. ) ;
#20591=DIRECTION ( 'NONE',  ( 0.000000000000000000, 0.2079116908177641720, 0.9781476007338045786 ) ) ;
#20605=EDGE_CURVE ( 'NONE', #73443, #73391, #20552, .T. ) ;
#20608=CARTESIAN_POINT ( 'NONE',  ( 11.99999999999999822, -28.89263327155693517, -71.91182617369219088 ) ) ;
#20612=CIRCLE ( 'NONE', #62673, 31.99999999999999289 ) ;
#20614=DIRECTION ( 'NONE',  ( -1.000000000000000000, -0.000000000000000000, 0.000000000000000000 ) ) ;
#20615=ORIENTED_EDGE ( 'NONE', *, *, #57542, .T. ) ;
#20616=ORIENTED_EDGE ( 'NONE', *, *, #54166, .T. ) ;
#20630=AXIS2_PLACEMENT_3D ( 'NONE', #41528, #64466, #25714 ) ;
#20632=EDGE_CURVE ( 'NONE', #29346, #6316, #51814, .T. ) ;
#20650=DIRECTION ( 'NONE',  ( -1.000000000000000000, 0.000000000000000000, 0.000000000000000000 ) ) ;
#20652=ORIENTED_EDGE ( 'NONE', *, *, #61454, .T. ) ;
#20655=CARTESIAN_POINT ( 'NONE',  ( 0.000000000000000000, 31.46837873494978055, 68.27212725128286763 ) ) ;
#20664=DIRECTION ( 'NONE',  ( 0.000000000000000000, -0.9945218953682730678, 0.1045284632676570929 ) ) ;
#20665=FACE_OUTER_BOUND ( 'NONE', #70811, .T. ) ;
#20667=CARTESIAN_POINT ( 'NONE',  ( 15.00000000000000000, 23.49999999999999645, -1.500000000000003997 ) ) ;
#20669=VECTOR ( 'NONE', #16876, 1000.000000000000000 ) ;
#20670=DIRECTION ( 'NONE',  ( 0.000000000000000000, -0.5877852522924708056, 0.8090169943749490056 ) ) ;
#20675=AXIS2_PLACEMENT_3D ( 'NONE', #28506, #16879, #5242 ) ;
#20676=DIRECTION ( 'NONE',  ( -1.000000000000000000, 0.000000000000000000, -0.000000000000000000 ) ) ;
#20683=VECTOR ( 'NONE', #5931, 999.9999999999998863 ) ;
#20686=EDGE_CURVE ( 'NONE', #73599, #10620, #2566, .T. ) ;
#20696=EDGE_CURVE ( 'NONE', #40781, #67331, #49392, .T. ) ;
#20697=EDGE_CURVE ( 'NONE', #23233, #48188, #51336, .T. ) ;
#20699=DIRECTION ( 'NONE',  ( -1.000000000000000000, 0.000000000000000000, -0.000000000000000000 ) ) ;
#20706=CARTESIAN_POINT ( 'NONE',  ( 11.99999999999999822, 8.830959090342393125, 74.65491531819122883 ) ) ;
#20712=ADVANCED_FACE ( 'NONE', ( #63028 ), #61519, .T. ) ;
#20718=ORIENTED_EDGE ( 'NONE', *, *, #37002, .T. ) ;
#20726=EDGE_CURVE ( 'NONE', #66942, #13012, #10376, .T. ) ;
#20727=EDGE_CURVE ( 'NONE', #68066, #11414, #47041, .T. ) ;
#20733=CARTESIAN_POINT ( 'NONE',  ( 11.99999999999999822, 12.93880638057315657, 76.41127070299278046 ) ) ;
#20740=DIRECTION ( 'NONE',  ( 0.000000000000000000, -0.8910065241883626808, -0.4539904997395568520 ) ) ;
#20741=VECTOR ( 'NONE', #41737, 1000.000000000000000 ) ;
#20744=VECTOR ( 'NONE', #69212, 1000.000000000000000 ) ;
#20745=EDGE_LOOP ( 'NONE', ( #10007, #21443, #17654, #4238 ) ) ;
#20748=DIRECTION ( 'NONE',  ( -1.000000000000000000, -0.000000000000000000, 0.000000000000000000 ) ) ;
#20754=DIRECTION ( 'NONE',  ( -1.000000000000000000, 0.000000000000000000, 0.000000000000000000 ) ) ;
#20758=CARTESIAN_POINT ( 'NONE',  ( 0.000000000000000000, 0.000000000000000000, 0.000000000000000000 ) ) ;
#20761=ADVANCED_FACE ( 'NONE', ( #4021 ), #44609, .T. ) ;
#20762=DIRECTION ( 'NONE',  ( 0.000000000000000000, 0.8910065241883656784, 0.4539904997395511344 ) ) ;
#20763=EDGE_CURVE ( 'NONE', #12172, #45600, #68619, .T. ) ;
#20769=DIRECTION ( 'NONE',  ( 0.000000000000000000, 0.000000000000000000, 1.000000000000000000 ) ) ;
#20775=ORIENTED_EDGE ( 'NONE', *, *, #28622, .F. ) ;
#20776=CARTESIAN_POINT ( 'NONE',  ( 6.000000000000000000, 80.28980883073781172, -16.65972982744850128 ) ) ;
#20780=LINE ( 'NONE', #65927, #28012 ) ;
#20782=AXIS2_PLACEMENT_3D ( 'NONE', #43354, #66274, #59146 ) ;
#20783=ORIENTED_EDGE ( 'NONE', *, *, #23113, .T. ) ;
#20786=VERTEX_POINT ( 'NONE', #44975 ) ;
#20787=AXIS2_PLACEMENT_3D ( 'NONE', #4502, #74010, #67639 ) ;
#20791=ORIENTED_EDGE ( 'NONE', *, *, #52201, .F. ) ;
#20803=ORIENTED_EDGE ( 'NONE', *, *, #50154, .T. ) ;
#20806=EDGE_CURVE ( 'NONE', #45028, #62825, #23157, .T. ) ;
#20819=VERTEX_POINT ( 'NONE', #29506 ) ;
#20826=DIRECTION ( 'NONE',  ( 0.000000000000000000, -0.7071067811865389130, -0.7071067811865562325 ) ) ;
#20827=DIRECTION ( 'NONE',  ( -0.000000000000000000, -1.000000000000000000, -1.445602896647339656E-16 ) ) ;
#20834=AXIS2_PLACEMENT_3D ( 'NONE', #67498, #43838, #68245 ) ;
#20843=AXIS2_PLACEMENT_3D ( 'NONE', #13907, #60182, #30462 ) ;
#20849=CARTESIAN_POINT ( 'NONE',  ( 11.99999999999999822, 73.44644590900094272, -24.73286445877629802 ) ) ;
#20853=DIRECTION ( 'NONE',  ( -1.000000000000000000, -0.000000000000000000, -0.000000000000000000 ) ) ;
#20854=DIRECTION ( 'NONE',  ( -1.000000000000000000, 0.000000000000000000, 0.000000000000000000 ) ) ;
#20866=EDGE_CURVE ( 'NONE', #66496, #35486, #34414, .T. ) ;
#20869=CIRCLE ( 'NONE', #41278, 31.99999999999998579 ) ;
#20871=ORIENTED_EDGE ( 'NONE', *, *, #18747, .F. ) ;
#20881=AXIS2_PLACEMENT_3D ( 'NONE', #70619, #47343, #30038 ) ;
#20892=ORIENTED_EDGE ( 'NONE', *, *, #29930, .T. ) ;
#20894=EDGE_CURVE ( 'NONE', #33655, #55964, #33884, .T. ) ;
#20896=ADVANCED_FACE ( 'NONE', ( #58842 ), #35529, .T. ) ;
#20921=ORIENTED_EDGE ( 'NONE', *, *, #22240, .T. ) ;
#20923=CARTESIAN_POINT ( 'NONE',  ( 11.99999999999999822, -41.76937507738745836, -62.50329211542482710 ) ) ;
#20926=DIRECTION ( 'NONE',  ( 0.000000000000000000, 0.000000000000000000, 1.000000000000000000 ) ) ;
#20933=FACE_OUTER_BOUND ( 'NONE', #36508, .T. ) ;
#20937=CYLINDRICAL_SURFACE ( 'NONE', #25242, 77.49899999999999523 ) ;
#20944=CARTESIAN_POINT ( 'NONE',  ( 11.99999999999999822, -74.65491531819124305, 8.830959090342128448 ) ) ;
#20948=CARTESIAN_POINT ( 'NONE',  ( -10.00000000000000000, 0.000000000000000000, 0.000000000000000000 ) ) ;
#20949=EDGE_CURVE ( 'NONE', #63525, #24130, #1734, .T. ) ;
#20961=DIRECTION ( 'NONE',  ( -1.000000000000000000, 0.000000000000000000, 0.000000000000000000 ) ) ;
#20963=ORIENTED_EDGE ( 'NONE', *, *, #60939, .T. ) ;
#20965=EDGE_CURVE ( 'NONE', #10184, #16367, #70843, .T. ) ;
#20967=CYLINDRICAL_SURFACE ( 'NONE', #18863, 77.49899999999999523 ) ;
#20968=DIRECTION ( 'NONE',  ( 0.000000000000000000, 0.000000000000000000, 1.000000000000000000 ) ) ;
#20970=CARTESIAN_POINT ( 'NONE',  ( 15.00000000000000000, 0.000000000000000000, 0.000000000000000000 ) ) ;
#20971=LINE ( 'NONE', #49174, #59718 ) ;
#20977=DIRECTION ( 'NONE',  ( 0.000000000000000000, 0.6691306063588579045, -0.7431448254773945772 ) ) ;
#20978=EDGE_CURVE ( 'NONE', #64618, #46085, #8812, .T. ) ;
#20979=EDGE_CURVE ( 'NONE', #47807, #7440, #37012, .T. ) ;
#20994=CIRCLE ( 'NONE', #35389, 82.00000000000000000 ) ;
#20999=AXIS2_PLACEMENT_3D ( 'NONE', #27522, #28257, #10230 ) ;
#21007=ORIENTED_EDGE ( 'NONE', *, *, #40670, .T. ) ;
#21010=EDGE_LOOP ( 'NONE', ( #73136, #2178, #63344, #70888 ) ) ;
#21011=CARTESIAN_POINT ( 'NONE',  ( 11.99999999999999822, -81.90746397400386059, -3.894527615418766242 ) ) ;
#21015=VECTOR ( 'NONE', #15950, 1000.000000000000000 ) ;
#21016=DIRECTION ( 'NONE',  ( 0.000000000000000000, 0.000000000000000000, 1.000000000000000000 ) ) ;
#21019=DIRECTION ( 'NONE',  ( 0.000000000000000000, 0.2334453638558990629, 0.9723699203976782224 ) ) ;
#21024=DIRECTION ( 'NONE',  ( 0.000000000000000000, -0.8910065241883722287, 0.4539904997395383113 ) ) ;
#21030=EDGE_CURVE ( 'NONE', #30236, #41798, #9177, .T. ) ;
#21032=VECTOR ( 'NONE', #48651, 1000.000000000000000 ) ;
#21045=AXIS2_PLACEMENT_3D ( 'NONE', #5154, #38606, #67921 ) ;
#21046=ORIENTED_EDGE ( 'NONE', *, *, #1925, .T. ) ;
#21049=EDGE_CURVE ( 'NONE', #8256, #56438, #74181, .T. ) ;
#21056=VECTOR ( 'NONE', #30165, 1000.000000000000000 ) ;
#21063=EDGE_LOOP ( 'NONE', ( #23247, #53271, #47821, #30020 ) ) ;
#21071=DIRECTION ( 'NONE',  ( -1.000000000000000000, 0.000000000000000000, -0.000000000000000000 ) ) ;
#21074=ORIENTED_EDGE ( 'NONE', *, *, #7381, .F. ) ;
#21084=EDGE_LOOP ( 'NONE', ( #59670, #40579, #38566, #50188 ) ) ;
#21086=ORIENTED_EDGE ( 'NONE', *, *, #14243, .F. ) ;
#21096=CIRCLE ( 'NONE', #67922, 31.99999999999999289 ) ;
#21099=CIRCLE ( 'NONE', #71542, 31.99999999999998579 ) ;
#21110=CIRCLE ( 'NONE', #19927, 77.49900000000000944 ) ;
#21118=CARTESIAN_POINT ( 'NONE',  ( 15.00000000000000000, 8.688484142253932063, -21.88630264137371029 ) ) ;
#21120=AXIS2_PLACEMENT_3D ( 'NONE', #36491, #41049, #63978 ) ;
#21123=DIRECTION ( 'NONE',  ( 0.000000000000000000, 0.000000000000000000, 1.000000000000000000 ) ) ;
#21125=ADVANCED_FACE ( 'NONE', ( #28313 ), #21562, .T. ) ;
#21129=ORIENTED_EDGE ( 'NONE', *, *, #68945, .T. ) ;
#21131=CARTESIAN_POINT ( 'NONE',  ( 0.000000000000000000, -77.32052557432837148, -5.256550761633681290 ) ) ;
#21137=DIRECTION ( 'NONE',  ( -1.000000000000000000, 0.000000000000000000, -0.000000000000000000 ) ) ;
#21144=CYLINDRICAL_SURFACE ( 'NONE', #16223, 82.00000000000000000 ) ;
#21149=EDGE_LOOP ( 'NONE', ( #3751, #36654, #62994, #66078 ) ) ;
#21153=VERTEX_POINT ( 'NONE', #2298 ) ;
#21155=AXIS2_PLACEMENT_3D ( 'NONE', #38043, #20385, #60256 ) ;
#21179=DIRECTION ( 'NONE',  ( -1.000000000000000000, 0.000000000000000000, -0.000000000000000000 ) ) ;
#21184=ADVANCED_FACE ( 'NONE', ( #14268 ), #36458, .F. ) ;
#21191=ADVANCED_FACE ( 'NONE', ( #70288 ), #65056, .T. ) ;
#21194=CARTESIAN_POINT ( 'NONE',  ( 11.99999999999999822, 0.000000000000000000, 0.000000000000000000 ) ) ;
#21195=DIRECTION ( 'NONE',  ( 0.000000000000000000, 0.000000000000000000, 1.000000000000000000 ) ) ;
#21198=AXIS2_PLACEMENT_3D ( 'NONE', #4957, #61345, #5327 ) ;
#21207=FACE_OUTER_BOUND ( 'NONE', #970, .T. ) ;
#21214=AXIS2_PLACEMENT_3D ( 'NONE', #17267, #68030, #11253 ) ;
#21226=VERTEX_POINT ( 'NONE', #19168 ) ;
#21236=CARTESIAN_POINT ( 'NONE',  ( 11.99999999999999822, -20.40083707022935400, 72.35432306680478121 ) ) ;
#21239=CARTESIAN_POINT ( 'NONE',  ( 11.99999999999999822, 55.19960302592066625, 51.03279382321107249 ) ) ;
#21247=VERTEX_POINT ( 'NONE', #48117 ) ;
#21249=FACE_OUTER_BOUND ( 'NONE', #19434, .T. ) ;
#21250=LINE ( 'NONE', #66410, #13438 ) ;
#21262=VERTEX_POINT ( 'NONE', #31550 ) ;
#21265=FACE_OUTER_BOUND ( 'NONE', #7581, .T. ) ;
#21269=DIRECTION ( 'NONE',  ( 1.000000000000000000, 0.000000000000000000, 0.000000000000000000 ) ) ;
#21273=ORIENTED_EDGE ( 'NONE', *, *, #65110, .F. ) ;
#21278=EDGE_CURVE ( 'NONE', #15874, #52714, #13887, .T. ) ;
#21283=ADVANCED_FACE ( 'NONE', ( #48848 ), #71767, .T. ) ;
#21289=CARTESIAN_POINT ( 'NONE',  ( 11.99999999999999822, 30.41916302227114599, 71.27951684758035356 ) ) ;
#21295=CARTESIAN_POINT ( 'NONE',  ( 0.000000000000000000, -46.53671651293907274, -59.03961581697448935 ) ) ;
#21298=DIRECTION ( 'NONE',  ( -1.000000000000000000, 0.000000000000000000, -0.000000000000000000 ) ) ;
#21311=EDGE_CURVE ( 'NONE', #67063, #26486, #56710, .T. ) ;
#21321=EDGE_LOOP ( 'NONE', ( #59720, #31697, #65949, #44990 ) ) ;
#21324=CARTESIAN_POINT ( 'NONE',  ( 11.99999999999999822, 73.95703589264006439, -23.16143007188350822 ) ) ;
#21328=DIRECTION ( 'NONE',  ( -1.000000000000000000, -0.000000000000000000, 0.000000000000000000 ) ) ;
#21346=DIRECTION ( 'NONE',  ( -1.000000000000000000, -0.000000000000000000, -0.000000000000000000 ) ) ;
#21350=VERTEX_POINT ( 'NONE', #33035 ) ;
#21352=CARTESIAN_POINT ( 'NONE',  ( 15.00000000000000000, 0.000000000000000000, 0.000000000000000000 ) ) ;
#21354=ORIENTED_EDGE ( 'NONE', *, *, #17233, .T. ) ;
#21358=AXIS2_PLACEMENT_3D ( 'NONE', #67446, #26846, #49771 ) ;
#21359=ADVANCED_FACE ( 'NONE', ( #31925 ), #55232, .F. ) ;
#21361=AXIS2_PLACEMENT_3D ( 'NONE', #53132, #29812, #18540 ) ;
#21362=CARTESIAN_POINT ( 'NONE',  ( 0.000000000000000000, -31.46837873494930093, -68.27212725128309501 ) ) ;
#21364=EDGE_CURVE ( 'NONE', #72371, #43291, #14640, .T. ) ;
#21366=DIRECTION ( 'NONE',  ( 1.000000000000000000, -0.000000000000000000, -0.000000000000000000 ) ) ;
#21379=AXIS2_PLACEMENT_3D ( 'NONE', #53280, #58542, #23976 ) ;
#21392=CARTESIAN_POINT ( 'NONE',  ( 5.999999999999999112, -44.99326035066101781, 68.55367621811126355 ) ) ;
#21393=DIRECTION ( 'NONE',  ( 0.000000000000000000, -0.4999999999999921174, 0.8660254037844431485 ) ) ;
#21400=DIRECTION ( 'NONE',  ( -1.000000000000000000, -0.000000000000000000, 0.000000000000000000 ) ) ;
#21403=VECTOR ( 'NONE', #71139, 1000.000000000000000 ) ;
#21404=AXIS2_PLACEMENT_3D ( 'NONE', #49054, #50803, #33897 ) ;
#21421=DIRECTION ( 'NONE',  ( -1.000000000000000000, 0.000000000000000000, 0.000000000000000000 ) ) ;
#21428=EDGE_LOOP ( 'NONE', ( #33909, #33256, #7433, #29850 ) ) ;
#21431=CIRCLE ( 'NONE', #63500, 77.49899999999999523 ) ;
#21432=VERTEX_POINT ( 'NONE', #49953 ) ;
#21443=ORIENTED_EDGE ( 'NONE', *, *, #6703, .F. ) ;
#21450=EDGE_CURVE ( 'NONE', #15852, #19406, #51823, .T. ) ;
#21451=AXIS2_PLACEMENT_3D ( 'NONE', #17036, #21548, #56897 ) ;
#21457=EDGE_CURVE ( 'NONE', #55964, #57897, #42324, .T. ) ;
#21458=ORIENTED_EDGE ( 'NONE', *, *, #51684, .F. ) ;
#21459=AXIS2_PLACEMENT_3D ( 'NONE', #64836, #31342, #36246 ) ;
#21469=ORIENTED_EDGE ( 'NONE', *, *, #32399, .F. ) ;
#21483=CIRCLE ( 'NONE', #40721, 31.99999999999998579 ) ;
#21487=AXIS2_PLACEMENT_3D ( 'NONE', #24781, #42086, #65024 ) ;
#21489=FACE_OUTER_BOUND ( 'NONE', #39511, .T. ) ;
#21492=VECTOR ( 'NONE', #19931, 1000.000000000000000 ) ;
#21493=FACE_OUTER_BOUND ( 'NONE', #8493, .T. ) ;
#21496=DIRECTION ( 'NONE',  ( -1.000000000000000000, -0.000000000000000000, 0.000000000000000000 ) ) ;
#21501=CARTESIAN_POINT ( 'NONE',  ( 11.99999999999999822, 0.000000000000000000, 0.000000000000000000 ) ) ;
#21504=AXIS2_PLACEMENT_3D ( 'NONE', #60950, #49295, #71105 ) ;
#21514=AXIS2_PLACEMENT_3D ( 'NONE', #60092, #13461, #48052 ) ;
#21521=EDGE_LOOP ( 'NONE', ( #13503, #69731, #49130, #29633 ) ) ;
#21525=CARTESIAN_POINT ( 'NONE',  ( 0.000000000000000000, 66.50666863322000211, 39.78640506895628448 ) ) ;
#21527=ORIENTED_EDGE ( 'NONE', *, *, #2266, .F. ) ;
#21530=DIRECTION ( 'NONE',  ( -1.000000000000000000, 0.000000000000000000, 0.000000000000000000 ) ) ;
#21534=VERTEX_POINT ( 'NONE', #53207 ) ;
#21548=DIRECTION ( 'NONE',  ( -1.000000000000000000, -0.000000000000000000, -0.000000000000000000 ) ) ;
#21556=ORIENTED_EDGE ( 'NONE', *, *, #19439, .F. ) ;
#21559=CYLINDRICAL_SURFACE ( 'NONE', #49323, 31.99999999999998579 ) ;
#21562=CYLINDRICAL_SURFACE ( 'NONE', #67480, 82.00000000000000000 ) ;
#21569=EDGE_CURVE ( 'NONE', #73113, #51687, #53100, .T. ) ;
#21570=CARTESIAN_POINT ( 'NONE',  ( 0.000000000000000000, 59.75363087400153006, -56.15606465354896670 ) ) ;
#21578=CIRCLE ( 'NONE', #16766, 31.99999999999998579 ) ;
#21583=CARTESIAN_POINT ( 'NONE',  ( 15.00000000000000000, 0.000000000000000000, 0.000000000000000000 ) ) ;
#21595=CARTESIAN_POINT ( 'NONE',  ( 11.99999999999999822, 55.20638768913831029, -51.02545421589267960 ) ) ;
#21600=DIRECTION ( 'NONE',  ( -1.000000000000000000, -0.000000000000000000, -0.000000000000000000 ) ) ;
#21603=AXIS2_PLACEMENT_3D ( 'NONE', #47193, #69746, #40821 ) ;
#21608=ORIENTED_EDGE ( 'NONE', *, *, #72222, .F. ) ;
#21613=EDGE_CURVE ( 'NONE', #8165, #30236, #17093, .T. ) ;
#21620=EDGE_CURVE ( 'NONE', #46914, #15732, #50724, .T. ) ;
#21633=ORIENTED_EDGE ( 'NONE', *, *, #72326, .T. ) ;
#21637=DIRECTION ( 'NONE',  ( -1.000000000000000000, 0.000000000000000000, -0.000000000000000000 ) ) ;
#21638=AXIS2_PLACEMENT_3D ( 'NONE', #42125, #70291, #36462 ) ;
#21642=VERTEX_POINT ( 'NONE', #55427 ) ;
#21646=ORIENTED_EDGE ( 'NONE', *, *, #49219, .F. ) ;
#21652=CARTESIAN_POINT ( 'NONE',  ( 11.99999999999999822, -44.88180994100329713, -63.18004540533077318 ) ) ;
#21666=EDGE_CURVE ( 'NONE', #33478, #59348, #70855, .T. ) ;
#21667=CARTESIAN_POINT ( 'NONE',  ( 0.000000000000000000, 39.78640506895698081, -66.50666863321957578 ) ) ;
#21672=ORIENTED_EDGE ( 'NONE', *, *, #34194, .T. ) ;
#21680=DIRECTION ( 'NONE',  ( -1.000000000000000000, 0.000000000000000000, 0.000000000000000000 ) ) ;
#21681=DIRECTION ( 'NONE',  ( 1.000000000000000000, -0.000000000000000000, -0.000000000000000000 ) ) ;
#21693=DIRECTION ( 'NONE',  ( 0.000000000000000000, 0.000000000000000000, 1.000000000000000000 ) ) ;
#21703=CARTESIAN_POINT ( 'NONE',  ( 0.000000000000000000, 0.000000000000000000, 0.000000000000000000 ) ) ;
#21709=EDGE_CURVE ( 'NONE', #6766, #44013, #42309, .T. ) ;
#21712=CARTESIAN_POINT ( 'NONE',  ( -10.00000000000000000, 0.000000000000000000, 0.000000000000000000 ) ) ;
#21713=CARTESIAN_POINT ( 'NONE',  ( 0.000000000000000000, 39.47590169984846398, 71.87247863392427405 ) ) ;
#21714=LINE ( 'NONE', #43921, #11046 ) ;
#21720=ORIENTED_EDGE ( 'NONE', *, *, #2328, .T. ) ;
#21721=VERTEX_POINT ( 'NONE', #8080 ) ;
#21723=DIRECTION ( 'NONE',  ( -1.000000000000000000, -0.000000000000000000, 0.000000000000000000 ) ) ;
#21738=EDGE_LOOP ( 'NONE', ( #14032, #42267, #53511, #15944 ) ) ;
#21739=EDGE_CURVE ( 'NONE', #53358, #52748, #30284, .T. ) ;
#21744=CARTESIAN_POINT ( 'NONE',  ( 12.00000000000000000, -19.89357724625003598, -12.59942793731059041 ) ) ;
#21748=EDGE_CURVE ( 'NONE', #3018, #31113, #48305, .T. ) ;
#21751=VERTEX_POINT ( 'NONE', #33221 ) ;
#21755=EDGE_CURVE ( 'NONE', #4487, #63285, #45925, .T. ) ;
#21761=DIRECTION ( 'NONE',  ( 0.000000000000000000, 0.7604059656000276002, 0.6494480483301875440 ) ) ;
#21771=CIRCLE ( 'NONE', #50579, 82.00000000000000000 ) ;
#21777=CARTESIAN_POINT ( 'NONE',  ( 11.99999999999999822, 0.000000000000000000, 0.000000000000000000 ) ) ;
#21785=CYLINDRICAL_SURFACE ( 'NONE', #44603, 77.49899999999999523 ) ;
#21801=ADVANCED_FACE ( 'NONE', ( #39996 ), #56167, .T. ) ;
#21804=ORIENTED_EDGE ( 'NONE', *, *, #12984, .T. ) ;
#21807=ORIENTED_EDGE ( 'NONE', *, *, #64934, .F. ) ;
#21814=CIRCLE ( 'NONE', #71065, 82.00000000000000000 ) ;
#21815=ORIENTED_EDGE ( 'NONE', *, *, #57917, .F. ) ;
#21822=ORIENTED_EDGE ( 'NONE', *, *, #60595, .F. ) ;
#21824=ORIENTED_EDGE ( 'NONE', *, *, #27940, .F. ) ;
#21825=DIRECTION ( 'NONE',  ( -1.000000000000000000, 0.000000000000000000, 0.000000000000000000 ) ) ;
#21827=VERTEX_POINT ( 'NONE', #61448 ) ;
#21830=ADVANCED_FACE ( 'NONE', ( #50522 ), #22331, .T. ) ;
#21838=DIRECTION ( 'NONE',  ( -1.000000000000000000, 0.000000000000000000, -0.000000000000000000 ) ) ;
#21840=ORIENTED_EDGE ( 'NONE', *, *, #20449, .T. ) ;
#21842=ORIENTED_EDGE ( 'NONE', *, *, #39386, .T. ) ;
#21848=CARTESIAN_POINT ( 'NONE',  ( 11.99999999999999822, 0.000000000000000000, 0.000000000000000000 ) ) ;
#21856=AXIS2_PLACEMENT_3D ( 'NONE', #45097, #37960, #33414 ) ;
#21858=CARTESIAN_POINT ( 'NONE',  ( 11.99999999999999822, -64.81221759200306565, -50.23322058963420034 ) ) ;
#21861=AXIS2_PLACEMENT_3D ( 'NONE', #15372, #37585, #55608 ) ;
#21868=AXIS2_PLACEMENT_3D ( 'NONE', #12282, #58518, #6296 ) ;
#21878=CARTESIAN_POINT ( 'NONE',  ( 0.000000000000000000, -81.34940948281344220, 10.30890764327355846 ) ) ;
#21883=CARTESIAN_POINT ( 'NONE',  ( 0.000000000000000000, -31.47745569255189224, 68.26794271651249346 ) ) ;
#21886=DIRECTION ( 'NONE',  ( -1.000000000000000000, 0.000000000000000000, 0.000000000000000000 ) ) ;
#21890=DIRECTION ( 'NONE',  ( -1.000000000000000000, 0.000000000000000000, 0.000000000000000000 ) ) ;
#21891=ORIENTED_EDGE ( 'NONE', *, *, #73389, .F. ) ;
#21896=CARTESIAN_POINT ( 'NONE',  ( -10.00000000000000000, 0.000000000000000000, 0.000000000000000000 ) ) ;
#21902=CIRCLE ( 'NONE', #8707, 31.99999999999998579 ) ;
#21904=VERTEX_POINT ( 'NONE', #18528 ) ;
#21905=ORIENTED_EDGE ( 'NONE', *, *, #25273, .F. ) ;
#21907=EDGE_CURVE ( 'NONE', #7440, #41355, #52985, .T. ) ;
#21909=ADVANCED_FACE ( 'NONE', ( #52372 ), #58387, .F. ) ;
#21910=ORIENTED_EDGE ( 'NONE', *, *, #55555, .F. ) ;
#21914=DIRECTION ( 'NONE',  ( -1.000000000000000000, 0.000000000000000000, 0.000000000000000000 ) ) ;
#21920=CIRCLE ( 'NONE', #24391, 31.99999999999999645 ) ;
#21923=EDGE_CURVE ( 'NONE', #18767, #58541, #29802, .T. ) ;
#21929=DIRECTION ( 'NONE',  ( 0.000000000000000000, 0.000000000000000000, 1.000000000000000000 ) ) ;
#21932=FACE_OUTER_BOUND ( 'NONE', #47356, .T. ) ;
#21942=DIRECTION ( 'NONE',  ( 0.000000000000000000, 0.000000000000000000, 1.000000000000000000 ) ) ;
#21943=DIRECTION ( 'NONE',  ( 0.000000000000000000, 0.000000000000000000, 1.000000000000000000 ) ) ;
#21945=CARTESIAN_POINT ( 'NONE',  ( 11.99999999999999822, 0.000000000000000000, 0.000000000000000000 ) ) ;
#21946=DIRECTION ( 'NONE',  ( 0.000000000000000000, -0.8526401643540860720, -0.5224985647159590130 ) ) ;
#21947=LINE ( 'NONE', #56159, #18013 ) ;
#21949=EDGE_LOOP ( 'NONE', ( #16478, #69515, #581, #27750 ) ) ;
#21964=CYLINDRICAL_SURFACE ( 'NONE', #69314, 31.99999999999998579 ) ;
#21974=DIRECTION ( 'NONE',  ( -1.000000000000000000, -0.000000000000000000, 0.000000000000000000 ) ) ;
#21977=DIRECTION ( 'NONE',  ( 0.000000000000000000, 0.7604059656000276002, 0.6494480483301876550 ) ) ;
#21981=ADVANCED_FACE ( 'NONE', ( #64782 ), #13264, .T. ) ;
#21984=ORIENTED_EDGE ( 'NONE', *, *, #12407, .T. ) ;
#21989=ORIENTED_EDGE ( 'NONE', *, *, #21311, .F. ) ;
#21991=ORIENTED_EDGE ( 'NONE', *, *, #1495, .T. ) ;
#22008=ORIENTED_EDGE ( 'NONE', *, *, #63001, .T. ) ;
#22014=DIRECTION ( 'NONE',  ( -1.000000000000000000, 0.000000000000000000, 0.000000000000000000 ) ) ;
#22021=ORIENTED_EDGE ( 'NONE', *, *, #42953, .T. ) ;
#22025=ORIENTED_EDGE ( 'NONE', *, *, #2418, .T. ) ;
#22031=DIRECTION ( 'NONE',  ( -1.000000000000000000, -0.000000000000000000, 0.000000000000000000 ) ) ;
#22036=DIRECTION ( 'NONE',  ( 0.000000000000000000, -0.9510565162951565288, 0.3090169943749382919 ) ) ;
#22037=VECTOR ( 'NONE', #3043, 1000.000000000000000 ) ;
#22043=DIRECTION ( 'NONE',  ( -1.000000000000000000, 0.000000000000000000, -0.000000000000000000 ) ) ;
#22050=AXIS2_PLACEMENT_3D ( 'NONE', #21352, #61982, #10090 ) ;
#22053=CARTESIAN_POINT ( 'NONE',  ( 0.000000000000000000, 68.27212725128275395, -31.46837873495001503 ) ) ;
#22056=DIRECTION ( 'NONE',  ( 0.000000000000000000, -0.9238795325112906243, 0.3826834323650805669 ) ) ;
#22059=DIRECTION ( 'NONE',  ( -1.000000000000000000, 0.000000000000000000, 0.000000000000000000 ) ) ;
#22062=CYLINDRICAL_SURFACE ( 'NONE', #51370, 31.99999999999998579 ) ;
#22064=DIRECTION ( 'NONE',  ( -0.000000000000000000, -0.6691306063588670083, -0.7431448254773863615 ) ) ;
#22074=AXIS2_PLACEMENT_3D ( 'NONE', #12281, #52138, #35582 ) ;
#22079=AXIS2_PLACEMENT_3D ( 'NONE', #30202, #24213, #58041 ) ;
#22084=CARTESIAN_POINT ( 'NONE',  ( 11.99999999999999822, -6.903761155838323837, 77.19088730480521576 ) ) ;
#22092=CARTESIAN_POINT ( 'NONE',  ( 0.000000000000000000, 0.8261519478441983200, -77.49459641780885022 ) ) ;
#22093=DIRECTION ( 'NONE',  ( 0.000000000000000000, 0.7431448254773954654, 0.6691306063588569053 ) ) ;
#22101=EDGE_LOOP ( 'NONE', ( #38842, #24056, #62946, #19273 ) ) ;
#22103=CARTESIAN_POINT ( 'NONE',  ( 11.99999999999999822, -65.59268652807183742, -36.72794159290312166 ) ) ;
#22109=LINE ( 'NONE', #56329, #43151 ) ;
#22110=ORIENTED_EDGE ( 'NONE', *, *, #58000, .T. ) ;
#22112=AXIS2_PLACEMENT_3D ( 'NONE', #49859, #37496, #32570 ) ;
#22132=EDGE_CURVE ( 'NONE', #52748, #31332, #72357, .T. ) ;
#22133=VECTOR ( 'NONE', #32251, 1000.000000000000000 ) ;
#22140=LINE ( 'NONE', #38692, #63308 ) ;
#22144=AXIS2_PLACEMENT_3D ( 'NONE', #47495, #25306, #48234 ) ;
#22145=CIRCLE ( 'NONE', #24555, 31.99999999999998934 ) ;
#22152=CIRCLE ( 'NONE', #72560, 31.99999999999999289 ) ;
#22155=CARTESIAN_POINT ( 'NONE',  ( 0.000000000000000000, 63.18004540533029001, 44.88180994100398635 ) ) ;
#22157=DIRECTION ( 'NONE',  ( 0.000000000000000000, -0.6691306063588586817, 0.7431448254773939111 ) ) ;
#22159=DIRECTION ( 'NONE',  ( -1.000000000000000000, 0.000000000000000000, 0.000000000000000000 ) ) ;
#22162=EDGE_CURVE ( 'NONE', #68158, #34606, #65014, .T. ) ;
#22185=AXIS2_PLACEMENT_3D ( 'NONE', #15164, #67418, #16281 ) ;
#22190=VECTOR ( 'NONE', #73747, 1000.000000000000000 ) ;
#22191=ORIENTED_EDGE ( 'NONE', *, *, #19832, .T. ) ;
#22193=DIRECTION ( 'NONE',  ( -1.000000000000000000, 0.000000000000000000, 0.000000000000000000 ) ) ;
#22199=CIRCLE ( 'NONE', #39001, 31.99999999999998224 ) ;
#22202=ORIENTED_EDGE ( 'NONE', *, *, #1849, .T. ) ;
#22203=VECTOR ( 'NONE', #41182, 1000.000000000000000 ) ;
#22224=DIRECTION ( 'NONE',  ( 0.000000000000000000, 0.3826834323650904479, -0.9238795325112865164 ) ) ;
#22226=EDGE_CURVE ( 'NONE', #63342, #56025, #6203, .T. ) ;
#22229=LINE ( 'NONE', #27486, #58366 ) ;
#22240=EDGE_CURVE ( 'NONE', #46961, #57093, #56594, .T. ) ;
#22241=AXIS2_PLACEMENT_3D ( 'NONE', #52843, #64132, #7354 ) ;
#22246=LINE ( 'NONE', #72253, #28086 ) ;
#22248=DIRECTION ( 'NONE',  ( -1.000000000000000000, 0.000000000000000000, -0.000000000000000000 ) ) ;
#22250=CYLINDRICAL_SURFACE ( 'NONE', #5360, 77.49899999999999523 ) ;
#22259=ORIENTED_EDGE ( 'NONE', *, *, #9994, .T. ) ;
#22261=DIRECTION ( 'NONE',  ( 0.000000000000000000, -0.9969173337331271867, -0.07845909572785571273 ) ) ;
#22263=EDGE_CURVE ( 'NONE', #72991, #43856, #68779, .T. ) ;
#22267=CARTESIAN_POINT ( 'NONE',  ( 0.000000000000000000, 35.91791733033476675, 68.67312586195008350 ) ) ;
#22268=EDGE_CURVE ( 'NONE', #70465, #69052, #73355, .T. ) ;
#22271=AXIS2_PLACEMENT_3D ( 'NONE', #54798, #14200, #54431 ) ;
#22274=VERTEX_POINT ( 'NONE', #33501 ) ;
#22277=CARTESIAN_POINT ( 'NONE',  ( 11.99999999999999822, 0.000000000000000000, 0.000000000000000000 ) ) ;
#22282=ORIENTED_EDGE ( 'NONE', *, *, #66532, .F. ) ;
#22292=EDGE_LOOP ( 'NONE', ( #25893, #33912, #57426, #32900 ) ) ;
#22304=DIRECTION ( 'NONE',  ( -1.000000000000000000, -0.000000000000000000, 0.000000000000000000 ) ) ;
#22314=DIRECTION ( 'NONE',  ( -1.000000000000000000, 0.000000000000000000, 0.000000000000000000 ) ) ;
#22321=CARTESIAN_POINT ( 'NONE',  ( 11.99999999999999822, 0.000000000000000000, 0.000000000000000000 ) ) ;
#22326=EDGE_CURVE ( 'NONE', #60480, #5309, #49439, .T. ) ;
#22331=CYLINDRICAL_SURFACE ( 'NONE', #45823, 31.99999999999998579 ) ;
#22336=ORIENTED_EDGE ( 'NONE', *, *, #1796, .F. ) ;
#22340=CARTESIAN_POINT ( 'NONE',  ( 0.000000000000000000, 23.16143007188530234, -73.95703589263949596 ) ) ;
#22346=VECTOR ( 'NONE', #41817, 1000.000000000000000 ) ;
#22357=AXIS2_PLACEMENT_3D ( 'NONE', #3220, #48680, #14466 ) ;
#22364=AXIS2_PLACEMENT_3D ( 'NONE', #3758, #49586, #36459 ) ;
#22365=CARTESIAN_POINT ( 'NONE',  ( 11.99999999999999822, 34.44570377933693806, -69.42325613327405165 ) ) ;
#22367=DIRECTION ( 'NONE',  ( -1.000000000000000000, 0.000000000000000000, -0.000000000000000000 ) ) ;
#22370=ORIENTED_EDGE ( 'NONE', *, *, #11855, .F. ) ;
#22373=VERTEX_POINT ( 'NONE', #44808 ) ;
#22375=LINE ( 'NONE', #50184, #53247 ) ;
#22380=ORIENTED_EDGE ( 'NONE', *, *, #55159, .T. ) ;
#22390=LINE ( 'NONE', #11831, #15259 ) ;
#22394=CARTESIAN_POINT ( 'NONE',  ( 11.99999999999999822, 0.000000000000000000, 0.000000000000000000 ) ) ;
#22402=CARTESIAN_POINT ( 'NONE',  ( 11.99999999999999822, 0.000000000000000000, 0.000000000000000000 ) ) ;
#22405=CARTESIAN_POINT ( 'NONE',  ( 15.00000000000000000, 5.835314593368777558, 22.81335362449846471 ) ) ;
#22412=ORIENTED_EDGE ( 'NONE', *, *, #34368, .T. ) ;
#22413=EDGE_CURVE ( 'NONE', #39476, #66935, #2691, .T. ) ;
#22415=CIRCLE ( 'NONE', #34424, 77.49899999999999523 ) ;
#22422=DIRECTION ( 'NONE',  ( -1.000000000000000000, 0.000000000000000000, 0.000000000000000000 ) ) ;
#22425=EDGE_CURVE ( 'NONE', #35486, #48585, #69828, .T. ) ;
#22431=DIRECTION ( 'NONE',  ( -1.000000000000000000, -0.000000000000000000, 0.000000000000000000 ) ) ;
#22433=CARTESIAN_POINT ( 'NONE',  ( 12.00000000000000000, 14.60985201121729737, 18.46759930825687235 ) ) ;
#22448=AXIS2_PLACEMENT_3D ( 'NONE', #24192, #47127, #18896 ) ;
#22454=AXIS2_PLACEMENT_3D ( 'NONE', #20655, #15002, #32287 ) ;
#22456=VECTOR ( 'NONE', #63261, 1000.000000000000000 ) ;
#22459=VECTOR ( 'NONE', #64030, 1000.000000000000000 ) ;
#22462=ORIENTED_EDGE ( 'NONE', *, *, #9583, .T. ) ;
#22468=DIRECTION ( 'NONE',  ( 0.000000000000000000, 0.000000000000000000, -1.000000000000000000 ) ) ;
#22474=CARTESIAN_POINT ( 'NONE',  ( 11.99999999999999822, 0.000000000000000000, 0.000000000000000000 ) ) ;
#22482=CYLINDRICAL_SURFACE ( 'NONE', #48584, 82.00000000000000000 ) ;
#22487=ORIENTED_EDGE ( 'NONE', *, *, #5565, .T. ) ;
#22491=ORIENTED_EDGE ( 'NONE', *, *, #39377, .F. ) ;
#22497=EDGE_CURVE ( 'NONE', #12910, #55755, #26617, .T. ) ;
#22502=CARTESIAN_POINT ( 'NONE',  ( 11.99999999999999822, 77.49459641780886443, 0.8261519478433866359 ) ) ;
#22508=CARTESIAN_POINT ( 'NONE',  ( -10.00000000000000000, 0.000000000000000000, 0.000000000000000000 ) ) ;
#22513=ORIENTED_EDGE ( 'NONE', *, *, #21748, .T. ) ;
#22517=DIRECTION ( 'NONE',  ( 0.000000000000000000, -0.8526401643540970632, 0.5224985647159409163 ) ) ;
#22526=CYLINDRICAL_SURFACE ( 'NONE', #7376, 82.00000000000000000 ) ;
#22529=LINE ( 'NONE', #16890, #62077 ) ;
#22534=CARTESIAN_POINT ( 'NONE',  ( 0.000000000000000000, -58.39081064771786345, 50.95692526931308919 ) ) ;
#22538=DIRECTION ( 'NONE',  ( -1.000000000000000000, 0.000000000000000000, -0.000000000000000000 ) ) ;
#22539=CARTESIAN_POINT ( 'NONE',  ( 15.00000000000000000, 9.615535125378766423, -24.73947219025917121 ) ) ;
#22541=VECTOR ( 'NONE', #39958, 1000.000000000000114 ) ;
#22543=ORIENTED_EDGE ( 'NONE', *, *, #65038, .T. ) ;
#22572=VERTEX_POINT ( 'NONE', #36468 ) ;
#22582=DIRECTION ( 'NONE',  ( 0.000000000000000000, 0.9510565162951544194, -0.3090169943749446757 ) ) ;
#22587=ORIENTED_EDGE ( 'NONE', *, *, #21364, .F. ) ;
#22588=FACE_OUTER_BOUND ( 'NONE', #5185, .T. ) ;
#22590=AXIS2_PLACEMENT_3D ( 'NONE', #13664, #43740, #31326 ) ;
#22591=AXIS2_PLACEMENT_3D ( 'NONE', #15486, #20397, #9108 ) ;
#22597=ORIENTED_EDGE ( 'NONE', *, *, #6285, .T. ) ;
#22602=ADVANCED_FACE ( 'NONE', ( #19546 ), #71411, .T. ) ;
#22609=CARTESIAN_POINT ( 'NONE',  ( 0.000000000000000000, -80.55351364060578589, -15.33399622253570094 ) ) ;
#22610=LINE ( 'NONE', #16971, #53592 ) ;
#22615=EDGE_CURVE ( 'NONE', #9042, #25161, #13172, .T. ) ;
#22622=DIRECTION ( 'NONE',  ( 0.000000000000000000, 0.000000000000000000, 1.000000000000000000 ) ) ;
#22623=CARTESIAN_POINT ( 'NONE',  ( -10.00000000000000000, 0.000000000000000000, 0.000000000000000000 ) ) ;
#22634=VECTOR ( 'NONE', #2722, 1000.000000000000227 ) ;
#22640=CYLINDRICAL_SURFACE ( 'NONE', #46368, 82.00000000000000000 ) ;
#22652=ADVANCED_FACE ( 'NONE', ( #13899 ), #3398, .T. ) ;
#22664=CIRCLE ( 'NONE', #57495, 31.99999999999998579 ) ;
#22668=VECTOR ( 'NONE', #46213, 1000.000000000000000 ) ;
#22669=ORIENTED_EDGE ( 'NONE', *, *, #20360, .T. ) ;
#22680=CIRCLE ( 'NONE', #38280, 82.00000000000000000 ) ;
#22683=CYLINDRICAL_SURFACE ( 'NONE', #55228, 82.00000000000000000 ) ;
#22694=DIRECTION ( 'NONE',  ( 0.000000000000000000, 0.8526401643540935105, -0.5224985647159466895 ) ) ;
#22696=AXIS2_PLACEMENT_3D ( 'NONE', #5050, #27194, #11404 ) ;
#22699=AXIS2_PLACEMENT_3D ( 'NONE', #30432, #35357, #65048 ) ;
#22710=DIRECTION ( 'NONE',  ( -1.000000000000000000, -0.000000000000000000, 0.000000000000000000 ) ) ;
#22711=ADVANCED_FACE ( 'NONE', ( #47753 ), #30454, .F. ) ;
#22712=CARTESIAN_POINT ( 'NONE',  ( 11.99999999999999822, 0.000000000000000000, 0.000000000000000000 ) ) ;
#22715=CYLINDRICAL_SURFACE ( 'NONE', #27711, 82.00000000000000000 ) ;
#22717=CIRCLE ( 'NONE', #15494, 82.00000000000000000 ) ;
#22718=ORIENTED_EDGE ( 'NONE', *, *, #16450, .T. ) ;
#22721=FACE_OUTER_BOUND ( 'NONE', #11444, .T. ) ;
#22723=CYLINDRICAL_SURFACE ( 'NONE', #14174, 77.49899999999999523 ) ;
#22730=CIRCLE ( 'NONE', #17934, 82.00000000000000000 ) ;
#22733=DIRECTION ( 'NONE',  ( -1.000000000000000000, -0.000000000000000000, 0.000000000000000000 ) ) ;
#22739=VECTOR ( 'NONE', #56374, 1000.000000000000000 ) ;
#22749=DIRECTION ( 'NONE',  ( -1.000000000000000000, 0.000000000000000000, 0.000000000000000000 ) ) ;
#22753=ORIENTED_EDGE ( 'NONE', *, *, #28076, .T. ) ;
#22756=ADVANCED_FACE ( 'NONE', ( #67276 ), #15018, .T. ) ;
#22758=ADVANCED_FACE ( 'NONE', ( #68018 ), #66539, .T. ) ;
#22760=ORIENTED_EDGE ( 'NONE', *, *, #22326, .T. ) ;
#22771=DIRECTION ( 'NONE',  ( 0.000000000000000000, 0.000000000000000000, 1.000000000000000000 ) ) ;
#22776=EDGE_CURVE ( 'NONE', #63927, #2660, #21902, .T. ) ;
#22781=VERTEX_POINT ( 'NONE', #60895 ) ;
#22787=CARTESIAN_POINT ( 'NONE',  ( 11.99999999999999822, 44.99326035066149387, -68.55367621811095091 ) ) ;
#22792=AXIS2_PLACEMENT_3D ( 'NONE', #9081, #26371, #49663 ) ;
#22793=DIRECTION ( 'NONE',  ( 0.000000000000000000, 0.000000000000000000, -1.000000000000000000 ) ) ;
#22801=ORIENTED_EDGE ( 'NONE', *, *, #27035, .F. ) ;
#22802=CIRCLE ( 'NONE', #16781, 31.99999999999998934 ) ;
#22803=DIRECTION ( 'NONE',  ( 0.000000000000000000, 0.8090169943749486725, -0.5877852522924713607 ) ) ;
#22809=AXIS2_PLACEMENT_3D ( 'NONE', #20923, #9274, #38216 ) ;
#22817=CARTESIAN_POINT ( 'NONE',  ( 15.00000000000000000, 18.84667830672605859, 18.68964196561243796 ) ) ;
#22824=VERTEX_POINT ( 'NONE', #32673 ) ;
#22829=CIRCLE ( 'NONE', #19208, 77.49899999999999523 ) ;
#22838=EDGE_CURVE ( 'NONE', #56792, #38016, #4509, .T. ) ;
#22847=CARTESIAN_POINT ( 'NONE',  ( 11.99999999999999822, 75.16055320797030959, 18.89407956138283851 ) ) ;
#22848=EDGE_CURVE ( 'NONE', #29316, #57242, #5997, .T. ) ;
#22852=ORIENTED_EDGE ( 'NONE', *, *, #44259, .T. ) ;
#22853=ORIENTED_EDGE ( 'NONE', *, *, #55443, .F. ) ;
#22854=ORIENTED_EDGE ( 'NONE', *, *, #21755, .F. ) ;
#22869=ORIENTED_EDGE ( 'NONE', *, *, #55273, .T. ) ;
#22878=DIRECTION ( 'NONE',  ( -1.000000000000000000, -0.000000000000000000, 0.000000000000000000 ) ) ;
#22882=CARTESIAN_POINT ( 'NONE',  ( 5.999999999999999112, -59.75363087400114637, 56.15606465354937171 ) ) ;
#22884=ADVANCED_FACE ( 'NONE', ( #63142 ), #17623, .T. ) ;
#22887=ORIENTED_EDGE ( 'NONE', *, *, #28004, .T. ) ;
#22888=FACE_BOUND ( 'NONE', #24321, .T. ) ;
#22899=AXIS2_PLACEMENT_3D ( 'NONE', #22907, #16137, #5251 ) ;
#22900=CARTESIAN_POINT ( 'NONE',  ( 0.000000000000000000, -62.20884554314051229, 46.21855187248609553 ) ) ;
#22901=CIRCLE ( 'NONE', #19276, 82.00000000000000000 ) ;
#22906=DIRECTION ( 'NONE',  ( 0.000000000000000000, 0.000000000000000000, 1.000000000000000000 ) ) ;
#22907=CARTESIAN_POINT ( 'NONE',  ( 11.99999999999999822, -41.76937507738831812, 62.50329211542423025 ) ) ;
#22909=CARTESIAN_POINT ( 'NONE',  ( 11.99999999999999822, 16.65972982745045528, -80.28980883073741381 ) ) ;
#22919=DIRECTION ( 'NONE',  ( -1.000000000000000000, 0.000000000000000000, -0.000000000000000000 ) ) ;
#22922=EDGE_CURVE ( 'NONE', #62534, #12399, #11078, .T. ) ;
#22925=ORIENTED_EDGE ( 'NONE', *, *, #29551, .F. ) ;
#22926=CYLINDRICAL_SURFACE ( 'NONE', #55157, 31.99999999999998579 ) ;
#22935=CARTESIAN_POINT ( 'NONE',  ( 0.000000000000000000, -5.256550761632340141, -77.32052557432847095 ) ) ;
#22936=ORIENTED_EDGE ( 'NONE', *, *, #23838, .T. ) ;
#22942=AXIS2_PLACEMENT_3D ( 'NONE', #37760, #31728, #32097 ) ;
#22946=AXIS2_PLACEMENT_3D ( 'NONE', #9565, #31375, #3948 ) ;
#22958=DIRECTION ( 'NONE',  ( 0.000000000000000000, -0.3090169943749350168, -0.9510565162951576390 ) ) ;
#22959=EDGE_CURVE ( 'NONE', #52520, #48721, #46567, .T. ) ;
#22968=AXIS2_PLACEMENT_3D ( 'NONE', #13056, #58942, #42020 ) ;
#22973=DIRECTION ( 'NONE',  ( -1.000000000000000000, -0.000000000000000000, 0.000000000000000000 ) ) ;
#22975=EDGE_LOOP ( 'NONE', ( #43942, #67727, #43001, #70809 ) ) ;
#22976=LINE ( 'NONE', #45907, #39486 ) ;
#22985=CYLINDRICAL_SURFACE ( 'NONE', #42279, 82.00000000000000000 ) ;
#22992=CARTESIAN_POINT ( 'NONE',  ( 12.00000000000000000, 20.85821328998756385, 10.92862929874494249 ) ) ;
#22993=CARTESIAN_POINT ( 'NONE',  ( 0.000000000000000000, -59.03342792756297541, 46.54456581323783126 ) ) ;
#23009=ORIENTED_EDGE ( 'NONE', *, *, #6471, .F. ) ;
#23013=EDGE_CURVE ( 'NONE', #9893, #21904, #7472, .T. ) ;
#23014=FACE_OUTER_BOUND ( 'NONE', #40043, .T. ) ;
#23015=EDGE_CURVE ( 'NONE', #13138, #54220, #17089, .T. ) ;
#23020=ORIENTED_EDGE ( 'NONE', *, *, #5196, .T. ) ;
#23026=ORIENTED_EDGE ( 'NONE', *, *, #64604, .F. ) ;
#23036=CARTESIAN_POINT ( 'NONE',  ( 11.99999999999999822, -81.50828551894220197, -8.966570791701590437 ) ) ;
#23044=EDGE_LOOP ( 'NONE', ( #56034, #59547, #34674, #12365 ) ) ;
#23046=ORIENTED_EDGE ( 'NONE', *, *, #52008, .T. ) ;
#23052=AXIS2_PLACEMENT_3D ( 'NONE', #38330, #22157, #72523 ) ;
#23068=DIRECTION ( 'NONE',  ( -1.000000000000000000, -0.000000000000000000, 0.000000000000000000 ) ) ;
#23072=DIRECTION ( 'NONE',  ( -1.000000000000000000, 0.000000000000000000, 0.000000000000000000 ) ) ;
#23073=DIRECTION ( 'NONE',  ( 0.000000000000000000, 0.000000000000000000, 1.000000000000000000 ) ) ;
#23078=AXIS2_PLACEMENT_3D ( 'NONE', #70786, #18550, #40759 ) ;
#23081=CARTESIAN_POINT ( 'NONE',  ( 11.99999999999999822, 71.21200624218852226, -40.65526001592539984 ) ) ;
#23089=EDGE_CURVE ( 'NONE', #32106, #67992, #1488, .T. ) ;
#23113=EDGE_CURVE ( 'NONE', #25431, #15633, #67533, .T. ) ;
#23119=ORIENTED_EDGE ( 'NONE', *, *, #35573, .F. ) ;
#23122=ADVANCED_FACE ( 'NONE', ( #29125 ), #64100, .T. ) ;
#23123=AXIS2_PLACEMENT_3D ( 'NONE', #1933, #25556, #29702 ) ;
#23135=VERTEX_POINT ( 'NONE', #24248 ) ;
#23157=LINE ( 'NONE', #18242, #66260 ) ;
#23168=CARTESIAN_POINT ( 'NONE',  ( 0.000000000000000000, -29.01471420065616513, 76.69515212746007649 ) ) ;
#23178=FACE_OUTER_BOUND ( 'NONE', #12772, .T. ) ;
#23180=DIRECTION ( 'NONE',  ( 0.000000000000000000, -0.9510565162951503115, 0.3090169943749573878 ) ) ;
#23182=LINE ( 'NONE', #73180, #28932 ) ;
#23185=DIRECTION ( 'NONE',  ( 0.000000000000000000, -0.4539904997395542430, 0.8910065241883641241 ) ) ;
#23193=EDGE_CURVE ( 'NONE', #46802, #50648, #62787, .T. ) ;
#23197=DIRECTION ( 'NONE',  ( 0.000000000000000000, 0.000000000000000000, 1.000000000000000000 ) ) ;
#23202=EDGE_CURVE ( 'NONE', #31895, #24576, #72350, .T. ) ;
#23206=VECTOR ( 'NONE', #25142, 1000.000000000000000 ) ;
#23208=ORIENTED_EDGE ( 'NONE', *, *, #46269, .F. ) ;
#23212=DIRECTION ( 'NONE',  ( -1.000000000000000000, 0.000000000000000000, 0.000000000000000000 ) ) ;
#23217=CARTESIAN_POINT ( 'NONE',  ( 11.99999999999999822, 65.64334221924909230, 41.19522573413756561 ) ) ;
#23220=AXIS2_PLACEMENT_3D ( 'NONE', #5488, #45713, #57341 ) ;
#23221=ORIENTED_EDGE ( 'NONE', *, *, #3324, .T. ) ;
#23233=VERTEX_POINT ( 'NONE', #35145 ) ;
#23235=ORIENTED_EDGE ( 'NONE', *, *, #45450, .T. ) ;
#23243=LINE ( 'NONE', #712, #55128 ) ;
#23247=ORIENTED_EDGE ( 'NONE', *, *, #46280, .T. ) ;
#23249=PLANE ( 'NONE',  #20532 ) ;
#23256=CARTESIAN_POINT ( 'NONE',  ( 5.999999999999999112, 77.16300072079660310, 27.74655509720697211 ) ) ;
#23257=CARTESIAN_POINT ( 'NONE',  ( 11.99999999999999822, 0.000000000000000000, 0.000000000000000000 ) ) ;
#23261=ADVANCED_FACE ( 'NONE', ( #6584 ), #42284, .T. ) ;
#23270=CARTESIAN_POINT ( 'NONE',  ( 11.99999999999999822, 36.73666225445894185, 65.58780272294090707 ) ) ;
#23275=AXIS2_PLACEMENT_3D ( 'NONE', #7212, #24498, #30129 ) ;
#23279=CARTESIAN_POINT ( 'NONE',  ( 0.000000000000000000, -73.73191006444582740, 14.66109333815435889 ) ) ;
#23281=DIRECTION ( 'NONE',  ( 0.000000000000000000, 0.000000000000000000, 1.000000000000000000 ) ) ;
#23287=CARTESIAN_POINT ( 'NONE',  ( 11.99999999999999822, 20.41045688087930898, -72.35160999960793049 ) ) ;
#23289=CIRCLE ( 'NONE', #68901, 77.49899999999999523 ) ;
#23290=FACE_OUTER_BOUND ( 'NONE', #6557, .T. ) ;
#23316=DIRECTION ( 'NONE',  ( -1.000000000000000000, 0.000000000000000000, 0.000000000000000000 ) ) ;
#23321=ORIENTED_EDGE ( 'NONE', *, *, #2328, .F. ) ;
#23323=VERTEX_POINT ( 'NONE', #59193 ) ;
#23337=VECTOR ( 'NONE', #64399, 1000.000000000000000 ) ;
#23338=EDGE_CURVE ( 'NONE', #2660, #54637, #37383, .T. ) ;
#23343=VERTEX_POINT ( 'NONE', #43017 ) ;
#23350=CARTESIAN_POINT ( 'NONE',  ( -10.00000000000000000, 0.000000000000000000, 0.000000000000000000 ) ) ;
#23353=CARTESIAN_POINT ( 'NONE',  ( 11.99999999999999822, 0.000000000000000000, 0.000000000000000000 ) ) ;
#23363=CARTESIAN_POINT ( 'NONE',  ( 11.99999999999999822, 0.000000000000000000, 0.000000000000000000 ) ) ;
#23364=CARTESIAN_POINT ( 'NONE',  ( 0.000000000000000000, 0.000000000000000000, 0.000000000000000000 ) ) ;
#23371=CARTESIAN_POINT ( 'NONE',  ( 11.99999999999999822, 35.91791733033570466, -68.67312586194960033 ) ) ;
#23373=VECTOR ( 'NONE', #63821, 999.9999999999998863 ) ;
#23378=CARTESIAN_POINT ( 'NONE',  ( 15.00000000000000000, -22.67460108101774452, 6.353146135318220367 ) ) ;
#23383=EDGE_LOOP ( 'NONE', ( #62806, #3991, #53794, #22936 ) ) ;
#23395=VERTEX_POINT ( 'NONE', #50552 ) ;
#23407=ORIENTED_EDGE ( 'NONE', *, *, #24015, .T. ) ;
#23422=ORIENTED_EDGE ( 'NONE', *, *, #48564, .T. ) ;
#23429=CARTESIAN_POINT ( 'NONE',  ( 0.000000000000000000, 0.000000000000000000, 0.000000000000000000 ) ) ;
#23462=DIRECTION ( 'NONE',  ( 0.000000000000000000, 0.000000000000000000, 1.000000000000000000 ) ) ;
#23464=LINE ( 'NONE', #6907, #47314 ) ;
#23480=VERTEX_POINT ( 'NONE', #22365 ) ;
#23488=ORIENTED_EDGE ( 'NONE', *, *, #60170, .T. ) ;
#23491=ORIENTED_EDGE ( 'NONE', *, *, #839, .F. ) ;
#23528=ADVANCED_FACE ( 'NONE', ( #71164 ), #12916, .T. ) ;
#23531=DIRECTION ( 'NONE',  ( -1.000000000000000000, 0.000000000000000000, -0.000000000000000000 ) ) ;
#23539=AXIS2_PLACEMENT_3D ( 'NONE', #12153, #28331, #57670 ) ;
#23542=FACE_OUTER_BOUND ( 'NONE', #6042, .T. ) ;
#23550=CARTESIAN_POINT ( 'NONE',  ( 12.00000000000000000, -26.23277895567251861, -4.042438405569750870 ) ) ;
#23551=VERTEX_POINT ( 'NONE', #42254 ) ;
#23552=CARTESIAN_POINT ( 'NONE',  ( 11.99999999999999822, -18.89407956138204980, -75.16055320797050854 ) ) ;
#23563=VERTEX_POINT ( 'NONE', #58798 ) ;
#23566=CARTESIAN_POINT ( 'NONE',  ( 11.99999999999999822, -39.47590169984795239, -71.87247863392457248 ) ) ;
#23570=VECTOR ( 'NONE', #51534, 1000.000000000000000 ) ;
#23576=ORIENTED_EDGE ( 'NONE', *, *, #51159, .F. ) ;
#23579=ADVANCED_FACE ( 'NONE', ( #65188 ), #2440, .T. ) ;
#23584=VECTOR ( 'NONE', #48731, 1000.000000000000000 ) ;
#23592=DIRECTION ( 'NONE',  ( 0.000000000000000000, 0.9945218953682732899, -0.1045284632676548031 ) ) ;
#23597=EDGE_CURVE ( 'NONE', #37377, #36873, #42360, .T. ) ;
#23600=EDGE_LOOP ( 'NONE', ( #3172, #59014, #40426, #56720 ) ) ;
#23603=CARTESIAN_POINT ( 'NONE',  ( 11.99999999999999822, 0.000000000000000000, 0.000000000000000000 ) ) ;
#23605=DIRECTION ( 'NONE',  ( -1.000000000000000000, -0.000000000000000000, -0.000000000000000000 ) ) ;
#23618=ORIENTED_EDGE ( 'NONE', *, *, #44288, .F. ) ;
#23619=LINE ( 'NONE', #23256, #20669 ) ;
#23621=EDGE_CURVE ( 'NONE', #28446, #40627, #38759, .T. ) ;
#23622=ORIENTED_EDGE ( 'NONE', *, *, #52531, .T. ) ;
#23625=EDGE_CURVE ( 'NONE', #19963, #30236, #24380, .T. ) ;
#23640=FACE_OUTER_BOUND ( 'NONE', #40690, .T. ) ;
#23652=CIRCLE ( 'NONE', #2066, 31.99999999999998579 ) ;
#23664=ORIENTED_EDGE ( 'NONE', *, *, #23754, .T. ) ;
#23678=DIRECTION ( 'NONE',  ( -1.000000000000000000, -0.000000000000000000, 0.000000000000000000 ) ) ;
#23681=CIRCLE ( 'NONE', #20080, 82.00000000000000000 ) ;
#23689=AXIS2_PLACEMENT_3D ( 'NONE', #68471, #73712, #22224 ) ;
#23702=CARTESIAN_POINT ( 'NONE',  ( 0.000000000000000000, -46.21855187248585395, -62.20884554314068993 ) ) ;
#23707=LINE ( 'NONE', #59043, #42756 ) ;
#23708=ADVANCED_FACE ( 'NONE', ( #48622 ), #32424, .T. ) ;
#23709=EDGE_CURVE ( 'NONE', #13504, #65473, #20780, .T. ) ;
#23731=DIRECTION ( 'NONE',  ( -1.000000000000000000, 0.000000000000000000, 0.000000000000000000 ) ) ;
#23736=DIRECTION ( 'NONE',  ( 0.000000000000000000, 0.000000000000000000, 1.000000000000000000 ) ) ;
#23746=ADVANCED_FACE ( 'NONE', ( #66654 ), #8771, .T. ) ;
#23754=EDGE_CURVE ( 'NONE', #63641, #13981, #17188, .T. ) ;
#23770=EDGE_CURVE ( 'NONE', #30840, #26458, #15134, .T. ) ;
#23772=VERTEX_POINT ( 'NONE', #9872 ) ;
#23773=ORIENTED_EDGE ( 'NONE', *, *, #53370, .T. ) ;
#23785=EDGE_CURVE ( 'NONE', #9630, #4678, #26773, .T. ) ;
#23786=ORIENTED_EDGE ( 'NONE', *, *, #20727, .F. ) ;
#23794=CIRCLE ( 'NONE', #32142, 31.99999999999998224 ) ;
#23795=LINE ( 'NONE', #18152, #733 ) ;
#23809=CARTESIAN_POINT ( 'NONE',  ( 11.99999999999999822, -68.55367621811173251, 44.99326035066031437 ) ) ;
#23813=CARTESIAN_POINT ( 'NONE',  ( 0.000000000000000000, 34.44570377933598593, 69.42325613327452061 ) ) ;
#23815=AXIS2_PLACEMENT_3D ( 'NONE', #42915, #30137, #65843 ) ;
#23823=CIRCLE ( 'NONE', #73003, 82.00000000000000000 ) ;
#23837=ORIENTED_EDGE ( 'NONE', *, *, #69365, .F. ) ;
#23838=EDGE_CURVE ( 'NONE', #59443, #12497, #63899, .T. ) ;
#23840=ORIENTED_EDGE ( 'NONE', *, *, #54491, .F. ) ;
#23841=AXIS2_PLACEMENT_3D ( 'NONE', #29948, #45796, #52146 ) ;
#23844=CIRCLE ( 'NONE', #33432, 82.00000000000000000 ) ;
#23845=EDGE_CURVE ( 'NONE', #20436, #29463, #1145, .T. ) ;
#23848=ORIENTED_EDGE ( 'NONE', *, *, #66878, .T. ) ;
#23850=CIRCLE ( 'NONE', #35855, 82.00000000000000000 ) ;
#23854=ORIENTED_EDGE ( 'NONE', *, *, #62423, .F. ) ;
#23856=DIRECTION ( 'NONE',  ( -1.000000000000000000, -0.000000000000000000, -0.000000000000000000 ) ) ;
#23857=EDGE_CURVE ( 'NONE', #54220, #27635, #3998, .T. ) ;
#23860=AXIS2_PLACEMENT_3D ( 'NONE', #61461, #9578, #72703 ) ;
#23863=ORIENTED_EDGE ( 'NONE', *, *, #63417, .F. ) ;
#23869=CARTESIAN_POINT ( 'NONE',  ( 0.000000000000000000, 73.72996012237460661, -14.67089635893632504 ) ) ;
#23873=AXIS2_PLACEMENT_3D ( 'NONE', #27066, #20699, #72917 ) ;
#23876=ORIENTED_EDGE ( 'NONE', *, *, #52866, .F. ) ;
#23879=ORIENTED_EDGE ( 'NONE', *, *, #72375, .T. ) ;
#23882=ORIENTED_EDGE ( 'NONE', *, *, #56037, .T. ) ;
#23890=CARTESIAN_POINT ( 'NONE',  ( 0.000000000000000000, -68.67312586195022561, 35.91791733033451806 ) ) ;
#23905=FACE_OUTER_BOUND ( 'NONE', #10187, .T. ) ;
#23911=FACE_OUTER_BOUND ( 'NONE', #55679, .T. ) ;
#23913=CARTESIAN_POINT ( 'NONE',  ( 0.000000000000000000, 0.000000000000000000, 0.000000000000000000 ) ) ;
#23918=CIRCLE ( 'NONE', #1148, 31.99999999999998224 ) ;
#23927=CIRCLE ( 'NONE', #3548, 31.99999999999998579 ) ;
#23929=EDGE_CURVE ( 'NONE', #6219, #28446, #51864, .T. ) ;
#23934=ORIENTED_EDGE ( 'NONE', *, *, #66976, .T. ) ;
#23937=ADVANCED_FACE ( 'NONE', ( #19485 ), #65733, .T. ) ;
#23938=CARTESIAN_POINT ( 'NONE',  ( 11.99999999999999822, 77.32052557432849937, -5.256550761632002633 ) ) ;
#23946=LINE ( 'NONE', #22847, #73484 ) ;
#23954=ORIENTED_EDGE ( 'NONE', *, *, #39567, .T. ) ;
#23967=FACE_OUTER_BOUND ( 'NONE', #43123, .T. ) ;
#23969=ADVANCED_FACE ( 'NONE', ( #30759 ), #72100, .F. ) ;
#23970=CARTESIAN_POINT ( 'NONE',  ( 11.99999999999999822, -12.93880638057260946, -76.41127070299286572 ) ) ;
#23976=DIRECTION ( 'NONE',  ( 0.000000000000000000, 0.000000000000000000, 1.000000000000000000 ) ) ;
#23980=CARTESIAN_POINT ( 'NONE',  ( 11.99999999999999822, 70.52718814184260054, 26.02418014898334420 ) ) ;
#23981=ORIENTED_EDGE ( 'NONE', *, *, #32237, .T. ) ;
#23982=LINE ( 'NONE', #22502, #73536 ) ;
#23987=ORIENTED_EDGE ( 'NONE', *, *, #59502, .F. ) ;
#24005=DIRECTION ( 'NONE',  ( 0.000000000000000000, 0.000000000000000000, 1.000000000000000000 ) ) ;
#24007=CARTESIAN_POINT ( 'NONE',  ( 11.99999999999999822, -6.903761155838323837, 77.19088730480521576 ) ) ;
#24011=CARTESIAN_POINT ( 'NONE',  ( 11.99999999999999822, -63.18004540533059554, 44.88180994100355292 ) ) ;
#24013=CYLINDRICAL_SURFACE ( 'NONE', #13227, 31.99999999999998579 ) ;
#24014=CIRCLE ( 'NONE', #64801, 77.49900000000000944 ) ;
#24015=EDGE_CURVE ( 'NONE', #55862, #34944, #12400, .T. ) ;
#24017=AXIS2_PLACEMENT_3D ( 'NONE', #26484, #9566, #32486 ) ;
#24020=EDGE_CURVE ( 'NONE', #15645, #27772, #55188, .T. ) ;
#24024=ORIENTED_EDGE ( 'NONE', *, *, #64536, .F. ) ;
#24029=EDGE_CURVE ( 'NONE', #9630, #30413, #49173, .T. ) ;
#24038=VECTOR ( 'NONE', #49707, 1000.000000000000000 ) ;
#24047=ORIENTED_EDGE ( 'NONE', *, *, #11353, .F. ) ;
#24055=DIRECTION ( 'NONE',  ( 0.000000000000000000, 0.000000000000000000, 1.000000000000000000 ) ) ;
#24056=ORIENTED_EDGE ( 'NONE', *, *, #33586, .F. ) ;
#24057=FACE_OUTER_BOUND ( 'NONE', #17635, .T. ) ;
#24065=ORIENTED_EDGE ( 'NONE', *, *, #61283, .T. ) ;
#24066=DIRECTION ( 'NONE',  ( -1.000000000000000000, 0.000000000000000000, 0.000000000000000000 ) ) ;
#24069=EDGE_CURVE ( 'NONE', #50948, #6766, #56802, .T. ) ;
#24080=DIRECTION ( 'NONE',  ( 0.000000000000000000, 0.000000000000000000, 1.000000000000000000 ) ) ;
#24091=DIRECTION ( 'NONE',  ( 0.000000000000000000, 0.000000000000000000, -1.000000000000000000 ) ) ;
#24094=DIRECTION ( 'NONE',  ( 0.000000000000000000, 0.000000000000000000, -1.000000000000000000 ) ) ;
#24095=VECTOR ( 'NONE', #71386, 1000.000000000000000 ) ;
#24098=CIRCLE ( 'NONE', #56507, 31.99999999999998579 ) ;
#24108=DIRECTION ( 'NONE',  ( -1.000000000000000000, 0.000000000000000000, 0.000000000000000000 ) ) ;
#24118=VERTEX_POINT ( 'NONE', #21713 ) ;
#24130=VERTEX_POINT ( 'NONE', #33352 ) ;
#24133=ORIENTED_EDGE ( 'NONE', *, *, #67756, .T. ) ;
#24140=EDGE_CURVE ( 'NONE', #10445, #21534, #16828, .T. ) ;
#24159=FACE_OUTER_BOUND ( 'NONE', #58621, .T. ) ;
#24160=CARTESIAN_POINT ( 'NONE',  ( 11.99999999999999822, -74.74816331893404708, -33.71516098798819172 ) ) ;
#24174=CARTESIAN_POINT ( 'NONE',  ( 15.00000000000000000, -1.278221433540145391, 26.51162292216073979 ) ) ;
#24175=STYLED_ITEM ( 'NONE', ( #18180 ), #58845 ) ;
#24187=DIRECTION ( 'NONE',  ( -1.000000000000000000, 0.000000000000000000, 0.000000000000000000 ) ) ;
#24191=VERTEX_POINT ( 'NONE', #22092 ) ;
#24192=CARTESIAN_POINT ( 'NONE',  ( 11.99999999999999822, 0.000000000000000000, 0.000000000000000000 ) ) ;
#24194=ADVANCED_FACE ( 'NONE', ( #26974 ), #61207, .T. ) ;
#24200=DIRECTION ( 'NONE',  ( -1.000000000000000000, 0.000000000000000000, 0.000000000000000000 ) ) ;
#24203=AXIS2_PLACEMENT_3D ( 'NONE', #35563, #70878, #64150 ) ;
#24205=DIRECTION ( 'NONE',  ( -1.000000000000000000, 0.000000000000000000, -0.000000000000000000 ) ) ;
#24213=DIRECTION ( 'NONE',  ( -1.000000000000000000, 0.000000000000000000, 0.000000000000000000 ) ) ;
#24214=FACE_OUTER_BOUND ( 'NONE', #63098, .T. ) ;
#24225=CIRCLE ( 'NONE', #72175, 82.00000000000000000 ) ;
#24227=ADVANCED_FACE ( 'NONE', ( #70154 ), #1431, .T. ) ;
#24230=VERTEX_POINT ( 'NONE', #69795 ) ;
#24233=DIRECTION ( 'NONE',  ( 0.000000000000000000, -0.2334453638559126909, 0.9723699203976748917 ) ) ;
#24248=CARTESIAN_POINT ( 'NONE',  ( 0.000000000000000000, -2.543863470248951320, 81.96053171279901051 ) ) ;
#24250=DIRECTION ( 'NONE',  ( 1.000000000000000000, 0.000000000000000000, 0.000000000000000000 ) ) ;
#24254=ORIENTED_EDGE ( 'NONE', *, *, #12629, .T. ) ;
#24255=CARTESIAN_POINT ( 'NONE',  ( 0.000000000000000000, 71.91182617369187824, 28.89263327155770256 ) ) ;
#24263=DIRECTION ( 'NONE',  ( 1.000000000000000000, -0.000000000000000000, -0.000000000000000000 ) ) ;
#24268=VERTEX_POINT ( 'NONE', #682 ) ;
#24272=DIRECTION ( 'NONE',  ( -1.000000000000000000, 0.000000000000000000, 0.000000000000000000 ) ) ;
#24278=ADVANCED_FACE ( 'NONE', ( #41596 ), #40491, .T. ) ;
#24280=LINE ( 'NONE', #63397, #6688 ) ;
#24288=LINE ( 'NONE', #41947, #56545 ) ;
#24290=CYLINDRICAL_SURFACE ( 'NONE', #38856, 31.99999999999998579 ) ;
#24291=CARTESIAN_POINT ( 'NONE',  ( 0.000000000000000000, 74.65491531819118620, -8.830959090342659579 ) ) ;
#24293=ADVANCED_FACE ( 'NONE', ( #52498 ), #1055, .T. ) ;
#24297=ORIENTED_EDGE ( 'NONE', *, *, #44165, .F. ) ;
#24320=ORIENTED_EDGE ( 'NONE', *, *, #51631, .F. ) ;
#24321=EDGE_LOOP ( 'NONE', ( #23863, #32508, #8878, #64545 ) ) ;
#24322=ORIENTED_EDGE ( 'NONE', *, *, #60782, .F. ) ;
#24327=DIRECTION ( 'NONE',  ( -1.000000000000000000, 0.000000000000000000, 0.000000000000000000 ) ) ;
#24333=EDGE_CURVE ( 'NONE', #74276, #19944, #47987, .T. ) ;
#24335=CARTESIAN_POINT ( 'NONE',  ( 15.00000000000000000, -1.278221433540507546, -26.51162292216071492 ) ) ;
#24338=AXIS2_PLACEMENT_3D ( 'NONE', #32980, #55927, #73575 ) ;
#24340=VERTEX_POINT ( 'NONE', #71261 ) ;
#24346=DIRECTION ( 'NONE',  ( -1.000000000000000000, -0.000000000000000000, -0.000000000000000000 ) ) ;
#24347=AXIS2_PLACEMENT_3D ( 'NONE', #70660, #62574, #33976 ) ;
#24348=CIRCLE ( 'NONE', #56769, 77.49899999999999523 ) ;
#24352=EDGE_CURVE ( 'NONE', #54048, #8287, #70080, .T. ) ;
#24372=DIRECTION ( 'NONE',  ( -1.000000000000000000, -0.000000000000000000, 0.000000000000000000 ) ) ;
#24377=LINE ( 'NONE', #41658, #62588 ) ;
#24380=CIRCLE ( 'NONE', #38812, 31.99999999999998579 ) ;
#24385=CARTESIAN_POINT ( 'NONE',  ( 0.000000000000000000, 62.50884508063487033, -41.76106447765422303 ) ) ;
#24386=EDGE_CURVE ( 'NONE', #47511, #73508, #42715, .T. ) ;
#24390=LINE ( 'NONE', #13098, #41661 ) ;
#24391=AXIS2_PLACEMENT_3D ( 'NONE', #60890, #15381, #31193 ) ;
#24395=EDGE_LOOP ( 'NONE', ( #49523, #3085, #71543, #34339 ) ) ;
#24398=CARTESIAN_POINT ( 'NONE',  ( 6.000000000000000000, -3.894527615418457600, 81.90746397400387480 ) ) ;
#24401=EDGE_LOOP ( 'NONE', ( #45036, #51770, #5667, #37065 ) ) ;
#24402=LINE ( 'NONE', #47337, #68381 ) ;
#24414=ADVANCED_FACE ( 'NONE', ( #65286 ), #60021, .T. ) ;
#24436=VECTOR ( 'NONE', #45133, 1000.000000000000000 ) ;
#24445=DIRECTION ( 'NONE',  ( 0.000000000000000000, 0.000000000000000000, 1.000000000000000000 ) ) ;
#24449=AXIS2_PLACEMENT_3D ( 'NONE', #35550, #52467, #23180 ) ;
#24451=DIRECTION ( 'NONE',  ( -1.000000000000000000, -0.000000000000000000, -0.000000000000000000 ) ) ;
#24453=CARTESIAN_POINT ( 'NONE',  ( -10.00000000000000000, 0.000000000000000000, 0.000000000000000000 ) ) ;
#24458=DIRECTION ( 'NONE',  ( 0.000000000000000000, 0.6494480483301793283, 0.7604059656000345946 ) ) ;
#24459=EDGE_CURVE ( 'NONE', #12324, #31904, #22375, .T. ) ;
#24464=EDGE_CURVE ( 'NONE', #30036, #72747, #62883, .T. ) ;
#24472=EDGE_CURVE ( 'NONE', #34276, #67063, #4059, .T. ) ;
#24482=CARTESIAN_POINT ( 'NONE',  ( 0.000000000000000000, 74.74816331893430288, 33.71516098798768724 ) ) ;
#24483=DIRECTION ( 'NONE',  ( -1.000000000000000000, -0.000000000000000000, 0.000000000000000000 ) ) ;
#24493=VERTEX_POINT ( 'NONE', #61122 ) ;
#24497=VERTEX_POINT ( 'NONE', #4738 ) ;
#24498=DIRECTION ( 'NONE',  ( -1.000000000000000000, 0.000000000000000000, -0.000000000000000000 ) ) ;
#24499=ORIENTED_EDGE ( 'NONE', *, *, #52201, .T. ) ;
#24506=ORIENTED_EDGE ( 'NONE', *, *, #27304, .F. ) ;
#24508=EDGE_CURVE ( 'NONE', #39310, #29971, #40047, .T. ) ;
#24510=ORIENTED_EDGE ( 'NONE', *, *, #55094, .F. ) ;
#24517=CARTESIAN_POINT ( 'NONE',  ( 15.00000000000000000, -3.948201729842355068, -23.21447184625292692 ) ) ;
#24519=ADVANCED_FACE ( 'NONE', ( #38557 ), #39678, .T. ) ;
#24530=CYLINDRICAL_SURFACE ( 'NONE', #36181, 77.49899999999999523 ) ;
#24541=CARTESIAN_POINT ( 'NONE',  ( 15.00000000000000000, -3.948201729842032215, 23.21447184625297666 ) ) ;
#24544=CARTESIAN_POINT ( 'NONE',  ( 0.000000000000000000, 16.65972982745045528, -80.28980883073738539 ) ) ;
#24547=CIRCLE ( 'NONE', #20881, 31.99999999999998579 ) ;
#24553=CIRCLE ( 'NONE', #11338, 82.00000000000000000 ) ;
#24555=AXIS2_PLACEMENT_3D ( 'NONE', #14857, #37803, #60735 ) ;
#24558=FACE_OUTER_BOUND ( 'NONE', #17923, .T. ) ;
#24569=DIRECTION ( 'NONE',  ( -1.000000000000000000, -0.000000000000000000, -0.000000000000000000 ) ) ;
#24573=LINE ( 'NONE', #35113, #28146 ) ;
#24576=VERTEX_POINT ( 'NONE', #13214 ) ;
#24577=CARTESIAN_POINT ( 'NONE',  ( 0.000000000000000000, 74.65491531819118620, -8.830959090342659579 ) ) ;
#24578=DIRECTION ( 'NONE',  ( 0.000000000000000000, 0.000000000000000000, 1.000000000000000000 ) ) ;
#24579=ORIENTED_EDGE ( 'NONE', *, *, #1796, .T. ) ;
#24581=ORIENTED_EDGE ( 'NONE', *, *, #36261, .F. ) ;
#24585=ORIENTED_EDGE ( 'NONE', *, *, #7550, .F. ) ;
#24587=CARTESIAN_POINT ( 'NONE',  ( 0.000000000000000000, 0.000000000000000000, 0.000000000000000000 ) ) ;
#24589=ORIENTED_EDGE ( 'NONE', *, *, #39240, .F. ) ;
#24591=CIRCLE ( 'NONE', #64221, 82.00000000000000000 ) ;
#24599=ORIENTED_EDGE ( 'NONE', *, *, #56192, .T. ) ;
#24618=CYLINDRICAL_SURFACE ( 'NONE', #17460, 31.99999999999998579 ) ;
#24625=DIRECTION ( 'NONE',  ( 0.000000000000000000, 0.000000000000000000, 1.000000000000000000 ) ) ;
#24627=VECTOR ( 'NONE', #11774, 1000.000000000000000 ) ;
#24628=VERTEX_POINT ( 'NONE', #7214 ) ;
#24629=ADVANCED_FACE ( 'NONE', ( #69626 ), #42176, .T. ) ;
#24631=LINE ( 'NONE', #51444, #35743 ) ;
#24633=CARTESIAN_POINT ( 'NONE',  ( 0.000000000000000000, 72.35160999960844208, -20.41045688087747223 ) ) ;
#24634=CYLINDRICAL_SURFACE ( 'NONE', #62564, 31.99999999999998579 ) ;
#24646=CARTESIAN_POINT ( 'NONE',  ( 12.00000000000000000, -22.32062822937488988, -14.36278369418800160 ) ) ;
#24667=DIRECTION ( 'NONE',  ( -1.000000000000000000, 0.000000000000000000, 0.000000000000000000 ) ) ;
#24670=ORIENTED_EDGE ( 'NONE', *, *, #58501, .F. ) ;
#24686=VERTEX_POINT ( 'NONE', #47437 ) ;
#24689=ADVANCED_FACE ( 'NONE', ( #36148 ), #59459, .T. ) ;
#24690=CARTESIAN_POINT ( 'NONE',  ( 11.99999999999999822, 68.67312586195046720, -35.91791733033404199 ) ) ;
#24697=VERTEX_POINT ( 'NONE', #47075 ) ;
#24701=EDGE_CURVE ( 'NONE', #38079, #22373, #25710, .T. ) ;
#24703=VECTOR ( 'NONE', #66341, 1000.000000000000114 ) ;
#24711=VECTOR ( 'NONE', #4655, 1000.000000000000000 ) ;
#24717=CARTESIAN_POINT ( 'NONE',  ( 11.99999999999999822, -46.54456581323762521, -59.03342792756313884 ) ) ;
#24722=DIRECTION ( 'NONE',  ( -1.000000000000000000, -0.000000000000000000, 0.000000000000000000 ) ) ;
#24733=DIRECTION ( 'NONE',  ( -1.000000000000000000, 0.000000000000000000, 0.000000000000000000 ) ) ;
#24744=CARTESIAN_POINT ( 'NONE',  ( 6.000000000000000000, -71.21200624218825226, 40.65526001592589722 ) ) ;
#24749=AXIS2_PLACEMENT_3D ( 'NONE', #23429, #18512, #64396 ) ;
#24751=EDGE_CURVE ( 'NONE', #66932, #55194, #53303, .T. ) ;
#24756=ADVANCED_FACE ( 'NONE', ( #2719 ), #72925, .T. ) ;
#24759=EDGE_CURVE ( 'NONE', #45705, #56648, #15429, .T. ) ;
#24773=DIRECTION ( 'NONE',  ( -1.000000000000000000, 0.000000000000000000, 0.000000000000000000 ) ) ;
#24775=CARTESIAN_POINT ( 'NONE',  ( -10.00000000000000000, 0.000000000000000000, 0.000000000000000000 ) ) ;
#24781=CARTESIAN_POINT ( 'NONE',  ( -10.00000000000000000, 0.000000000000000000, 0.000000000000000000 ) ) ;
#24794=VERTEX_POINT ( 'NONE', #8693 ) ;
#24795=ORIENTED_EDGE ( 'NONE', *, *, #47047, .T. ) ;
#24796=VERTEX_POINT ( 'NONE', #55292 ) ;
#24797=FACE_OUTER_BOUND ( 'NONE', #60289, .T. ) ;
#24808=ORIENTED_EDGE ( 'NONE', *, *, #6732, .F. ) ;
#24812=CARTESIAN_POINT ( 'NONE',  ( 5.999999999999999112, 81.96053171279902472, -2.543863470248677316 ) ) ;
#24820=CIRCLE ( 'NONE', #59608, 77.49899999999999523 ) ;
#24826=DIRECTION ( 'NONE',  ( 0.000000000000000000, 0.000000000000000000, 1.000000000000000000 ) ) ;
#24839=LINE ( 'NONE', #7560, #10557 ) ;
#24844=VERTEX_POINT ( 'NONE', #48901 ) ;
#24847=DIRECTION ( 'NONE',  ( -1.000000000000000000, -0.000000000000000000, 0.000000000000000000 ) ) ;
#24851=CARTESIAN_POINT ( 'NONE',  ( 11.99999999999999822, 0.000000000000000000, 0.000000000000000000 ) ) ;
#24852=VECTOR ( 'NONE', #57104, 1000.000000000000000 ) ;
#24854=CARTESIAN_POINT ( 'NONE',  ( 0.000000000000000000, 0.000000000000000000, 0.000000000000000000 ) ) ;
#24855=CIRCLE ( 'NONE', #34464, 31.99999999999998579 ) ;
#24856=EDGE_CURVE ( 'NONE', #359, #17023, #1713, .T. ) ;
#24861=ORIENTED_EDGE ( 'NONE', *, *, #16245, .F. ) ;
#24867=DIRECTION ( 'NONE',  ( -1.000000000000000000, 0.000000000000000000, -0.000000000000000000 ) ) ;
#24875=EDGE_CURVE ( 'NONE', #24493, #54754, #2943, .T. ) ;
#24877=ORIENTED_EDGE ( 'NONE', *, *, #39377, .T. ) ;
#24892=EDGE_CURVE ( 'NONE', #31231, #1337, #12513, .T. ) ;
#24893=EDGE_LOOP ( 'NONE', ( #43011, #73885, #51635, #22380 ) ) ;
#24896=ORIENTED_EDGE ( 'NONE', *, *, #47883, .F. ) ;
#24898=LINE ( 'NONE', #47825, #50349 ) ;
#24915=CARTESIAN_POINT ( 'NONE',  ( 0.000000000000000000, 46.21855187248719687, -62.20884554313968806 ) ) ;
#24919=VECTOR ( 'NONE', #22431, 1000.000000000000000 ) ;
#24928=DIRECTION ( 'NONE',  ( -1.000000000000000000, -0.000000000000000000, 0.000000000000000000 ) ) ;
#24943=FACE_OUTER_BOUND ( 'NONE', #29138, .T. ) ;
#24963=AXIS2_PLACEMENT_3D ( 'NONE', #57388, #34831, #68306 ) ;
#24975=DIRECTION ( 'NONE',  ( 0.000000000000000000, -0.9781476007338065770, -0.2079116908177544853 ) ) ;
#24984=CARTESIAN_POINT ( 'NONE',  ( 6.000000000000000000, -81.50828551894234408, 8.966570791700414489 ) ) ;
#24988=ADVANCED_FACE ( 'NONE', ( #24057 ), #17663, .T. ) ;
#25011=DIRECTION ( 'NONE',  ( 0.000000000000000000, -0.9781476007338041345, 0.2079116908177664480 ) ) ;
#25017=AXIS2_PLACEMENT_3D ( 'NONE', #24291, #41950, #18629 ) ;
#25021=CARTESIAN_POINT ( 'NONE',  ( 11.99999999999999822, 68.27212725128275395, -31.46837873495001503 ) ) ;
#25040=EDGE_LOOP ( 'NONE', ( #14208, #65406, #38920, #66038 ) ) ;
#25054=ORIENTED_EDGE ( 'NONE', *, *, #7562, .F. ) ;
#25058=EDGE_CURVE ( 'NONE', #22781, #21262, #8964, .T. ) ;
#25062=PLANE ( 'NONE',  #41895 ) ;
#25064=AXIS2_PLACEMENT_3D ( 'NONE', #48654, #14435, #14803 ) ;
#25067=CARTESIAN_POINT ( 'NONE',  ( 0.000000000000000000, 30.41916302227216562, -71.27951684757994144 ) ) ;
#25076=DIRECTION ( 'NONE',  ( 0.000000000000000000, 0.5224985647159440250, 0.8526401643540951758 ) ) ;
#25082=VERTEX_POINT ( 'NONE', #1528 ) ;
#25088=DIRECTION ( 'NONE',  ( 0.000000000000000000, -0.3826834323650772363, -0.9238795325112919565 ) ) ;
#25090=ORIENTED_EDGE ( 'NONE', *, *, #33926, .F. ) ;
#25104=DIRECTION ( 'NONE',  ( 0.000000000000000000, 0.7071067811865486830, -0.7071067811865463515 ) ) ;
#25110=DIRECTION ( 'NONE',  ( -1.000000000000000000, 0.000000000000000000, 0.000000000000000000 ) ) ;
#25131=AXIS2_PLACEMENT_3D ( 'NONE', #27322, #50258, #21693 ) ;
#25134=AXIS2_PLACEMENT_3D ( 'NONE', #49149, #21298, #2952 ) ;
#25142=DIRECTION ( 'NONE',  ( -1.000000000000000000, -0.000000000000000000, 0.000000000000000000 ) ) ;
#25155=DIRECTION ( 'NONE',  ( 0.000000000000000000, 0.000000000000000000, 1.000000000000000000 ) ) ;
#25161=VERTEX_POINT ( 'NONE', #66852 ) ;
#25162=DIRECTION ( 'NONE',  ( -1.000000000000000000, -0.000000000000000000, 0.000000000000000000 ) ) ;
#25174=ORIENTED_EDGE ( 'NONE', *, *, #28244, .F. ) ;
#25175=CARTESIAN_POINT ( 'NONE',  ( 15.00000000000000000, 23.49999999999999645, 1.499999999999995337 ) ) ;
#25207=CIRCLE ( 'NONE', #16790, 31.99999999999999289 ) ;
#25221=ORIENTED_EDGE ( 'NONE', *, *, #9424, .F. ) ;
#25225=CARTESIAN_POINT ( 'NONE',  ( 11.99999999999999822, 71.91182617369190666, 28.89263327155770966 ) ) ;
#25226=VERTEX_POINT ( 'NONE', #42816 ) ;
#25229=EDGE_CURVE ( 'NONE', #12729, #32190, #32944, .T. ) ;
#25230=CARTESIAN_POINT ( 'NONE',  ( 0.000000000000000000, -2.956366410620109519, -75.11725578898472122 ) ) ;
#25231=ORIENTED_EDGE ( 'NONE', *, *, #10078, .F. ) ;
#25236=ORIENTED_EDGE ( 'NONE', *, *, #62246, .T. ) ;
#25242=AXIS2_PLACEMENT_3D ( 'NONE', #50244, #37136, #9663 ) ;
#25246=AXIS2_PLACEMENT_3D ( 'NONE', #15353, #9344, #36805 ) ;
#25247=CARTESIAN_POINT ( 'NONE',  ( 11.99999999999999822, 50.95692526931414790, -58.39081064771693974 ) ) ;
#25248=ORIENTED_EDGE ( 'NONE', *, *, #50052, .F. ) ;
#25250=DIRECTION ( 'NONE',  ( -1.000000000000000000, 0.000000000000000000, 0.000000000000000000 ) ) ;
#25253=ORIENTED_EDGE ( 'NONE', *, *, #67536, .F. ) ;
#25254=DIRECTION ( 'NONE',  ( 0.000000000000000000, 0.7431448254773939111, 0.6691306063588584596 ) ) ;
#25266=DIRECTION ( 'NONE',  ( -1.000000000000000000, -0.000000000000000000, 0.000000000000000000 ) ) ;
#25268=CYLINDRICAL_SURFACE ( 'NONE', #66107, 77.49899999999999523 ) ;
#25270=CIRCLE ( 'NONE', #67285, 31.99999999999998224 ) ;
#25273=EDGE_CURVE ( 'NONE', #28106, #29672, #10141, .T. ) ;
#25276=EDGE_LOOP ( 'NONE', ( #41520, #72905, #44430, #27436 ) ) ;
#25283=LINE ( 'NONE', #53845, #39864 ) ;
#25286=ORIENTED_EDGE ( 'NONE', *, *, #10864, .T. ) ;
#25296=DIRECTION ( 'NONE',  ( -1.000000000000000000, 0.000000000000000000, 0.000000000000000000 ) ) ;
#25301=AXIS2_PLACEMENT_3D ( 'NONE', #46563, #74012, #4887 ) ;
#25306=DIRECTION ( 'NONE',  ( -1.000000000000000000, 0.000000000000000000, -0.000000000000000000 ) ) ;
#25311=CARTESIAN_POINT ( 'NONE',  ( 12.00000000000000355, 2.571758278209441661E-15, -21.00000000000000000 ) ) ;
#25317=CYLINDRICAL_SURFACE ( 'NONE', #49810, 82.00000000000000000 ) ;
#25319=AXIS2_PLACEMENT_3D ( 'NONE', #49943, #10852, #56732 ) ;
#25331=ORIENTED_EDGE ( 'NONE', *, *, #57576, .F. ) ;
#25336=FACE_OUTER_BOUND ( 'NONE', #62435, .T. ) ;
#25346=VECTOR ( 'NONE', #9174, 1000.000000000000000 ) ;
#25360=ADVANCED_FACE ( 'NONE', ( #73594 ), #22482, .T. ) ;
#25363=ORIENTED_EDGE ( 'NONE', *, *, #72624, .T. ) ;
#25368=DIRECTION ( 'NONE',  ( 1.000000000000000000, -0.000000000000000000, -0.000000000000000000 ) ) ;
#25370=CARTESIAN_POINT ( 'NONE',  ( 0.000000000000000000, 0.000000000000000000, 0.000000000000000000 ) ) ;
#25396=CARTESIAN_POINT ( 'NONE',  ( 15.00000000000000000, -1.278221433540507546, -26.51162292216071492 ) ) ;
#25403=CARTESIAN_POINT ( 'NONE',  ( 0.000000000000000000, -77.49459641780886443, -0.8261519478439277586 ) ) ;
#25408=VECTOR ( 'NONE', #18891, 1000.000000000000000 ) ;
#25412=EDGE_CURVE ( 'NONE', #10397, #3672, #47401, .T. ) ;
#25413=SURFACE_STYLE_USAGE ( .BOTH. , #34552 ) ;
#25416=EDGE_LOOP ( 'NONE', ( #54400, #14687, #7788, #13766 ) ) ;
#25421=ORIENTED_EDGE ( 'NONE', *, *, #69178, .F. ) ;
#25431=VERTEX_POINT ( 'NONE', #15724 ) ;
#25440=ORIENTED_EDGE ( 'NONE', *, *, #68708, .T. ) ;
#25449=CIRCLE ( 'NONE', #39846, 31.99999999999998579 ) ;
#25453=CARTESIAN_POINT ( 'NONE',  ( 11.99999999999999822, -73.73191006444582740, 14.66109333815435889 ) ) ;
#25459=CYLINDRICAL_SURFACE ( 'NONE', #22968, 77.49899999999999523 ) ;
#25461=VECTOR ( 'NONE', #66343, 1000.000000000000000 ) ;
#25468=ORIENTED_EDGE ( 'NONE', *, *, #32503, .T. ) ;
#25470=DIRECTION ( 'NONE',  ( -1.000000000000000000, -0.000000000000000000, 0.000000000000000000 ) ) ;
#25477=CARTESIAN_POINT ( 'NONE',  ( 11.99999999999999822, 0.000000000000000000, 0.000000000000000000 ) ) ;
#25478=LINE ( 'NONE', #48773, #25587 ) ;
#25480=CARTESIAN_POINT ( 'NONE',  ( 0.000000000000000000, -15.33399622253424432, -80.55351364060604169 ) ) ;
#25482=VERTEX_POINT ( 'NONE', #46516 ) ;
#25487=CARTESIAN_POINT ( 'NONE',  ( 15.00000000000000000, -0.9646360437372099028, 23.52805723605590771 ) ) ;
#25488=ADVANCED_FACE ( 'NONE', ( #35967 ), #12664, .F. ) ;
#25495=EDGE_LOOP ( 'NONE', ( #22110, #48078, #47725, #18392 ) ) ;
#25510=EDGE_LOOP ( 'NONE', ( #5425, #5752, #17678, #10387 ) ) ;
#25511=LINE ( 'NONE', #72475, #14171 ) ;
#25513=FACE_OUTER_BOUND ( 'NONE', #38261, .T. ) ;
#25514=ORIENTED_EDGE ( 'NONE', *, *, #7654, .F. ) ;
#25548=CARTESIAN_POINT ( 'NONE',  ( 11.99999999999999822, -77.32052557432837148, -5.256550761633681290 ) ) ;
#25556=DIRECTION ( 'NONE',  ( 1.000000000000000000, 0.000000000000000000, 0.000000000000000000 ) ) ;
#25566=DIRECTION ( 'NONE',  ( -1.000000000000000000, 0.000000000000000000, 0.000000000000000000 ) ) ;
#25568=CARTESIAN_POINT ( 'NONE',  ( 0.000000000000000000, 77.19088730480532945, -6.903761155836932062 ) ) ;
#25573=CYLINDRICAL_SURFACE ( 'NONE', #56315, 82.00000000000000000 ) ;
#25574=DIRECTION ( 'NONE',  ( -1.000000000000000000, 0.000000000000000000, -0.000000000000000000 ) ) ;
#25579=CARTESIAN_POINT ( 'NONE',  ( 11.99999999999999822, 0.000000000000000000, 0.000000000000000000 ) ) ;
#25580=DIRECTION ( 'NONE',  ( 0.000000000000000000, 0.000000000000000000, 1.000000000000000000 ) ) ;
#25587=VECTOR ( 'NONE', #24372, 1000.000000000000000 ) ;
#25593=VERTEX_POINT ( 'NONE', #37471 ) ;
#25600=VERTEX_POINT ( 'NONE', #48003 ) ;
#25602=CARTESIAN_POINT ( 'NONE',  ( 0.000000000000000000, -55.20638768913797634, 51.02545421589302777 ) ) ;
#25605=FACE_OUTER_BOUND ( 'NONE', #5239, .T. ) ;
#25610=CIRCLE ( 'NONE', #37647, 31.99999999999999289 ) ;
#25614=AXIS2_PLACEMENT_3D ( 'NONE', #18345, #41291, #52939 ) ;
#25619=CIRCLE ( 'NONE', #53265, 31.99999999999999645 ) ;
#25621=CARTESIAN_POINT ( 'NONE',  ( 15.00000000000000000, -11.95096189432345746, -23.69967320028757030 ) ) ;
#25643=CARTESIAN_POINT ( 'NONE',  ( 15.00000000000000000, -22.67460108101774452, 6.353146135318220367 ) ) ;
#25654=CARTESIAN_POINT ( 'NONE',  ( 11.99999999999999822, 70.53064760720278059, 26.01480285779964774 ) ) ;
#25675=VERTEX_POINT ( 'NONE', #72024 ) ;
#25676=CARTESIAN_POINT ( 'NONE',  ( 11.99999999999999822, -79.10210256391353312, -21.60688246758669706 ) ) ;
#25679=CIRCLE ( 'NONE', #56933, 82.00000000000000000 ) ;
#25698=ORIENTED_EDGE ( 'NONE', *, *, #46373, .F. ) ;
#25704=ORIENTED_EDGE ( 'NONE', *, *, #3499, .T. ) ;
#25706=VERTEX_POINT ( 'NONE', #14137 ) ;
#25707=VERTEX_POINT ( 'NONE', #48729 ) ;
#25710=CIRCLE ( 'NONE', #49685, 77.49899999999999523 ) ;
#25714=DIRECTION ( 'NONE',  ( 0.000000000000000000, 0.000000000000000000, 1.000000000000000000 ) ) ;
#25716=DIRECTION ( 'NONE',  ( -1.000000000000000000, 0.000000000000000000, 0.000000000000000000 ) ) ;
#25717=DIRECTION ( 'NONE',  ( -1.000000000000000000, -0.000000000000000000, 0.000000000000000000 ) ) ;
#25728=CARTESIAN_POINT ( 'NONE',  ( 11.99999999999999822, 0.000000000000000000, 0.000000000000000000 ) ) ;
#25731=ORIENTED_EDGE ( 'NONE', *, *, #20696, .T. ) ;
#25732=AXIS2_PLACEMENT_3D ( 'NONE', #71602, #37425, #43061 ) ;
#25735=CARTESIAN_POINT ( 'NONE',  ( 0.000000000000000000, 0.000000000000000000, 0.000000000000000000 ) ) ;
#25737=ORIENTED_EDGE ( 'NONE', *, *, #23709, .T. ) ;
#25738=ADVANCED_FACE ( 'NONE', ( #66766 ), #36707, .T. ) ;
#25745=DIRECTION ( 'NONE',  ( 0.000000000000000000, -0.7604059656000226042, -0.6494480483301934282 ) ) ;
#25754=FACE_OUTER_BOUND ( 'NONE', #33309, .T. ) ;
#25763=FACE_OUTER_BOUND ( 'NONE', #4720, .T. ) ;
#25772=LINE ( 'NONE', #18007, #9481 ) ;
#25777=ADVANCED_FACE ( 'NONE', ( #38191 ), #16755, .T. ) ;
#25801=LINE ( 'NONE', #72397, #23584 ) ;
#25807=ORIENTED_EDGE ( 'NONE', *, *, #16442, .T. ) ;
#25818=LINE ( 'NONE', #48016, #67540 ) ;
#25819=CARTESIAN_POINT ( 'NONE',  ( 11.99999999999999822, 0.000000000000000000, 0.000000000000000000 ) ) ;
#25826=CARTESIAN_POINT ( 'NONE',  ( 11.99999999999999822, -2.946379043145784582, -75.11764819372150725 ) ) ;
#25832=ORIENTED_EDGE ( 'NONE', *, *, #12247, .T. ) ;
#25838=DIRECTION ( 'NONE',  ( -1.000000000000000000, 0.000000000000000000, -0.000000000000000000 ) ) ;
#25847=CYLINDRICAL_SURFACE ( 'NONE', #72154, 31.99999999999998579 ) ;
#25848=ORIENTED_EDGE ( 'NONE', *, *, #33882, .T. ) ;
#25875=DIRECTION ( 'NONE',  ( 0.000000000000000000, -0.7604059656000369261, 0.6494480483301767748 ) ) ;
#25888=LINE ( 'NONE', #66132, #43090 ) ;
#25893=ORIENTED_EDGE ( 'NONE', *, *, #1512, .F. ) ;
#25896=ADVANCED_FACE ( 'NONE', ( #34400 ), #68998, .T. ) ;
#25897=EDGE_LOOP ( 'NONE', ( #23773, #51283, #56161, #19837 ) ) ;
#25899=DIRECTION ( 'NONE',  ( -1.000000000000000000, 0.000000000000000000, 0.000000000000000000 ) ) ;
#25900=ORIENTED_EDGE ( 'NONE', *, *, #54992, .T. ) ;
#25910=ORIENTED_EDGE ( 'NONE', *, *, #44102, .F. ) ;
#25911=EDGE_CURVE ( 'NONE', #70942, #73391, #34781, .T. ) ;
#25921=DIRECTION ( 'NONE',  ( -1.000000000000000000, 0.000000000000000000, 0.000000000000000000 ) ) ;
#25922=DIRECTION ( 'NONE',  ( -1.000000000000000000, -0.000000000000000000, -0.000000000000000000 ) ) ;
#25934=AXIS2_PLACEMENT_3D ( 'NONE', #28293, #63276, #28665 ) ;
#25957=CARTESIAN_POINT ( 'NONE',  ( 11.99999999999999822, -75.11725578898466438, -2.956366410621452001 ) ) ;
#25961=CYLINDRICAL_SURFACE ( 'NONE', #5935, 77.49899999999999523 ) ;
#25962=ORIENTED_EDGE ( 'NONE', *, *, #39888, .F. ) ;
#25974=EDGE_CURVE ( 'NONE', #64000, #25226, #53454, .T. ) ;
#25975=ORIENTED_EDGE ( 'NONE', *, *, #7550, .T. ) ;
#25979=VECTOR ( 'NONE', #39147, 1000.000000000000000 ) ;
#25980=VERTEX_POINT ( 'NONE', #12583 ) ;
#25986=EDGE_CURVE ( 'NONE', #71078, #58524, #35480, .T. ) ;
#25988=VERTEX_POINT ( 'NONE', #35876 ) ;
#25991=FACE_OUTER_BOUND ( 'NONE', #59644, .T. ) ;
#25994=DIRECTION ( 'NONE',  ( -1.000000000000000000, 0.000000000000000000, -0.000000000000000000 ) ) ;
#26000=VERTEX_POINT ( 'NONE', #53182 ) ;
#26008=CARTESIAN_POINT ( 'NONE',  ( 0.000000000000000000, -81.96053171279901051, -2.543863470249259962 ) ) ;
#26009=DIRECTION ( 'NONE',  ( -1.000000000000000000, 0.000000000000000000, 0.000000000000000000 ) ) ;
#26011=CIRCLE ( 'NONE', #12804, 82.00000000000000000 ) ;
#26015=CARTESIAN_POINT ( 'NONE',  ( 11.99999999999999822, -75.16055320797016748, -18.89407956138335365 ) ) ;
#26038=FACE_OUTER_BOUND ( 'NONE', #50658, .T. ) ;
#26046=CIRCLE ( 'NONE', #35649, 31.99999999999999645 ) ;
#26054=AXIS2_PLACEMENT_3D ( 'NONE', #29933, #57789, #57416 ) ;
#26055=ORIENTED_EDGE ( 'NONE', *, *, #33361, .T. ) ;
#26057=VERTEX_POINT ( 'NONE', #65957 ) ;
#26058=ORIENTED_EDGE ( 'NONE', *, *, #49748, .F. ) ;
#26066=DIRECTION ( 'NONE',  ( 0.000000000000000000, 0.000000000000000000, 1.000000000000000000 ) ) ;
#26070=ORIENTED_EDGE ( 'NONE', *, *, #35648, .T. ) ;
#26081=CARTESIAN_POINT ( 'NONE',  ( 11.99999999999999822, 2.946379043147425492, -75.11764819372145041 ) ) ;
#26092=CARTESIAN_POINT ( 'NONE',  ( 5.999999999999999112, 33.71516098798741012, 74.74816331893441657 ) ) ;
#26099=ORIENTED_EDGE ( 'NONE', *, *, #18154, .F. ) ;
#26120=CIRCLE ( 'NONE', #65730, 82.00000000000000000 ) ;
#26124=EDGE_CURVE ( 'NONE', #67331, #21642, #65212, .T. ) ;
#26136=DIRECTION ( 'NONE',  ( -1.000000000000000000, -0.000000000000000000, 0.000000000000000000 ) ) ;
#26139=CIRCLE ( 'NONE', #2150, 77.49899999999999523 ) ;
#26150=CARTESIAN_POINT ( 'NONE',  ( 0.000000000000000000, 0.000000000000000000, 0.000000000000000000 ) ) ;
#26159=CARTESIAN_POINT ( 'NONE',  ( 11.99999999999999822, 75.16055320797030959, 18.89407956138283851 ) ) ;
#26173=ORIENTED_EDGE ( 'NONE', *, *, #45018, .T. ) ;
#26176=DIRECTION ( 'NONE',  ( -0.000000000000000000, -0.9135454576426006446, 0.4067366430758008744 ) ) ;
#26189=EDGE_LOOP ( 'NONE', ( #66950, #72950, #65321, #48706 ) ) ;
#26191=ORIENTED_EDGE ( 'NONE', *, *, #36589, .F. ) ;
#26196=CYLINDRICAL_SURFACE ( 'NONE', #29910, 31.99999999999998579 ) ;
#26204=LINE ( 'NONE', #31844, #44565 ) ;
#26212=CIRCLE ( 'NONE', #49024, 82.00000000000000000 ) ;
#26218=CIRCLE ( 'NONE', #65837, 77.49900000000000944 ) ;
#26221=ORIENTED_EDGE ( 'NONE', *, *, #26567, .F. ) ;
#26224=CARTESIAN_POINT ( 'NONE',  ( 0.000000000000000000, 0.000000000000000000, 0.000000000000000000 ) ) ;
#26232=DIRECTION ( 'NONE',  ( 0.000000000000000000, 0.000000000000000000, 1.000000000000000000 ) ) ;
#26234=CARTESIAN_POINT ( 'NONE',  ( 0.000000000000000000, -68.55367621811110723, -44.99326035066126650 ) ) ;
#26247=EDGE_LOOP ( 'NONE', ( #70159, #45882, #28265, #52836 ) ) ;
#26255=DIRECTION ( 'NONE',  ( 0.000000000000000000, 0.000000000000000000, 1.000000000000000000 ) ) ;
#26271=ORIENTED_EDGE ( 'NONE', *, *, #51021, .T. ) ;
#26273=ADVANCED_FACE ( 'NONE', ( #38105 ), #50106, .F. ) ;
#26276=ORIENTED_EDGE ( 'NONE', *, *, #54328, .T. ) ;
#26280=CARTESIAN_POINT ( 'NONE',  ( 0.000000000000000000, 75.11764819372142199, 2.946379043147685728 ) ) ;
#26295=CARTESIAN_POINT ( 'NONE',  ( 11.99999999999999822, -59.03961581697367933, -46.53671651294010303 ) ) ;
#26297=DIRECTION ( 'NONE',  ( 0.000000000000000000, 0.9135454576426010886, -0.4067366430757998752 ) ) ;
#26300=LINE ( 'NONE', #21392, #37653 ) ;
#26303=EDGE_CURVE ( 'NONE', #24118, #43739, #43984, .T. ) ;
#26305=DIRECTION ( 'NONE',  ( 0.000000000000000000, 0.9135454576426005335, -0.4067366430758009299 ) ) ;
#26307=DIRECTION ( 'NONE',  ( -1.000000000000000000, -0.000000000000000000, -0.000000000000000000 ) ) ;
#26315=FACE_OUTER_BOUND ( 'NONE', #41350, .T. ) ;
#26323=VECTOR ( 'NONE', #3661, 1000.000000000000000 ) ;
#26338=ORIENTED_EDGE ( 'NONE', *, *, #42625, .F. ) ;
#26340=ORIENTED_EDGE ( 'NONE', *, *, #11280, .T. ) ;
#26344=CARTESIAN_POINT ( 'NONE',  ( 11.99999999999999822, 59.03961581697399907, 46.53671651293969802 ) ) ;
#26346=DIRECTION ( 'NONE',  ( 0.000000000000000000, 0.9510565162951523099, 0.3090169943749514481 ) ) ;
#26347=DIRECTION ( 'NONE',  ( -1.000000000000000000, 0.000000000000000000, -0.000000000000000000 ) ) ;
#26349=DIRECTION ( 'NONE',  ( 0.000000000000000000, 0.000000000000000000, 1.000000000000000000 ) ) ;
#26353=EDGE_LOOP ( 'NONE', ( #6639, #30957, #9399, #40618 ) ) ;
#26361=VERTEX_POINT ( 'NONE', #29044 ) ;
#26367=ORIENTED_EDGE ( 'NONE', *, *, #69987, .F. ) ;
#26371=DIRECTION ( 'NONE',  ( -1.000000000000000000, -0.000000000000000000, -0.000000000000000000 ) ) ;
#26374=DIRECTION ( 'NONE',  ( -1.000000000000000000, -0.000000000000000000, -0.000000000000000000 ) ) ;
#26382=VECTOR ( 'NONE', #17121, 1000.000000000000000 ) ;
#26388=AXIS2_PLACEMENT_3D ( 'NONE', #26224, #61194, #14204 ) ;
#26394=DIRECTION ( 'NONE',  ( -1.000000000000000000, -0.000000000000000000, -0.000000000000000000 ) ) ;
#26404=ADVANCED_FACE ( 'NONE', ( #74165 ), #522, .F. ) ;
#26407=CARTESIAN_POINT ( 'NONE',  ( 11.99999999999999822, -2.956366410621191765, 75.11725578898467859 ) ) ;
#26417=CIRCLE ( 'NONE', #40868, 31.99999999999998934 ) ;
#26421=CARTESIAN_POINT ( 'NONE',  ( 0.000000000000000000, -71.91182617369207719, 28.89263327155721228 ) ) ;
#26427=CIRCLE ( 'NONE', #7223, 31.99999999999999289 ) ;
#26439=VERTEX_POINT ( 'NONE', #41083 ) ;
#26440=ORIENTED_EDGE ( 'NONE', *, *, #16445, .T. ) ;
#26442=CARTESIAN_POINT ( 'NONE',  ( 11.99999999999999822, 51.29473840253223216, 63.97538442413446091 ) ) ;
#26458=VERTEX_POINT ( 'NONE', #64016 ) ;
#26462=DIRECTION ( 'NONE',  ( 0.000000000000000000, 0.9510565162951543083, 0.3090169943749448977 ) ) ;
#26464=CARTESIAN_POINT ( 'NONE',  ( 11.99999999999999822, 63.18004540533030422, 44.88180994100399346 ) ) ;
#26467=DIRECTION ( 'NONE',  ( -1.000000000000000000, -0.000000000000000000, 0.000000000000000000 ) ) ;
#26468=AXIS2_PLACEMENT_3D ( 'NONE', #73635, #29253, #13 ) ;
#26475=ORIENTED_EDGE ( 'NONE', *, *, #32399, .T. ) ;
#26476=AXIS2_PLACEMENT_3D ( 'NONE', #23980, #17960, #12679 ) ;
#26477=EDGE_CURVE ( 'NONE', #63620, #47511, #68910, .T. ) ;
#26481=CARTESIAN_POINT ( 'NONE',  ( 15.00000000000000000, -23.29833615347109088, -3.418703333116486665 ) ) ;
#26484=CARTESIAN_POINT ( 'NONE',  ( 0.000000000000000000, -75.11725578898466438, -2.956366410621452001 ) ) ;
#26485=EDGE_CURVE ( 'NONE', #69892, #6635, #31994, .T. ) ;
#26486=VERTEX_POINT ( 'NONE', #53826 ) ;
#26488=CIRCLE ( 'NONE', #69741, 82.00000000000000000 ) ;
#26489=CARTESIAN_POINT ( 'NONE',  ( 11.99999999999999822, -34.94270380257692921, 74.18225833017875459 ) ) ;
#26490=AXIS2_PLACEMENT_3D ( 'NONE', #57176, #28578, #12403 ) ;
#26498=CIRCLE ( 'NONE', #57690, 82.00000000000000000 ) ;
#26508=DIRECTION ( 'NONE',  ( -1.000000000000000000, -0.000000000000000000, 0.000000000000000000 ) ) ;
#26509=EDGE_CURVE ( 'NONE', #38472, #30664, #7601, .T. ) ;
#26539=DIRECTION ( 'NONE',  ( -1.000000000000000000, 0.000000000000000000, -0.000000000000000000 ) ) ;
#26540=EDGE_CURVE ( 'NONE', #34012, #4061, #41805, .T. ) ;
#26550=CARTESIAN_POINT ( 'NONE',  ( 6.000000000000000000, 39.47590169984945163, -71.87247863392373404 ) ) ;
#26551=CARTESIAN_POINT ( 'NONE',  ( 12.00000000000000000, 22.07842321921480888, -8.187992925817425771 ) ) ;
#26556=ORIENTED_EDGE ( 'NONE', *, *, #15510, .F. ) ;
#26563=PLANE ( 'NONE',  #50417 ) ;
#26567=EDGE_CURVE ( 'NONE', #70160, #60573, #7963, .T. ) ;
#26568=CYLINDRICAL_SURFACE ( 'NONE', #41706, 77.49899999999999523 ) ;
#26569=EDGE_LOOP ( 'NONE', ( #41431, #11357, #58974, #13216 ) ) ;
#26571=AXIS2_PLACEMENT_3D ( 'NONE', #68175, #16301, #38116 ) ;
#26573=VECTOR ( 'NONE', #50711, 1000.000000000000000 ) ;
#26578=PLANE ( 'NONE',  #9677 ) ;
#26584=AXIS2_PLACEMENT_3D ( 'NONE', #28033, #74273, #67524 ) ;
#26587=FACE_OUTER_BOUND ( 'NONE', #5468, .T. ) ;
#26596=DIRECTION ( 'NONE',  ( 0.000000000000000000, 0.000000000000000000, 1.000000000000000000 ) ) ;
#26598=DIRECTION ( 'NONE',  ( -1.000000000000000000, 0.000000000000000000, 0.000000000000000000 ) ) ;
#26603=EDGE_CURVE ( 'NONE', #34276, #45130, #35655, .T. ) ;
#26614=ORIENTED_EDGE ( 'NONE', *, *, #21620, .T. ) ;
#26617=CIRCLE ( 'NONE', #56656, 31.99999999999998579 ) ;
#26620=ORIENTED_EDGE ( 'NONE', *, *, #24069, .T. ) ;
#26627=VECTOR ( 'NONE', #25921, 1000.000000000000000 ) ;
#26629=ORIENTED_EDGE ( 'NONE', *, *, #44563, .F. ) ;
#26630=LINE ( 'NONE', #33006, #60818 ) ;
#26631=CIRCLE ( 'NONE', #23220, 82.00000000000000000 ) ;
#26639=DIRECTION ( 'NONE',  ( 0.000000000000000000, 0.000000000000000000, 1.000000000000000000 ) ) ;
#26641=AXIS2_PLACEMENT_3D ( 'NONE', #2401, #64778, #30539 ) ;
#26643=ORIENTED_EDGE ( 'NONE', *, *, #61140, .T. ) ;
#26644=AXIS2_PLACEMENT_3D ( 'NONE', #48243, #18186, #12539 ) ;
#26647=LINE ( 'NONE', #3019, #62417 ) ;
#26657=DIRECTION ( 'NONE',  ( 0.000000000000000000, 0.7431448254773863615, -0.6691306063588670083 ) ) ;
#26659=CARTESIAN_POINT ( 'NONE',  ( 5.999999999999999112, 67.80270845531887858, 46.11716303203210288 ) ) ;
#26664=CARTESIAN_POINT ( 'NONE',  ( 0.000000000000000000, 0.000000000000000000, 0.000000000000000000 ) ) ;
#26674=AXIS2_PLACEMENT_3D ( 'NONE', #18719, #53679, #58964 ) ;
#26676=VECTOR ( 'NONE', #7353, 1000.000000000000000 ) ;
#26681=CARTESIAN_POINT ( 'NONE',  ( 5.999999999999999112, -64.81221759200306565, -50.23322058963418613 ) ) ;
#26683=DIRECTION ( 'NONE',  ( -1.000000000000000000, -0.000000000000000000, -0.000000000000000000 ) ) ;
#26685=AXIS2_PLACEMENT_3D ( 'NONE', #7536, #70661, #14273 ) ;
#26689=CARTESIAN_POINT ( 'NONE',  ( 0.000000000000000000, 34.44570377933693806, -69.42325613327405165 ) ) ;
#26696=CYLINDRICAL_SURFACE ( 'NONE', #56291, 31.99999999999998579 ) ;
#26700=EDGE_LOOP ( 'NONE', ( #24322, #52702, #34141, #30779 ) ) ;
#26705=DIRECTION ( 'NONE',  ( 0.000000000000000000, 0.000000000000000000, 1.000000000000000000 ) ) ;
#26710=DIRECTION ( 'NONE',  ( 1.000000000000000000, 0.000000000000000000, 0.000000000000000000 ) ) ;
#26712=EDGE_CURVE ( 'NONE', #66935, #16641, #24390, .T. ) ;
#26714=VERTEX_POINT ( 'NONE', #29639 ) ;
#26726=AXIS2_PLACEMENT_3D ( 'NONE', #47123, #52755, #68939 ) ;
#26730=AXIS2_PLACEMENT_3D ( 'NONE', #21712, #34108, #62329 ) ;
#26731=EDGE_LOOP ( 'NONE', ( #42214, #40440, #13955, #25236 ) ) ;
#26738=EDGE_CURVE ( 'NONE', #48419, #5745, #70226, .T. ) ;
#26741=LINE ( 'NONE', #32012, #53534 ) ;
#26746=AXIS2_PLACEMENT_3D ( 'NONE', #25477, #8179, #64233 ) ;
#26762=DIRECTION ( 'NONE',  ( -1.000000000000000000, 0.000000000000000000, -0.000000000000000000 ) ) ;
#26765=DIRECTION ( 'NONE',  ( 0.000000000000000000, 0.000000000000000000, 1.000000000000000000 ) ) ;
#26766=DIRECTION ( 'NONE',  ( 0.000000000000000000, 0.000000000000000000, 1.000000000000000000 ) ) ;
#26772=DIRECTION ( 'NONE',  ( 0.000000000000000000, 0.000000000000000000, 1.000000000000000000 ) ) ;
#26773=CIRCLE ( 'NONE', #6413, 77.49899999999999523 ) ;
#26775=EDGE_LOOP ( 'NONE', ( #44277, #6274, #15055, #10427 ) ) ;
#26776=LINE ( 'NONE', #50459, #44438 ) ;
#26781=LINE ( 'NONE', #67954, #13542 ) ;
#26783=ORIENTED_EDGE ( 'NONE', *, *, #72989, .F. ) ;
#26785=DIRECTION ( 'NONE',  ( 0.000000000000000000, 0.000000000000000000, 1.000000000000000000 ) ) ;
#26788=CIRCLE ( 'NONE', #60421, 77.49899999999999523 ) ;
#26789=CARTESIAN_POINT ( 'NONE',  ( 11.99999999999999822, -74.65374052328644439, -8.840884882375878107 ) ) ;
#26797=ORIENTED_EDGE ( 'NONE', *, *, #15438, .F. ) ;
#26798=ORIENTED_EDGE ( 'NONE', *, *, #30145, .T. ) ;
#26808=EDGE_CURVE ( 'NONE', #18566, #51720, #10333, .T. ) ;
#26817=DIRECTION ( 'NONE',  ( -1.000000000000000000, -0.000000000000000000, -0.000000000000000000 ) ) ;
#26821=DIRECTION ( 'NONE',  ( -1.000000000000000000, 0.000000000000000000, 0.000000000000000000 ) ) ;
#26823=CIRCLE ( 'NONE', #43642, 77.49899999999999523 ) ;
#26829=CYLINDRICAL_SURFACE ( 'NONE', #37376, 77.49899999999999523 ) ;
#26834=CARTESIAN_POINT ( 'NONE',  ( 0.000000000000000000, 0.000000000000000000, 0.000000000000000000 ) ) ;
#26846=DIRECTION ( 'NONE',  ( -1.000000000000000000, 0.000000000000000000, 0.000000000000000000 ) ) ;
#26849=DIRECTION ( 'NONE',  ( 0.000000000000000000, 0.000000000000000000, 1.000000000000000000 ) ) ;
#26851=VECTOR ( 'NONE', #37611, 1000.000000000000000 ) ;
#26863=CIRCLE ( 'NONE', #48502, 31.99999999999998934 ) ;
#26866=EDGE_LOOP ( 'NONE', ( #66664, #9167, #24510, #8085 ) ) ;
#26872=VERTEX_POINT ( 'NONE', #36397 ) ;
#26874=DIRECTION ( 'NONE',  ( -1.000000000000000000, -0.000000000000000000, -0.000000000000000000 ) ) ;
#26877=ORIENTED_EDGE ( 'NONE', *, *, #27240, .T. ) ;
#26878=AXIS2_PLACEMENT_3D ( 'NONE', #70040, #1675, #30559 ) ;
#26881=ADVANCED_FACE ( 'NONE', ( #61850 ), #47686, .T. ) ;
#26885=CYLINDRICAL_SURFACE ( 'NONE', #37104, 31.99999999999998579 ) ;
#26888=AXIS2_PLACEMENT_3D ( 'NONE', #58253, #2633, #24055 ) ;
#26892=DIRECTION ( 'NONE',  ( 0.000000000000000000, -0.4999999999999920064, 0.8660254037844432595 ) ) ;
#26903=DIRECTION ( 'NONE',  ( 0.000000000000000000, 0.000000000000000000, 1.000000000000000000 ) ) ;
#26904=CYLINDRICAL_SURFACE ( 'NONE', #32384, 31.99999999999998579 ) ;
#26906=DIRECTION ( 'NONE',  ( 0.000000000000000000, 0.000000000000000000, -1.000000000000000000 ) ) ;
#26912=AXIS2_PLACEMENT_3D ( 'NONE', #62558, #11400, #45999 ) ;
#26929=DIRECTION ( 'NONE',  ( 0.000000000000000000, 0.000000000000000000, 1.000000000000000000 ) ) ;
#26931=CARTESIAN_POINT ( 'NONE',  ( 15.00000000000000000, -20.55727247249748402, -16.78983467731284307 ) ) ;
#26932=FACE_OUTER_BOUND ( 'NONE', #14464, .T. ) ;
#26934=VERTEX_POINT ( 'NONE', #62556 ) ;
#26939=CYLINDRICAL_SURFACE ( 'NONE', #49133, 82.00000000000000000 ) ;
#26947=CARTESIAN_POINT ( 'NONE',  ( 0.000000000000000000, -3.894527615418457600, 81.90746397400387480 ) ) ;
#26951=CARTESIAN_POINT ( 'NONE',  ( 11.99999999999999822, 36.72794159290334903, -65.59268652807170952 ) ) ;
#26952=ORIENTED_EDGE ( 'NONE', *, *, #15778, .F. ) ;
#26962=DIRECTION ( 'NONE',  ( -1.000000000000000000, 0.000000000000000000, -0.000000000000000000 ) ) ;
#26964=VECTOR ( 'NONE', #25266, 1000.000000000000000 ) ;
#26970=VERTEX_POINT ( 'NONE', #16676 ) ;
#26973=DIRECTION ( 'NONE',  ( 0.000000000000000000, 0.000000000000000000, 1.000000000000000000 ) ) ;
#26974=FACE_OUTER_BOUND ( 'NONE', #4587, .T. ) ;
#26977=DIRECTION ( 'NONE',  ( -1.000000000000000000, -0.000000000000000000, 0.000000000000000000 ) ) ;
#26983=DIRECTION ( 'NONE',  ( -1.000000000000000000, 0.000000000000000000, 0.000000000000000000 ) ) ;
#26984=LINE ( 'NONE', #37553, #22133 ) ;
#26985=ORIENTED_EDGE ( 'NONE', *, *, #29943, .T. ) ;
#26993=EDGE_CURVE ( 'NONE', #45152, #15229, #12134, .T. ) ;
#27000=ORIENTED_EDGE ( 'NONE', *, *, #54552, .F. ) ;
#27009=AXIS2_PLACEMENT_3D ( 'NONE', #39814, #57108, #67266 ) ;
#27014=ORIENTED_EDGE ( 'NONE', *, *, #50938, .T. ) ;
#27035=EDGE_CURVE ( 'NONE', #17023, #52404, #17048, .T. ) ;
#27036=CARTESIAN_POINT ( 'NONE',  ( 15.00000000000000000, -13.04903810567646971, 19.60159698893442481 ) ) ;
#27044=FACE_OUTER_BOUND ( 'NONE', #57839, .T. ) ;
#27052=VERTEX_POINT ( 'NONE', #48576 ) ;
#27055=DIRECTION ( 'NONE',  ( 0.000000000000000000, -0.9510565162951566398, 0.3090169943749380144 ) ) ;
#27066=CARTESIAN_POINT ( 'NONE',  ( 11.99999999999999822, -20.40083707022935400, 72.35432306680478121 ) ) ;
#27075=EDGE_CURVE ( 'NONE', #16641, #28106, #66834, .T. ) ;
#27077=CYLINDRICAL_SURFACE ( 'NONE', #68254, 77.49899999999999523 ) ;
#27081=ADVANCED_FACE ( 'NONE', ( #8725 ), #47106, .T. ) ;
#27088=ORIENTED_EDGE ( 'NONE', *, *, #5812, .F. ) ;
#27091=CARTESIAN_POINT ( 'NONE',  ( 11.99999999999999822, -40.65526001592663619, 71.21200624218782593 ) ) ;
#27100=DIRECTION ( 'NONE',  ( 0.000000000000000000, 0.000000000000000000, 1.000000000000000000 ) ) ;
#27103=LINE ( 'NONE', #15092, #27820 ) ;
#27106=LINE ( 'NONE', #27862, #71924 ) ;
#27116=DIRECTION ( 'NONE',  ( -1.000000000000000000, -0.000000000000000000, 0.000000000000000000 ) ) ;
#27128=ADVANCED_FACE ( 'NONE', ( #59867 ), #18513, .F. ) ;
#27139=DIRECTION ( 'NONE',  ( -1.000000000000000000, 0.000000000000000000, 0.000000000000000000 ) ) ;
#27141=DIRECTION ( 'NONE',  ( 0.000000000000000000, 0.5877852522924742473, -0.8090169943749466741 ) ) ;
#27162=AXIS2_PLACEMENT_3D ( 'NONE', #821, #35713, #24094 ) ;
#27165=DIRECTION ( 'NONE',  ( 0.000000000000000000, 0.000000000000000000, 1.000000000000000000 ) ) ;
#27167=VERTEX_POINT ( 'NONE', #71118 ) ;
#27176=DIRECTION ( 'NONE',  ( -1.000000000000000000, 0.000000000000000000, 0.000000000000000000 ) ) ;
#27183=EDGE_LOOP ( 'NONE', ( #14811, #44495, #16521, #7143 ) ) ;
#27186=ORIENTED_EDGE ( 'NONE', *, *, #10059, .F. ) ;
#27187=DIRECTION ( 'NONE',  ( -1.000000000000000000, -0.000000000000000000, -0.000000000000000000 ) ) ;
#27194=DIRECTION ( 'NONE',  ( -1.000000000000000000, 0.000000000000000000, -0.000000000000000000 ) ) ;
#27198=CYLINDRICAL_SURFACE ( 'NONE', #5536, 77.49899999999999523 ) ;
#27203=ADVANCED_FACE ( 'NONE', ( #47468 ), #7613, .T. ) ;
#27207=ORIENTED_EDGE ( 'NONE', *, *, #32233, .T. ) ;
#27209=EDGE_CURVE ( 'NONE', #16098, #64851, #70749, .T. ) ;
#27220=EDGE_CURVE ( 'NONE', #48336, #13922, #19622, .T. ) ;
#27221=LINE ( 'NONE', #3962, #16048 ) ;
#27226=ORIENTED_EDGE ( 'NONE', *, *, #22959, .T. ) ;
#27234=EDGE_LOOP ( 'NONE', ( #44027, #24499, #35475, #35858 ) ) ;
#27235=AXIS2_PLACEMENT_3D ( 'NONE', #3524, #13749, #16256 ) ;
#27240=EDGE_CURVE ( 'NONE', #61698, #27755, #62119, .T. ) ;
#27251=DIRECTION ( 'NONE',  ( 0.000000000000000000, -0.6494480483301738882, -0.7604059656000392575 ) ) ;
#27252=CARTESIAN_POINT ( 'NONE',  ( 0.000000000000000000, 59.03961581697399907, 46.53671651293969802 ) ) ;
#27261=ORIENTED_EDGE ( 'NONE', *, *, #58930, .F. ) ;
#27267=CIRCLE ( 'NONE', #12897, 77.49900000000000944 ) ;
#27279=ORIENTED_EDGE ( 'NONE', *, *, #13132, .F. ) ;
#27281=DIRECTION ( 'NONE',  ( -1.000000000000000000, -0.000000000000000000, 0.000000000000000000 ) ) ;
#27282=CARTESIAN_POINT ( 'NONE',  ( 11.99999999999999822, 0.000000000000000000, 0.000000000000000000 ) ) ;
#27285=CYLINDRICAL_SURFACE ( 'NONE', #56488, 31.99999999999998579 ) ;
#27288=CARTESIAN_POINT ( 'NONE',  ( 11.99999999999999822, 75.11764819372149304, -2.946379043146603482 ) ) ;
#27289=CARTESIAN_POINT ( 'NONE',  ( 0.000000000000000000, 0.000000000000000000, 0.000000000000000000 ) ) ;
#27292=VERTEX_POINT ( 'NONE', #27480 ) ;
#27293=CIRCLE ( 'NONE', #52517, 31.99999999999998579 ) ;
#27304=EDGE_CURVE ( 'NONE', #67853, #15222, #10484, .T. ) ;
#27312=LINE ( 'NONE', #55535, #65219 ) ;
#27319=DIRECTION ( 'NONE',  ( 0.000000000000000000, 0.000000000000000000, 1.000000000000000000 ) ) ;
#27322=CARTESIAN_POINT ( 'NONE',  ( 11.99999999999999822, -31.47745569255092235, -68.26794271651296242 ) ) ;
#27326=EDGE_CURVE ( 'NONE', #68748, #4061, #43688, .T. ) ;
#27328=ORIENTED_EDGE ( 'NONE', *, *, #54836, .T. ) ;
#27340=CIRCLE ( 'NONE', #69383, 77.49900000000002365 ) ;
#27342=LINE ( 'NONE', #21324, #42878 ) ;
#27351=ORIENTED_EDGE ( 'NONE', *, *, #71864, .T. ) ;
#27353=CARTESIAN_POINT ( 'NONE',  ( 12.00000000000000000, 14.60985201121703980, -18.46759930825707841 ) ) ;
#27355=ORIENTED_EDGE ( 'NONE', *, *, #16228, .F. ) ;
#27360=DIRECTION ( 'NONE',  ( 0.000000000000000000, 0.000000000000000000, 1.000000000000000000 ) ) ;
#27361=ORIENTED_EDGE ( 'NONE', *, *, #34225, .T. ) ;
#27375=CARTESIAN_POINT ( 'NONE',  ( 15.00000000000000000, -14.54903810567644484, 22.19967320028775504 ) ) ;
#27387=CARTESIAN_POINT ( 'NONE',  ( 11.99999999999999822, -20.41045688087876897, 72.35160999960810102 ) ) ;
#27390=DIRECTION ( 'NONE',  ( 0.000000000000000000, 0.6691306063588670083, 0.7431448254773863615 ) ) ;
#27396=LINE ( 'NONE', #26659, #51718 ) ;
#27409=LINE ( 'NONE', #50343, #1997 ) ;
#27413=FACE_OUTER_BOUND ( 'NONE', #44783, .T. ) ;
#27417=FACE_OUTER_BOUND ( 'NONE', #11184, .T. ) ;
#27420=CARTESIAN_POINT ( 'NONE',  ( 11.99999999999999822, -72.35160999960801576, -20.41045688087902121 ) ) ;
#27430=ORIENTED_EDGE ( 'NONE', *, *, #72816, .F. ) ;
#27432=CARTESIAN_POINT ( 'NONE',  ( 0.000000000000000000, 49.70050353004889132, 59.46389618801982380 ) ) ;
#27433=VERTEX_POINT ( 'NONE', #68840 ) ;
#27436=ORIENTED_EDGE ( 'NONE', *, *, #44507, .T. ) ;
#27443=AXIS2_PLACEMENT_3D ( 'NONE', #11282, #33845, #51134 ) ;
#27447=DIRECTION ( 'NONE',  ( -1.000000000000000000, 0.000000000000000000, -0.000000000000000000 ) ) ;
#27449=AXIS2_PLACEMENT_3D ( 'NONE', #67369, #9116, #26765 ) ;
#27455=EDGE_LOOP ( 'NONE', ( #71185, #52376, #46497, #47253 ) ) ;
#27459=CARTESIAN_POINT ( 'NONE',  ( 11.99999999999999822, 14.66109333815460225, 73.73191006444577056 ) ) ;
#27477=CIRCLE ( 'NONE', #28654, 82.00000000000000000 ) ;
#27480=CARTESIAN_POINT ( 'NONE',  ( 0.000000000000000000, -40.65526001592564853, -71.21200624218839437 ) ) ;
#27483=AXIS2_PLACEMENT_3D ( 'NONE', #16149, #26307, #4901 ) ;
#27486=CARTESIAN_POINT ( 'NONE',  ( 5.999999999999999112, -79.10210256391353312, -21.60688246758669351 ) ) ;
#27488=VERTEX_POINT ( 'NONE', #818 ) ;
#27493=AXIS2_PLACEMENT_3D ( 'NONE', #23287, #46217, #759 ) ;
#27499=EDGE_CURVE ( 'NONE', #17107, #24230, #6068, .T. ) ;
#27500=ORIENTED_EDGE ( 'NONE', *, *, #67826, .T. ) ;
#27503=VECTOR ( 'NONE', #18419, 1000.000000000000000 ) ;
#27512=EDGE_CURVE ( 'NONE', #25600, #54039, #53686, .T. ) ;
#27518=CARTESIAN_POINT ( 'NONE',  ( 11.99999999999999822, 77.19088730480524418, 6.903761155838049390 ) ) ;
#27519=CARTESIAN_POINT ( 'NONE',  ( 11.99999999999999822, 8.966570791701867549, -81.50828551894218776 ) ) ;
#27522=CARTESIAN_POINT ( 'NONE',  ( 0.000000000000000000, -73.72996012237429397, -14.67089635893794508 ) ) ;
#27524=ORIENTED_EDGE ( 'NONE', *, *, #67022, .T. ) ;
#27532=CIRCLE ( 'NONE', #32305, 31.99999999999998224 ) ;
#27541=CIRCLE ( 'NONE', #6007, 31.99999999999998224 ) ;
#27546=VERTEX_POINT ( 'NONE', #48485 ) ;
#27550=ORIENTED_EDGE ( 'NONE', *, *, #24875, .F. ) ;
#27551=VECTOR ( 'NONE', #32654, 1000.000000000000000 ) ;
#27558=VECTOR ( 'NONE', #8456, 1000.000000000000227 ) ;
#27561=CARTESIAN_POINT ( 'NONE',  ( 11.99999999999999822, -72.35432306680469594, -20.40083707022958848 ) ) ;
#27562=DIRECTION ( 'NONE',  ( -1.000000000000000000, -0.000000000000000000, -0.000000000000000000 ) ) ;
#27565=FACE_OUTER_BOUND ( 'NONE', #55308, .T. ) ;
#27568=AXIS2_PLACEMENT_3D ( 'NONE', #50640, #57041, #56298 ) ;
#27576=LINE ( 'NONE', #67053, #46705 ) ;
#27587=ORIENTED_EDGE ( 'NONE', *, *, #47187, .T. ) ;
#27598=ADVANCED_FACE ( 'NONE', ( #36094 ), #14267, .T. ) ;
#27602=DIRECTION ( 'NONE',  ( 0.000000000000000000, 0.000000000000000000, 1.000000000000000000 ) ) ;
#27610=EDGE_CURVE ( 'NONE', #27765, #68607, #14071, .T. ) ;
#27619=AXIS2_PLACEMENT_3D ( 'NONE', #39362, #46763, #10789 ) ;
#27623=VECTOR ( 'NONE', #14401, 1000.000000000000114 ) ;
#27628=ORIENTED_EDGE ( 'NONE', *, *, #8325, .T. ) ;
#27630=ORIENTED_EDGE ( 'NONE', *, *, #4434, .T. ) ;
#27631=AXIS2_PLACEMENT_3D ( 'NONE', #12717, #13089, #1862 ) ;
#27635=VERTEX_POINT ( 'NONE', #70654 ) ;
#27642=PLANE ( 'NONE',  #65784 ) ;
#27646=ORIENTED_EDGE ( 'NONE', *, *, #29927, .F. ) ;
#27647=EDGE_LOOP ( 'NONE', ( #44598, #59599, #53817, #66859 ) ) ;
#27662=VERTEX_POINT ( 'NONE', #37584 ) ;
#27667=CARTESIAN_POINT ( 'NONE',  ( 5.999999999999999112, -56.15606465354916566, -59.75363087400133111 ) ) ;
#27670=CIRCLE ( 'NONE', #66106, 31.99999999999999289 ) ;
#27673=FACE_OUTER_BOUND ( 'NONE', #25276, .T. ) ;
#27679=ORIENTED_EDGE ( 'NONE', *, *, #72624, .F. ) ;
#27687=ORIENTED_EDGE ( 'NONE', *, *, #65305, .T. ) ;
#27690=ORIENTED_EDGE ( 'NONE', *, *, #5904, .F. ) ;
#27698=LINE ( 'NONE', #50622, #31293 ) ;
#27700=CYLINDRICAL_SURFACE ( 'NONE', #9971, 31.99999999999998579 ) ;
#27703=CARTESIAN_POINT ( 'NONE',  ( 11.99999999999999822, -36.73666225445940370, 65.58780272294062286 ) ) ;
#27704=CARTESIAN_POINT ( 'NONE',  ( 11.99999999999999822, 31.47745569255237896, -68.26794271651228030 ) ) ;
#27706=LINE ( 'NONE', #46116, #13387 ) ;
#27711=AXIS2_PLACEMENT_3D ( 'NONE', #4690, #10675, #61450 ) ;
#27716=CARTESIAN_POINT ( 'NONE',  ( 11.99999999999999822, -17.28742895386137945, 75.54627589209938776 ) ) ;
#27727=FACE_OUTER_BOUND ( 'NONE', #4469, .T. ) ;
#27742=CARTESIAN_POINT ( 'NONE',  ( -10.00000000000000000, 0.000000000000000000, 0.000000000000000000 ) ) ;
#27746=ORIENTED_EDGE ( 'NONE', *, *, #58555, .F. ) ;
#27750=ORIENTED_EDGE ( 'NONE', *, *, #73389, .T. ) ;
#27755=VERTEX_POINT ( 'NONE', #66525 ) ;
#27759=AXIS2_PLACEMENT_3D ( 'NONE', #15561, #22314, #4302 ) ;
#27760=CARTESIAN_POINT ( 'NONE',  ( 0.000000000000000000, 36.72794159290334903, -65.59268652807170952 ) ) ;
#27765=VERTEX_POINT ( 'NONE', #4493 ) ;
#27769=FACE_OUTER_BOUND ( 'NONE', #15526, .T. ) ;
#27772=VERTEX_POINT ( 'NONE', #33034 ) ;
#27792=EDGE_CURVE ( 'NONE', #590, #5835, #43964, .T. ) ;
#27793=CARTESIAN_POINT ( 'NONE',  ( 11.99999999999999822, 44.88180994100376608, 63.18004540533043922 ) ) ;
#27795=DIRECTION ( 'NONE',  ( 0.000000000000000000, 0.000000000000000000, 1.000000000000000000 ) ) ;
#27796=LINE ( 'NONE', #72889, #52087 ) ;
#27801=LINE ( 'NONE', #45109, #65962 ) ;
#27807=AXIS2_PLACEMENT_3D ( 'NONE', #4970, #10209, #32394 ) ;
#27820=VECTOR ( 'NONE', #49669, 1000.000000000000000 ) ;
#27821=DIRECTION ( 'NONE',  ( 0.000000000000000000, 0.7431448254773954654, 0.6691306063588569053 ) ) ;
#27825=VECTOR ( 'NONE', #58405, 1000.000000000000000 ) ;
#27831=ORIENTED_EDGE ( 'NONE', *, *, #14190, .F. ) ;
#27832=DIRECTION ( 'NONE',  ( 0.000000000000000000, 0.8526401643540897357, 0.5224985647159527957 ) ) ;
#27834=DIRECTION ( 'NONE',  ( 0.000000000000000000, 0.000000000000000000, 1.000000000000000000 ) ) ;
#27838=ORIENTED_EDGE ( 'NONE', *, *, #33870, .F. ) ;
#27843=ORIENTED_EDGE ( 'NONE', *, *, #44051, .F. ) ;
#27846=EDGE_CURVE ( 'NONE', #40890, #33344, #28505, .T. ) ;
#27860=CARTESIAN_POINT ( 'NONE',  ( 15.00000000000000000, 9.615535125378766423, -24.73947219025917121 ) ) ;
#27862=CARTESIAN_POINT ( 'NONE',  ( 5.999999999999999112, -60.67117009219175827, 55.16347631943019536 ) ) ;
#27863=EDGE_CURVE ( 'NONE', #70343, #31915, #64131, .T. ) ;
#27868=DIRECTION ( 'NONE',  ( 0.000000000000000000, -0.8090169943749433434, 0.5877852522924787992 ) ) ;
#27870=AXIS2_PLACEMENT_3D ( 'NONE', #10481, #50705, #44716 ) ;
#27879=DIRECTION ( 'NONE',  ( 0.000000000000000000, 0.000000000000000000, 1.000000000000000000 ) ) ;
#27881=DIRECTION ( 'NONE',  ( 1.000000000000000000, -0.000000000000000000, 0.000000000000000000 ) ) ;
#27882=DIRECTION ( 'NONE',  ( -1.000000000000000000, -0.000000000000000000, 0.000000000000000000 ) ) ;
#27885=CARTESIAN_POINT ( 'NONE',  ( 6.000000000000000000, -39.47590169984795239, -71.87247863392455827 ) ) ;
#27897=PLANE ( 'NONE',  #60747 ) ;
#27898=ORIENTED_EDGE ( 'NONE', *, *, #27499, .F. ) ;
#27899=EDGE_CURVE ( 'NONE', #60573, #18312, #24631, .T. ) ;
#27904=PLANE ( 'NONE',  #48874 ) ;
#27913=VERTEX_POINT ( 'NONE', #53206 ) ;
#27914=DIRECTION ( 'NONE',  ( -1.000000000000000000, 0.000000000000000000, 0.000000000000000000 ) ) ;
#27926=ORIENTED_EDGE ( 'NONE', *, *, #57625, .T. ) ;
#27933=CYLINDRICAL_SURFACE ( 'NONE', #64238, 31.99999999999998579 ) ;
#27938=EDGE_CURVE ( 'NONE', #10371, #68327, #40543, .T. ) ;
#27940=EDGE_CURVE ( 'NONE', #38016, #49934, #26139, .T. ) ;
#27944=VERTEX_POINT ( 'NONE', #11227 ) ;
#27946=DIRECTION ( 'NONE',  ( -1.000000000000000000, -0.000000000000000000, 0.000000000000000000 ) ) ;
#27967=AXIS2_PLACEMENT_3D ( 'NONE', #69880, #12007, #34943 ) ;
#27980=DIRECTION ( 'NONE',  ( -1.000000000000000000, 0.000000000000000000, 0.000000000000000000 ) ) ;
#27987=ORIENTED_EDGE ( 'NONE', *, *, #34196, .T. ) ;
#28001=CIRCLE ( 'NONE', #15984, 31.99999999999998579 ) ;
#28004=EDGE_CURVE ( 'NONE', #33844, #19051, #3373, .T. ) ;
#28012=VECTOR ( 'NONE', #67010, 1000.000000000000000 ) ;
#28023=ADVANCED_FACE ( 'NONE', ( #70472 ), #37025, .F. ) ;
#28033=CARTESIAN_POINT ( 'NONE',  ( 11.99999999999999822, -59.03961581697432592, 46.53671651293927880 ) ) ;
#28038=CIRCLE ( 'NONE', #4067, 31.99999999999998579 ) ;
#28042=ORIENTED_EDGE ( 'NONE', *, *, #60726, .F. ) ;
#28045=DIRECTION ( 'NONE',  ( -1.000000000000000000, 0.000000000000000000, -0.000000000000000000 ) ) ;
#28052=AXIS2_PLACEMENT_3D ( 'NONE', #47451, #71100, #70734 ) ;
#28054=LINE ( 'NONE', #12612, #41478 ) ;
#28055=LINE ( 'NONE', #283, #24919 ) ;
#28061=CARTESIAN_POINT ( 'NONE',  ( 12.00000000000000000, -23.29833615347104470, 3.418703333116808629 ) ) ;
#28062=LINE ( 'NONE', #39360, #1027 ) ;
#28066=CIRCLE ( 'NONE', #38865, 82.00000000000000000 ) ;
#28075=DIRECTION ( 'NONE',  ( 0.000000000000000000, -0.8910065241883722287, 0.4539904997395382558 ) ) ;
#28076=EDGE_CURVE ( 'NONE', #4971, #38198, #8461, .T. ) ;
#28086=VECTOR ( 'NONE', #20754, 1000.000000000000000 ) ;
#28088=ORIENTED_EDGE ( 'NONE', *, *, #26603, .F. ) ;
#28091=EDGE_CURVE ( 'NONE', #17154, #18663, #9351, .T. ) ;
#28102=ORIENTED_EDGE ( 'NONE', *, *, #8936, .F. ) ;
#28106=VERTEX_POINT ( 'NONE', #59592 ) ;
#28112=EDGE_LOOP ( 'NONE', ( #8933, #66388, #40245, #2528 ) ) ;
#28121=CYLINDRICAL_SURFACE ( 'NONE', #69382, 77.49899999999999523 ) ;
#28130=ORIENTED_EDGE ( 'NONE', *, *, #5904, .T. ) ;
#28132=ORIENTED_EDGE ( 'NONE', *, *, #58838, .F. ) ;
#28136=ORIENTED_EDGE ( 'NONE', *, *, #46587, .F. ) ;
#28141=DIRECTION ( 'NONE',  ( -1.000000000000000000, -0.000000000000000000, 0.000000000000000000 ) ) ;
#28145=AXIS2_PLACEMENT_3D ( 'NONE', #9853, #39546, #33513 ) ;
#28146=VECTOR ( 'NONE', #12543, 1000.000000000000227 ) ;
#28153=DIRECTION ( 'NONE',  ( 0.000000000000000000, 0.000000000000000000, -1.000000000000000000 ) ) ;
#28156=CARTESIAN_POINT ( 'NONE',  ( 0.000000000000000000, -51.03279382321048985, -55.19960302592120627 ) ) ;
#28171=LINE ( 'NONE', #39468, #53903 ) ;
#28177=ORIENTED_EDGE ( 'NONE', *, *, #53240, .F. ) ;
#28181=EDGE_CURVE ( 'NONE', #25226, #20333, #63420, .T. ) ;
#28186=EDGE_LOOP ( 'NONE', ( #62486, #27831, #62917, #71149 ) ) ;
#28197=DIRECTION ( 'NONE',  ( -1.000000000000000000, 0.000000000000000000, 0.000000000000000000 ) ) ;
#28198=ORIENTED_EDGE ( 'NONE', *, *, #67234, .F. ) ;
#28205=FACE_OUTER_BOUND ( 'NONE', #42785, .T. ) ;
#28212=ORIENTED_EDGE ( 'NONE', *, *, #50607, .T. ) ;
#28213=ORIENTED_EDGE ( 'NONE', *, *, #22776, .T. ) ;
#28218=ORIENTED_EDGE ( 'NONE', *, *, #12373, .T. ) ;
#28225=PLANE ( 'NONE',  #50009 ) ;
#28244=EDGE_CURVE ( 'NONE', #232, #45393, #66987, .T. ) ;
#28248=EDGE_CURVE ( 'NONE', #53818, #63724, #15938, .T. ) ;
#28257=DIRECTION ( 'NONE',  ( -1.000000000000000000, 0.000000000000000000, 0.000000000000000000 ) ) ;
#28259=EDGE_CURVE ( 'NONE', #12497, #27167, #64631, .T. ) ;
#28265=ORIENTED_EDGE ( 'NONE', *, *, #16228, .T. ) ;
#28267=LINE ( 'NONE', #69611, #41874 ) ;
#28269=EDGE_LOOP ( 'NONE', ( #68893, #17297, #66643, #38658 ) ) ;
#28271=ORIENTED_EDGE ( 'NONE', *, *, #34368, .F. ) ;
#28281=EDGE_LOOP ( 'NONE', ( #30504, #40689, #60412, #18895 ) ) ;
#28284=AXIS2_PLACEMENT_3D ( 'NONE', #27282, #16770, #11486 ) ;
#28286=VERTEX_POINT ( 'NONE', #23081 ) ;
#28287=ORIENTED_EDGE ( 'NONE', *, *, #72987, .F. ) ;
#28290=EDGE_LOOP ( 'NONE', ( #58699, #32897, #40210, #7405 ) ) ;
#28291=AXIS2_PLACEMENT_3D ( 'NONE', #20061, #36251, #59192 ) ;
#28293=CARTESIAN_POINT ( 'NONE',  ( 0.000000000000000000, -26.01480285779885904, 70.53064760720306481 ) ) ;
#28299=LINE ( 'NONE', #58359, #68477 ) ;
#28300=CARTESIAN_POINT ( 'NONE',  ( -10.00000000000000000, 0.000000000000000000, 0.000000000000000000 ) ) ;
#28307=CIRCLE ( 'NONE', #47527, 31.99999999999998224 ) ;
#28313=FACE_OUTER_BOUND ( 'NONE', #48008, .T. ) ;
#28317=DIRECTION ( 'NONE',  ( -1.000000000000000000, 0.000000000000000000, 0.000000000000000000 ) ) ;
#28318=VERTEX_POINT ( 'NONE', #1298 ) ;
#28323=DIRECTION ( 'NONE',  ( 0.000000000000000000, -0.5877852522924802425, 0.8090169943749422332 ) ) ;
#28326=DIRECTION ( 'NONE',  ( -1.000000000000000000, 0.000000000000000000, -0.000000000000000000 ) ) ;
#28331=DIRECTION ( 'NONE',  ( 0.000000000000000000, -1.000000000000000000, -2.312964634635746211E-15 ) ) ;
#28333=EDGE_CURVE ( 'NONE', #71434, #26872, #11409, .T. ) ;
#28334=DIRECTION ( 'NONE',  ( -1.000000000000000000, 0.000000000000000000, 0.000000000000000000 ) ) ;
#28336=EDGE_CURVE ( 'NONE', #51303, #237, #4605, .T. ) ;
#28356=ORIENTED_EDGE ( 'NONE', *, *, #47229, .T. ) ;
#28360=ORIENTED_EDGE ( 'NONE', *, *, #12544, .F. ) ;
#28364=ORIENTED_EDGE ( 'NONE', *, *, #19872, .F. ) ;
#28374=DIRECTION ( 'NONE',  ( 0.000000000000000000, 0.7071067811865436870, 0.7071067811865513475 ) ) ;
#28379=VERTEX_POINT ( 'NONE', #18890 ) ;
#28380=ORIENTED_EDGE ( 'NONE', *, *, #18339, .F. ) ;
#28386=CARTESIAN_POINT ( 'NONE',  ( 6.000000000000000000, -71.87247863392384772, -39.47590169984923136 ) ) ;
#28400=EDGE_CURVE ( 'NONE', #27944, #5496, #32203, .T. ) ;
#28403=CARTESIAN_POINT ( 'NONE',  ( 15.00000000000000000, -18.13022148937263012, -15.02647892043543898 ) ) ;
#28413=CARTESIAN_POINT ( 'NONE',  ( 11.99999999999999822, -50.23322058963300663, -64.81221759200398935 ) ) ;
#28416=CARTESIAN_POINT ( 'NONE',  ( 0.000000000000000000, 64.81221759200417409, -50.23322058963276504 ) ) ;
#28422=VERTEX_POINT ( 'NONE', #13263 ) ;
#28424=CARTESIAN_POINT ( 'NONE',  ( 11.99999999999999822, 0.000000000000000000, 0.000000000000000000 ) ) ;
#28427=DIRECTION ( 'NONE',  ( 0.000000000000000000, 0.4067366430757989870, 0.9135454576426015327 ) ) ;
#28434=AXIS2_PLACEMENT_3D ( 'NONE', #51947, #35035, #45960 ) ;
#28439=CARTESIAN_POINT ( 'NONE',  ( 11.99999999999999822, 77.49459641780886443, -0.8261519478433960728 ) ) ;
#28441=DIRECTION ( 'NONE',  ( -1.000000000000000000, 0.000000000000000000, 0.000000000000000000 ) ) ;
#28444=EDGE_CURVE ( 'NONE', #44775, #4487, #59137, .T. ) ;
#28446=VERTEX_POINT ( 'NONE', #24544 ) ;
#28457=ORIENTED_EDGE ( 'NONE', *, *, #3403, .F. ) ;
#28462=DIRECTION ( 'NONE',  ( 1.000000000000000000, 0.000000000000000000, 0.000000000000000000 ) ) ;
#28463=CARTESIAN_POINT ( 'NONE',  ( 6.000000000000000000, 3.894527615417885169, 81.90746397400390322 ) ) ;
#28474=VECTOR ( 'NONE', #43940, 1000.000000000000000 ) ;
#28475=VERTEX_POINT ( 'NONE', #2404 ) ;
#28485=CARTESIAN_POINT ( 'NONE',  ( 11.99999999999999822, 0.000000000000000000, 0.000000000000000000 ) ) ;
#28487=DIRECTION ( 'NONE',  ( -1.000000000000000000, 0.000000000000000000, 0.000000000000000000 ) ) ;
#28492=ORIENTED_EDGE ( 'NONE', *, *, #20258, .F. ) ;
#28495=FACE_BOUND ( 'NONE', #6581, .T. ) ;
#28504=CARTESIAN_POINT ( 'NONE',  ( 11.99999999999999822, 22.90783923731740401, -78.73519480814930205 ) ) ;
#28505=LINE ( 'NONE', #33398, #74189 ) ;
#28506=CARTESIAN_POINT ( 'NONE',  ( 11.99999999999999822, 14.66109333815564852, -73.73191006444555740 ) ) ;
#28510=PLANE ( 'NONE',  #61857 ) ;
#28512=CARTESIAN_POINT ( 'NONE',  ( 12.00000000000000000, 18.84667830672579925, -18.68964196561269375 ) ) ;
#28519=CARTESIAN_POINT ( 'NONE',  ( 0.000000000000000000, 2.946379043146343246, 75.11764819372150725 ) ) ;
#28541=ORIENTED_EDGE ( 'NONE', *, *, #44563, .T. ) ;
#28544=ORIENTED_EDGE ( 'NONE', *, *, #50214, .F. ) ;
#28547=VECTOR ( 'NONE', #20977, 1000.000000000000000 ) ;
#28551=ORIENTED_EDGE ( 'NONE', *, *, #43714, .F. ) ;
#28554=ORIENTED_EDGE ( 'NONE', *, *, #40467, .F. ) ;
#28561=CYLINDRICAL_SURFACE ( 'NONE', #15487, 31.99999999999998579 ) ;
#28571=DIRECTION ( 'NONE',  ( 0.000000000000000000, -0.1564344650402381687, 0.9876883405951365491 ) ) ;
#28576=CIRCLE ( 'NONE', #70586, 77.49899999999998101 ) ;
#28578=DIRECTION ( 'NONE',  ( -1.000000000000000000, 0.000000000000000000, -0.000000000000000000 ) ) ;
#28586=CIRCLE ( 'NONE', #64609, 77.49899999999999523 ) ;
#28589=DIRECTION ( 'NONE',  ( 1.000000000000000000, 0.000000000000000000, 0.000000000000000000 ) ) ;
#28593=CARTESIAN_POINT ( 'NONE',  ( 15.00000000000000000, -10.45096189432314127, 21.10159698893440350 ) ) ;
#28597=CARTESIAN_POINT ( 'NONE',  ( 11.99999999999999822, 31.47745569255237896, -68.26794271651228030 ) ) ;
#28620=AXIS2_PLACEMENT_3D ( 'NONE', #66641, #42976, #26766 ) ;
#28622=EDGE_CURVE ( 'NONE', #10925, #72940, #72973, .T. ) ;
#28640=CARTESIAN_POINT ( 'NONE',  ( 0.000000000000000000, 0.000000000000000000, 0.000000000000000000 ) ) ;
#28647=VERTEX_POINT ( 'NONE', #49678 ) ;
#28649=CARTESIAN_POINT ( 'NONE',  ( 0.000000000000000000, -74.65374052328644439, -8.840884882375878107 ) ) ;
#28654=AXIS2_PLACEMENT_3D ( 'NONE', #30235, #71561, #53176 ) ;
#28657=EDGE_LOOP ( 'NONE', ( #15991, #71008, #63911, #35623 ) ) ;
#28665=DIRECTION ( 'NONE',  ( 0.000000000000000000, 0.000000000000000000, -1.000000000000000000 ) ) ;
#28672=DIRECTION ( 'NONE',  ( 0.000000000000000000, 0.000000000000000000, 1.000000000000000000 ) ) ;
#28688=AXIS2_PLACEMENT_3D ( 'NONE', #43957, #43231, #3021 ) ;
#28695=VERTEX_POINT ( 'NONE', #28982 ) ;
#28698=CIRCLE ( 'NONE', #64712, 82.00000000000000000 ) ;
#28702=DIRECTION ( 'NONE',  ( 0.000000000000000000, 0.000000000000000000, 1.000000000000000000 ) ) ;
#28704=CARTESIAN_POINT ( 'NONE',  ( 11.99999999999999822, 11.30684508768450769, -76.66974797899825944 ) ) ;
#28712=DIRECTION ( 'NONE',  ( 0.000000000000000000, 0.2334453638559060851, -0.9723699203976764460 ) ) ;
#28713=CYLINDRICAL_SURFACE ( 'NONE', #34673, 31.99999999999998579 ) ;
#28714=CARTESIAN_POINT ( 'NONE',  ( 0.000000000000000000, 0.000000000000000000, 0.000000000000000000 ) ) ;
#28727=LINE ( 'NONE', #212, #52129 ) ;
#28736=VERTEX_POINT ( 'NONE', #29708 ) ;
#28741=VERTEX_POINT ( 'NONE', #40270 ) ;
#28749=ORIENTED_EDGE ( 'NONE', *, *, #2511, .F. ) ;
#28752=ORIENTED_EDGE ( 'NONE', *, *, #3163, .F. ) ;
#28756=VERTEX_POINT ( 'NONE', #22992 ) ;
#28759=DIRECTION ( 'NONE',  ( -1.000000000000000000, 0.000000000000000000, 0.000000000000000000 ) ) ;
#28761=CARTESIAN_POINT ( 'NONE',  ( 11.99999999999999822, 41.76937507738788469, 62.50329211542452157 ) ) ;
#28763=CARTESIAN_POINT ( 'NONE',  ( 0.000000000000000000, -8.830959090342926032, 74.65491531819115778 ) ) ;
#28769=ORIENTED_EDGE ( 'NONE', *, *, #47709, .T. ) ;
#28784=ORIENTED_EDGE ( 'NONE', *, *, #29359, .F. ) ;
#28791=VECTOR ( 'NONE', #11170, 1000.000000000000000 ) ;
#28801=AXIS2_PLACEMENT_3D ( 'NONE', #27703, #40753, #73930 ) ;
#28802=EDGE_CURVE ( 'NONE', #38492, #3018, #9460, .T. ) ;
#28808=DIRECTION ( 'NONE',  ( 0.000000000000000000, 0.000000000000000000, 1.000000000000000000 ) ) ;
#28811=AXIS2_PLACEMENT_3D ( 'NONE', #73313, #26710, #5304 ) ;
#28812=DIRECTION ( 'NONE',  ( -1.000000000000000000, 0.000000000000000000, -0.000000000000000000 ) ) ;
#28815=LINE ( 'NONE', #650, #5782 ) ;
#28818=CARTESIAN_POINT ( 'NONE',  ( 11.99999999999999822, 27.74655509720779989, -77.16300072079630468 ) ) ;
#28819=ORIENTED_EDGE ( 'NONE', *, *, #43480, .T. ) ;
#28825=CYLINDRICAL_SURFACE ( 'NONE', #15037, 21.00000000000000000 ) ;
#28829=CARTESIAN_POINT ( 'NONE',  ( 0.000000000000000000, 76.69515212746057387, -29.01471420065479379 ) ) ;
#28835=ADVANCED_FACE ( 'NONE', ( #1938 ), #53400, .T. ) ;
#28845=AXIS2_PLACEMENT_3D ( 'NONE', #6789, #63213, #56828 ) ;
#28846=VERTEX_POINT ( 'NONE', #48498 ) ;
#28850=DIRECTION ( 'NONE',  ( 0.000000000000000000, -0.2334453638558922350, -0.9723699203976797767 ) ) ;
#28855=CYLINDRICAL_SURFACE ( 'NONE', #35334, 31.99999999999998579 ) ;
#28860=VERTEX_POINT ( 'NONE', #30820 ) ;
#28871=DIRECTION ( 'NONE',  ( 0.000000000000000000, 0.000000000000000000, 1.000000000000000000 ) ) ;
#28873=DIRECTION ( 'NONE',  ( 1.000000000000000000, 0.000000000000000000, 0.000000000000000000 ) ) ;
#28875=DIRECTION ( 'NONE',  ( 0.000000000000000000, -0.7431448254773878048, 0.6691306063588654540 ) ) ;
#28879=EDGE_LOOP ( 'NONE', ( #33830, #23488, #44793, #72179 ) ) ;
#28880=DIRECTION ( 'NONE',  ( -1.000000000000000000, 0.000000000000000000, -0.000000000000000000 ) ) ;
#28885=DIRECTION ( 'NONE',  ( 1.000000000000000000, 0.000000000000000000, 0.000000000000000000 ) ) ;
#28888=ORIENTED_EDGE ( 'NONE', *, *, #17902, .T. ) ;
#28890=CYLINDRICAL_SURFACE ( 'NONE', #4491, 82.00000000000000000 ) ;
#28891=DIRECTION ( 'NONE',  ( 1.000000000000000000, 0.000000000000000000, 0.000000000000000000 ) ) ;
#28899=DIRECTION ( 'NONE',  ( -1.000000000000000000, 0.000000000000000000, 0.000000000000000000 ) ) ;
#28901=DIRECTION ( 'NONE',  ( 1.000000000000000000, -0.000000000000000000, -0.000000000000000000 ) ) ;
#28905=VECTOR ( 'NONE', #43969, 1000.000000000000000 ) ;
#28906=DIRECTION ( 'NONE',  ( -1.000000000000000000, -0.000000000000000000, -0.000000000000000000 ) ) ;
#28909=CARTESIAN_POINT ( 'NONE',  ( 0.000000000000000000, -64.81221759200306565, -50.23322058963418613 ) ) ;
#28917=PLANE ( 'NONE',  #31773 ) ;
#28920=EDGE_LOOP ( 'NONE', ( #60015, #23618, #45403, #52808 ) ) ;
#28923=EDGE_CURVE ( 'NONE', #18767, #19565, #7899, .T. ) ;
#28932=VECTOR ( 'NONE', #21681, 1000.000000000000000 ) ;
#28936=ORIENTED_EDGE ( 'NONE', *, *, #68375, .F. ) ;
#28950=AXIS2_PLACEMENT_3D ( 'NONE', #59689, #59315, #71312 ) ;
#28956=EDGE_LOOP ( 'NONE', ( #7402, #69561, #12091, #63629 ) ) ;
#28958=ORIENTED_EDGE ( 'NONE', *, *, #23625, .T. ) ;
#28961=DIRECTION ( 'NONE',  ( -1.000000000000000000, 0.000000000000000000, 0.000000000000000000 ) ) ;
#28971=ADVANCED_FACE ( 'NONE', ( #38329 ), #49962, .T. ) ;
#28974=CARTESIAN_POINT ( 'NONE',  ( 11.99999999999999822, 68.67312586195046720, -35.91791733033404199 ) ) ;
#28978=DIRECTION ( 'NONE',  ( 1.000000000000000000, 0.000000000000000000, -0.000000000000000000 ) ) ;
#28982=CARTESIAN_POINT ( 'NONE',  ( 11.99999999999999822, 3.894527615419054456, -81.90746397400384637 ) ) ;
#28984=ORIENTED_EDGE ( 'NONE', *, *, #31632, .F. ) ;
#28988=DIRECTION ( 'NONE',  ( 0.000000000000000000, -0.1564344650402381687, 0.9876883405951365491 ) ) ;
#28994=AXIS2_PLACEMENT_3D ( 'NONE', #49849, #50974, #73522 ) ;
#29011=ORIENTED_EDGE ( 'NONE', *, *, #19674, .F. ) ;
#29015=ADVANCED_FACE ( 'NONE', ( #20665 ), #39078, .F. ) ;
#29027=ORIENTED_EDGE ( 'NONE', *, *, #66046, .F. ) ;
#29043=CARTESIAN_POINT ( 'NONE',  ( 11.99999999999999822, -73.72996012237449293, 14.67089635893687571 ) ) ;
#29044=CARTESIAN_POINT ( 'NONE',  ( 0.000000000000000000, -60.67117009219096957, -55.16347631943106933 ) ) ;
#29045=DIRECTION ( 'NONE',  ( 0.000000000000000000, 0.7604059656000276002, 0.6494480483301875440 ) ) ;
#29046=DIRECTION ( 'NONE',  ( 0.000000000000000000, 0.000000000000000000, 1.000000000000000000 ) ) ;
#29071=CARTESIAN_POINT ( 'NONE',  ( 11.99999999999999822, -51.03279382321125723, 55.19960302592048862 ) ) ;
#29076=DIRECTION ( 'NONE',  ( 0.000000000000000000, -0.07845909572783056618, -0.9969173337331290741 ) ) ;
#29078=DIRECTION ( 'NONE',  ( -1.000000000000000000, -0.000000000000000000, -0.000000000000000000 ) ) ;
#29079=DIRECTION ( 'NONE',  ( 0.000000000000000000, -0.9135454576426010886, 0.4067366430757998752 ) ) ;
#29082=EDGE_CURVE ( 'NONE', #8991, #66021, #55986, .T. ) ;
#29086=CARTESIAN_POINT ( 'NONE',  ( 15.00000000000000000, 9.615535125378766423, -24.73947219025917121 ) ) ;
#29092=EDGE_CURVE ( 'NONE', #37544, #71894, #15521, .T. ) ;
#29099=VECTOR ( 'NONE', #17593, 1000.000000000000114 ) ;
#29100=EDGE_CURVE ( 'NONE', #31915, #64655, #31935, .T. ) ;
#29105=DIRECTION ( 'NONE',  ( 0.000000000000000000, 1.000000000000000000, 1.301042606982602757E-15 ) ) ;
#29120=CARTESIAN_POINT ( 'NONE',  ( 11.99999999999999822, 11.30684508768450769, -76.66974797899825944 ) ) ;
#29125=FACE_OUTER_BOUND ( 'NONE', #35866, .T. ) ;
#29130=ORIENTED_EDGE ( 'NONE', *, *, #43843, .T. ) ;
#29132=ORIENTED_EDGE ( 'NONE', *, *, #47109, .F. ) ;
#29134=EDGE_CURVE ( 'NONE', #3531, #12759, #34536, .T. ) ;
#29138=EDGE_LOOP ( 'NONE', ( #8765, #9355, #33214, #58187, #38276, #84, #5003, #35253, #13459, #59932, #72320, #24877, #65358, #15539, #8200, #50857, #24795, #52047, #44864, #57439, #13119, #65479, #32801, #66373, #1294, #29520, #53723, #14378, #41306, #61332, #5938, #38202, #3740, #7669, #34773, #48083, #73315, #58786, #49364, #38384, #56080, #38748, #28271, #67889, #69971, #69101, #15202, #38378, #1048, #46816, #55702, #70906, #20803, #62529, #55376, #57537, #32550, #18480, #30497, #28888, #11287, #72426, #37561, #42638, #60991, #10677, #70149, #64225, #14506, #1902, #21672, #54191, #40308, #59656, #8030, #60007, #42201, #9499, #32069, #41990, #53243, #38, #21984, #36036, #15069, #20921, #34407, #3358, #62148, #44313, #59844, #41330, #28360, #262, #41970, #37447, #71210, #26614, #56412, #58259, #46725, #40164, #3106, #68438, #803, #36446, #52839, #73616, #26367, #69195, #12182, #5036, #45818, #9990, #20963, #22852, #4421, #35005, #32693, #56149, #35196, #25363, #39575, #53991, #15343, #6747, #34893, #32366, #13128, #35884, #1907, #10331, #19676, #22487, #20615, #18641, #50468, #45586, #66518, #1063, #10663, #38963, #6589, #3236, #21458, #35663, #7513, #68976, #24047, #599, #3656, #71541, #50572, #57611, #48272, #67368, #62243, #25832, #52974, #17566, #9605, #21991, #47418, #64556, #35991, #11651, #10730, #50082, #9124, #70380, #64623, #5368, #68751, #69468, #45128, #10853, #69020, #72384, #58467, #52881, #60560, #30118, #20892, #49731, #41, #2165, #73346, #51962, #39859, #48482, #61529, #17974, #50779, #18107, #37738, #48830, #60931, #14295, #23622, #5279, #7866, #34127, #56039, #29663, #28749, #54107, #51373, #54799, #65037, #1971, #65331, #45598, #65475, #44782, #57775, #43499, #21074, #49890, #73674, #13430, #6486, #57083, #35044, #33980, #68717, #70096, #15902, #52179, #5111, #48722, #9513, #49013, #71875, #65392, #39581, #49501, #37929, #3089, #64096, #30408, #21815, #4091, #59155, #34106, #46525, #20353, #67350, #64744, #4934, #30596, #46952, #9527, #64413, #60204, #55499, #12304, #21905, #57092, #65936, #72078, #52335, #39704, #71827, #12432, #52034, #30750, #17404, #51586, #48750, #43131, #65039, #68704, #49661, #5090, #25231, #41343, #11837, #1700, #28102, #3095, #40134, #32876, #2984, #42998, #64194, #51297, #49441, #12215, #8886, #62029, #67601, #31634, #57451, #29653, #49027, #34234, #2797, #19756, #972, #30401, #4833, #5510, #24581, #38368, #22597, #1822, #24670, #44468, #12271, #19408, #56400, #9880, #4311, #74175, #10472, #41138, #56113, #4865, #60028, #9549, #73319, #16565, #1189, #53005, #68079 ) ) ;
#29142=CARTESIAN_POINT ( 'NONE',  ( 11.99999999999999822, -46.53671651293907274, -59.03961581697448935 ) ) ;
#29163=CARTESIAN_POINT ( 'NONE',  ( 11.99999999999999822, -55.20638768913797634, 51.02545421589302777 ) ) ;
#29166=FACE_OUTER_BOUND ( 'NONE', #29744, .T. ) ;
#29173=CARTESIAN_POINT ( 'NONE',  ( 11.99999999999999822, 0.000000000000000000, 0.000000000000000000 ) ) ;
#29186=VECTOR ( 'NONE', #38074, 1000.000000000000000 ) ;
#29193=CIRCLE ( 'NONE', #61638, 31.99999999999998579 ) ;
#29201=VERTEX_POINT ( 'NONE', #17622 ) ;
#29203=ORIENTED_EDGE ( 'NONE', *, *, #34272, .T. ) ;
#29216=DIRECTION ( 'NONE',  ( 0.000000000000000000, 0.000000000000000000, 1.000000000000000000 ) ) ;
#29219=VERTEX_POINT ( 'NONE', #18718 ) ;
#29225=CYLINDRICAL_SURFACE ( 'NONE', #60479, 77.49899999999999523 ) ;
#29226=DIRECTION ( 'NONE',  ( 0.000000000000000000, 0.000000000000000000, 1.000000000000000000 ) ) ;
#29229=CARTESIAN_POINT ( 'NONE',  ( 0.000000000000000000, 0.000000000000000000, 0.000000000000000000 ) ) ;
#29232=ORIENTED_EDGE ( 'NONE', *, *, #48525, .T. ) ;
#29245=DIRECTION ( 'NONE',  ( 0.000000000000000000, 0.000000000000000000, -1.000000000000000000 ) ) ;
#29246=ORIENTED_EDGE ( 'NONE', *, *, #24751, .F. ) ;
#29249=CARTESIAN_POINT ( 'NONE',  ( 15.00000000000000000, 24.81905959214275370, 9.408202855044498492 ) ) ;
#29253=DIRECTION ( 'NONE',  ( 0.000000000000000000, 0.4999999999999938938, -0.8660254037844421493 ) ) ;
#29260=DIRECTION ( 'NONE',  ( -1.000000000000000000, 0.000000000000000000, 0.000000000000000000 ) ) ;
#29261=PRODUCT_DEFINITION ( 'UNKNOWN', '', #31660, #14564 ) ;
#29266=AXIS2_PLACEMENT_3D ( 'NONE', #36848, #48503, #48139 ) ;
#29267=CARTESIAN_POINT ( 'NONE',  ( 11.99999999999999822, 0.000000000000000000, 0.000000000000000000 ) ) ;
#29269=EDGE_CURVE ( 'NONE', #4105, #29346, #54058, .T. ) ;
#29273=DIRECTION ( 'NONE',  ( 0.000000000000000000, 0.000000000000000000, 1.000000000000000000 ) ) ;
#29276=AXIS2_PLACEMENT_3D ( 'NONE', #39791, #33765, #45060 ) ;
#29284=VERTEX_POINT ( 'NONE', #64235 ) ;
#29295=LINE ( 'NONE', #56414, #24436 ) ;
#29305=ORIENTED_EDGE ( 'NONE', *, *, #16290, .T. ) ;
#29309=AXIS2_PLACEMENT_3D ( 'NONE', #51274, #16703, #16329 ) ;
#29311=DIRECTION ( 'NONE',  ( 0.000000000000000000, 0.000000000000000000, 1.000000000000000000 ) ) ;
#29315=ORIENTED_EDGE ( 'NONE', *, *, #13212, .F. ) ;
#29316=VERTEX_POINT ( 'NONE', #71319 ) ;
#29333=CIRCLE ( 'NONE', #14905, 77.49899999999998101 ) ;
#29346=VERTEX_POINT ( 'NONE', #30368 ) ;
#29347=DIRECTION ( 'NONE',  ( 0.000000000000000000, 0.000000000000000000, 1.000000000000000000 ) ) ;
#29356=DIRECTION ( 'NONE',  ( 0.000000000000000000, 0.9723699203976773342, -0.2334453638559024491 ) ) ;
#29359=EDGE_CURVE ( 'NONE', #72240, #54635, #7098, .T. ) ;
#29360=DIRECTION ( 'NONE',  ( -1.000000000000000000, 0.000000000000000000, 0.000000000000000000 ) ) ;
#29363=DIRECTION ( 'NONE',  ( -1.000000000000000000, -0.000000000000000000, 0.000000000000000000 ) ) ;
#29364=CARTESIAN_POINT ( 'NONE',  ( 0.000000000000000000, -68.26794271651239399, -31.47745569255214093 ) ) ;
#29374=CARTESIAN_POINT ( 'NONE',  ( 0.000000000000000000, -51.02545421589285723, -55.20638768913812555 ) ) ;
#29376=EDGE_LOOP ( 'NONE', ( #5120, #49942, #57890, #9138 ) ) ;
#29377=CIRCLE ( 'NONE', #30563, 77.49899999999999523 ) ;
#29392=ORIENTED_EDGE ( 'NONE', *, *, #35043, .F. ) ;
#29398=DIRECTION ( 'NONE',  ( -1.000000000000000000, 0.000000000000000000, -0.000000000000000000 ) ) ;
#29401=FACE_OUTER_BOUND ( 'NONE', #26189, .T. ) ;
#29421=ADVANCED_FACE ( 'NONE', ( #20584 ), #16047, .F. ) ;
#29425=CARTESIAN_POINT ( 'NONE',  ( -10.00000000000000000, 0.000000000000000000, 0.000000000000000000 ) ) ;
#29440=LINE ( 'NONE', #52382, #40015 ) ;
#29449=DIRECTION ( 'NONE',  ( -1.000000000000000000, -0.000000000000000000, -0.000000000000000000 ) ) ;
#29450=DIRECTION ( 'NONE',  ( 0.000000000000000000, 0.000000000000000000, 1.000000000000000000 ) ) ;
#29455=ORIENTED_EDGE ( 'NONE', *, *, #34272, .F. ) ;
#29457=EDGE_CURVE ( 'NONE', #66558, #40071, #53781, .T. ) ;
#29461=DIRECTION ( 'NONE',  ( -1.000000000000000000, 0.000000000000000000, 0.000000000000000000 ) ) ;
#29463=VERTEX_POINT ( 'NONE', #26947 ) ;
#29476=CARTESIAN_POINT ( 'NONE',  ( 15.00000000000000000, -3.948201729842032215, 23.21447184625297666 ) ) ;
#29478=AXIS2_PLACEMENT_3D ( 'NONE', #65228, #36637, #69742 ) ;
#29488=CARTESIAN_POINT ( 'NONE',  ( -10.00000000000000000, 0.000000000000000000, 0.000000000000000000 ) ) ;
#29490=CARTESIAN_POINT ( 'NONE',  ( 0.000000000000000000, 0.000000000000000000, 0.000000000000000000 ) ) ;
#29501=VERTEX_POINT ( 'NONE', #73185 ) ;
#29504=CARTESIAN_POINT ( 'NONE',  ( 11.99999999999999822, -59.03961581697367933, -46.53671651294010303 ) ) ;
#29506=CARTESIAN_POINT ( 'NONE',  ( 11.99999999999999822, 54.21277698773675979, 55.38113227695801299 ) ) ;
#29508=EDGE_LOOP ( 'NONE', ( #41075, #12473, #12684, #47888 ) ) ;
#29511=ORIENTED_EDGE ( 'NONE', *, *, #68281, .T. ) ;
#29520=ORIENTED_EDGE ( 'NONE', *, *, #26303, .T. ) ;
#29525=CIRCLE ( 'NONE', #53527, 31.99999999999998934 ) ;
#29528=LINE ( 'NONE', #1393, #57671 ) ;
#29544=ADVANCED_FACE ( 'NONE', ( #50625 ), #34079, .T. ) ;
#29549=LINE ( 'NONE', #59537, #42067 ) ;
#29551=EDGE_CURVE ( 'NONE', #73160, #1543, #28062, .T. ) ;
#29555=EDGE_LOOP ( 'NONE', ( #259, #18015, #56120, #1506 ) ) ;
#29560=CARTESIAN_POINT ( 'NONE',  ( 0.000000000000000000, -63.18004540533059554, 44.88180994100355292 ) ) ;
#29561=CARTESIAN_POINT ( 'NONE',  ( 6.000000000000000000, 74.18225833017888249, 34.94270380257665209 ) ) ;
#29578=ORIENTED_EDGE ( 'NONE', *, *, #70833, .F. ) ;
#29590=CARTESIAN_POINT ( 'NONE',  ( 0.000000000000000000, -18.89407956138310496, 75.16055320797023853 ) ) ;
#29595=FACE_BOUND ( 'NONE', #51355, .T. ) ;
#29597=ADVANCED_FACE ( 'NONE', ( #17899 ), #22062, .T. ) ;
#29603=ORIENTED_EDGE ( 'NONE', *, *, #58666, .F. ) ;
#29605=CARTESIAN_POINT ( 'NONE',  ( 0.000000000000000000, -44.88180994100419952, 63.18004540533013369 ) ) ;
#29615=LINE ( 'NONE', #48038, #10863 ) ;
#29622=AXIS2_PLACEMENT_3D ( 'NONE', #23257, #11961, #69478 ) ;
#29625=CARTESIAN_POINT ( 'NONE',  ( 15.00000000000000000, -25.60904388321916159, 6.976881207771517879 ) ) ;
#29627=EDGE_CURVE ( 'NONE', #10925, #70197, #28815, .T. ) ;
#29629=LINE ( 'NONE', #6361, #22668 ) ;
#29633=ORIENTED_EDGE ( 'NONE', *, *, #73220, .T. ) ;
#29634=DIRECTION ( 'NONE',  ( -1.000000000000000000, 0.000000000000000000, 0.000000000000000000 ) ) ;
#29639=CARTESIAN_POINT ( 'NONE',  ( 0.000000000000000000, -71.87247863392443037, 39.47590169984818687 ) ) ;
#29645=CARTESIAN_POINT ( 'NONE',  ( 11.99999999999999822, 0.000000000000000000, 0.000000000000000000 ) ) ;
#29646=VERTEX_POINT ( 'NONE', #290 ) ;
#29653=ORIENTED_EDGE ( 'NONE', *, *, #58131, .T. ) ;
#29661=ORIENTED_EDGE ( 'NONE', *, *, #3493, .T. ) ;
#29663=ORIENTED_EDGE ( 'NONE', *, *, #48701, .T. ) ;
#29672=VERTEX_POINT ( 'NONE', #45383 ) ;
#29677=VERTEX_POINT ( 'NONE', #4801 ) ;
#29679=ADVANCED_FACE ( 'NONE', ( #17166 ), #16424, .T. ) ;
#29686=ORIENTED_EDGE ( 'NONE', *, *, #35471, .F. ) ;
#29701=DIRECTION ( 'NONE',  ( 0.000000000000000000, 0.000000000000000000, 1.000000000000000000 ) ) ;
#29702=DIRECTION ( 'NONE',  ( 0.000000000000000000, 0.000000000000000000, -1.000000000000000000 ) ) ;
#29708=CARTESIAN_POINT ( 'NONE',  ( 11.99999999999999822, -76.69515212745996280, -29.01471420065643869 ) ) ;
#29714=EDGE_CURVE ( 'NONE', #11167, #2055, #23794, .T. ) ;
#29722=CIRCLE ( 'NONE', #47766, 31.99999999999998579 ) ;
#29743=ORIENTED_EDGE ( 'NONE', *, *, #59865, .T. ) ;
#29744=EDGE_LOOP ( 'NONE', ( #19862, #27628, #23119, #5878 ) ) ;
#29745=CIRCLE ( 'NONE', #71773, 82.00000000000000000 ) ;
#29748=AXIS2_PLACEMENT_3D ( 'NONE', #11531, #16819, #57407 ) ;
#29755=DIRECTION ( 'NONE',  ( 0.000000000000000000, -0.5877852522924624790, -0.8090169943749551118 ) ) ;
#29767=DIRECTION ( 'NONE',  ( 0.000000000000000000, -0.3826834323650970537, 0.9238795325112838519 ) ) ;
#29777=ORIENTED_EDGE ( 'NONE', *, *, #44165, .T. ) ;
#29782=CARTESIAN_POINT ( 'NONE',  ( 11.99999999999999822, 0.000000000000000000, 0.000000000000000000 ) ) ;
#29790=CARTESIAN_POINT ( 'NONE',  ( 11.99999999999999822, 22.90783923731629201, 78.73519480814962890 ) ) ;
#29792=ORIENTED_EDGE ( 'NONE', *, *, #9944, .T. ) ;
#29793=AXIS2_PLACEMENT_3D ( 'NONE', #22712, #18527, #28323 ) ;
#29802=LINE ( 'NONE', #5796, #25408 ) ;
#29810=VECTOR ( 'NONE', #72928, 1000.000000000000000 ) ;
#29811=CARTESIAN_POINT ( 'NONE',  ( 11.99999999999999822, -50.95692526931287603, -58.39081064771804819 ) ) ;
#29812=DIRECTION ( 'NONE',  ( 0.000000000000000000, -0.4067366430757899942, 0.9135454576426055295 ) ) ;
#29818=DIRECTION ( 'NONE',  ( -1.000000000000000000, -0.000000000000000000, -0.000000000000000000 ) ) ;
#29821=ORIENTED_EDGE ( 'NONE', *, *, #61190, .T. ) ;
#29822=DIRECTION ( 'NONE',  ( 0.000000000000000000, 0.2334453638558991462, 0.9723699203976781114 ) ) ;
#29828=ADVANCED_FACE ( 'NONE', ( #31017 ), #58875, .F. ) ;
#29832=CARTESIAN_POINT ( 'NONE',  ( 0.000000000000000000, 0.000000000000000000, 0.000000000000000000 ) ) ;
#29836=DIRECTION ( 'NONE',  ( 0.000000000000000000, -1.301042606982602560E-15, 1.000000000000000000 ) ) ;
#29843=EDGE_CURVE ( 'NONE', #41355, #12604, #19001, .T. ) ;
#29844=ORIENTED_EDGE ( 'NONE', *, *, #62423, .T. ) ;
#29847=LINE ( 'NONE', #52803, #53985 ) ;
#29850=ORIENTED_EDGE ( 'NONE', *, *, #52112, .T. ) ;
#29853=ORIENTED_EDGE ( 'NONE', *, *, #53238, .F. ) ;
#29860=CARTESIAN_POINT ( 'NONE',  ( 0.000000000000000000, 0.000000000000000000, 0.000000000000000000 ) ) ;
#29879=FACE_OUTER_BOUND ( 'NONE', #29376, .T. ) ;
#29901=CARTESIAN_POINT ( 'NONE',  ( 11.99999999999999822, 0.000000000000000000, 0.000000000000000000 ) ) ;
#29906=DIRECTION ( 'NONE',  ( 0.000000000000000000, 0.000000000000000000, 1.000000000000000000 ) ) ;
#29910=AXIS2_PLACEMENT_3D ( 'NONE', #32202, #16415, #49139 ) ;
#29927=EDGE_CURVE ( 'NONE', #27546, #64186, #50441, .T. ) ;
#29930=EDGE_CURVE ( 'NONE', #23323, #74042, #55012, .T. ) ;
#29933=CARTESIAN_POINT ( 'NONE',  ( 11.99999999999999822, 0.000000000000000000, 0.000000000000000000 ) ) ;
#29936=CARTESIAN_POINT ( 'NONE',  ( 11.99999999999999822, 73.95703589263975175, 23.16143007188452785 ) ) ;
#29943=EDGE_CURVE ( 'NONE', #23233, #55121, #64625, .T. ) ;
#29948=CARTESIAN_POINT ( 'NONE',  ( 11.99999999999999822, 0.000000000000000000, 0.000000000000000000 ) ) ;
#29956=CYLINDRICAL_SURFACE ( 'NONE', #11946, 82.00000000000000000 ) ;
#29957=ORIENTED_EDGE ( 'NONE', *, *, #5196, .F. ) ;
#29960=ORIENTED_EDGE ( 'NONE', *, *, #12405, .F. ) ;
#29964=ORIENTED_EDGE ( 'NONE', *, *, #53571, .F. ) ;
#29967=CARTESIAN_POINT ( 'NONE',  ( 0.000000000000000000, 0.000000000000000000, 0.000000000000000000 ) ) ;
#29971=VERTEX_POINT ( 'NONE', #59993 ) ;
#29972=DIRECTION ( 'NONE',  ( 0.000000000000000000, 0.000000000000000000, 1.000000000000000000 ) ) ;
#29980=VECTOR ( 'NONE', #71922, 1000.000000000000000 ) ;
#29982=EDGE_CURVE ( 'NONE', #17939, #20251, #70610, .T. ) ;
#29987=ORIENTED_EDGE ( 'NONE', *, *, #17176, .T. ) ;
#29995=DIRECTION ( 'NONE',  ( -1.000000000000000000, 0.000000000000000000, 0.000000000000000000 ) ) ;
#30001=CARTESIAN_POINT ( 'NONE',  ( 11.99999999999999822, -59.46389618801929089, -49.70050353004953081 ) ) ;
#30002=DIRECTION ( 'NONE',  ( 1.000000000000000000, -0.000000000000000000, -0.000000000000000000 ) ) ;
#30020=ORIENTED_EDGE ( 'NONE', *, *, #49494, .T. ) ;
#30023=EDGE_LOOP ( 'NONE', ( #7005, #7064, #19323, #8338 ) ) ;
#30030=EDGE_LOOP ( 'NONE', ( #2814, #28287, #60956, #34005 ) ) ;
#30035=AXIS2_PLACEMENT_3D ( 'NONE', #1125, #18000, #64606 ) ;
#30036=VERTEX_POINT ( 'NONE', #51924 ) ;
#30038=DIRECTION ( 'NONE',  ( 0.000000000000000000, -0.7071067811865389130, -0.7071067811865562325 ) ) ;
#30039=ORIENTED_EDGE ( 'NONE', *, *, #40263, .T. ) ;
#30045=DIRECTION ( 'NONE',  ( 1.000000000000000000, 0.000000000000000000, 0.000000000000000000 ) ) ;
#30049=ORIENTED_EDGE ( 'NONE', *, *, #40670, .F. ) ;
#30069=FACE_OUTER_BOUND ( 'NONE', #57444, .T. ) ;
#30072=LINE ( 'NONE', #71028, #44396 ) ;
#30078=CARTESIAN_POINT ( 'NONE',  ( 11.99999999999999822, 65.58780272294129077, -36.73666225445822420 ) ) ;
#30087=DIRECTION ( 'NONE',  ( -1.000000000000000000, 0.000000000000000000, 0.000000000000000000 ) ) ;
#30105=AXIS2_PLACEMENT_3D ( 'NONE', #58121, #7364, #18626 ) ;
#30110=EDGE_CURVE ( 'NONE', #53386, #8327, #51423, .T. ) ;
#30112=CYLINDRICAL_SURFACE ( 'NONE', #39173, 31.99999999999998579 ) ;
#30118=ORIENTED_EDGE ( 'NONE', *, *, #6534, .T. ) ;
#30119=DIRECTION ( 'NONE',  ( -1.000000000000000000, 0.000000000000000000, -0.000000000000000000 ) ) ;
#30129=DIRECTION ( 'NONE',  ( 0.000000000000000000, 0.9723699203976773342, -0.2334453638559024213 ) ) ;
#30134=EDGE_CURVE ( 'NONE', #34985, #46802, #40647, .T. ) ;
#30137=DIRECTION ( 'NONE',  ( -1.000000000000000000, -0.000000000000000000, 0.000000000000000000 ) ) ;
#30138=ORIENTED_EDGE ( 'NONE', *, *, #42295, .T. ) ;
#30139=LINE ( 'NONE', #69984, #70810 ) ;
#30145=EDGE_CURVE ( 'NONE', #35960, #10633, #5831, .T. ) ;
#30150=DIRECTION ( 'NONE',  ( -1.000000000000000000, 0.000000000000000000, 0.000000000000000000 ) ) ;
#30156=ORIENTED_EDGE ( 'NONE', *, *, #8737, .T. ) ;
#30163=CARTESIAN_POINT ( 'NONE',  ( 15.00000000000000000, 8.688484142254226938, 21.88630264137359305 ) ) ;
#30165=DIRECTION ( 'NONE',  ( -1.000000000000000000, -0.000000000000000000, 0.000000000000000000 ) ) ;
#30168=CARTESIAN_POINT ( 'NONE',  ( 12.00000000000000000, -22.67460108101782978, -6.353146135317906840 ) ) ;
#30176=VECTOR ( 'NONE', #53649, 1000.000000000000114 ) ;
#30187=VECTOR ( 'NONE', #23592, 999.9999999999998863 ) ;
#30193=CARTESIAN_POINT ( 'NONE',  ( 0.000000000000000000, -79.10210256391383155, 21.60688246758558506 ) ) ;
#30202=CARTESIAN_POINT ( 'NONE',  ( 11.99999999999999822, -46.54456581323762521, -59.03342792756313884 ) ) ;
#30212=ORIENTED_EDGE ( 'NONE', *, *, #48864, .T. ) ;
#30215=ORIENTED_EDGE ( 'NONE', *, *, #69316, .F. ) ;
#30217=DIRECTION ( 'NONE',  ( -1.000000000000000000, 0.000000000000000000, 0.000000000000000000 ) ) ;
#30221=ORIENTED_EDGE ( 'NONE', *, *, #50475, .T. ) ;
#30224=AXIS2_PLACEMENT_3D ( 'NONE', #70101, #57359, #52833 ) ;
#30230=DIRECTION ( 'NONE',  ( 0.000000000000000000, -0.8660254037844432595, -0.4999999999999919509 ) ) ;
#30232=VERTEX_POINT ( 'NONE', #64692 ) ;
#30234=ORIENTED_EDGE ( 'NONE', *, *, #49729, .T. ) ;
#30235=CARTESIAN_POINT ( 'NONE',  ( 0.000000000000000000, 0.000000000000000000, 0.000000000000000000 ) ) ;
#30236=VERTEX_POINT ( 'NONE', #60541 ) ;
#30239=DIRECTION ( 'NONE',  ( 0.000000000000000000, -0.4539904997395350361, -0.8910065241883738940 ) ) ;
#30244=DIRECTION ( 'NONE',  ( -1.000000000000000000, 0.000000000000000000, 0.000000000000000000 ) ) ;
#30251=EDGE_LOOP ( 'NONE', ( #39034, #63181, #55492, #8971 ) ) ;
#30257=CARTESIAN_POINT ( 'NONE',  ( 11.99999999999999822, 0.000000000000000000, 0.000000000000000000 ) ) ;
#30259=CARTESIAN_POINT ( 'NONE',  ( 0.000000000000000000, 68.67312586194995561, 35.91791733033500122 ) ) ;
#30276=CYLINDRICAL_SURFACE ( 'NONE', #72819, 77.49899999999999523 ) ;
#30284=CIRCLE ( 'NONE', #7475, 31.99999999999998579 ) ;
#30290=CARTESIAN_POINT ( 'NONE',  ( 11.99999999999999822, 0.000000000000000000, 0.000000000000000000 ) ) ;
#30297=ORIENTED_EDGE ( 'NONE', *, *, #19247, .T. ) ;
#30315=VERTEX_POINT ( 'NONE', #66181 ) ;
#30327=ORIENTED_EDGE ( 'NONE', *, *, #73518, .T. ) ;
#30339=DIRECTION ( 'NONE',  ( -1.000000000000000000, 0.000000000000000000, 0.000000000000000000 ) ) ;
#30342=DIRECTION ( 'NONE',  ( 0.000000000000000000, -0.2079116908177664758, -0.9781476007338042455 ) ) ;
#30345=DIRECTION ( 'NONE',  ( -1.000000000000000000, -0.000000000000000000, -0.000000000000000000 ) ) ;
#30347=EDGE_LOOP ( 'NONE', ( #62717, #8106, #33179, #58640 ) ) ;
#30349=CARTESIAN_POINT ( 'NONE',  ( 11.99999999999999822, 26.01480285779933510, -70.53064760720289428 ) ) ;
#30355=ADVANCED_FACE ( 'NONE', ( #42501 ), #25573, .T. ) ;
#30359=CARTESIAN_POINT ( 'NONE',  ( -10.00000000000000000, 0.000000000000000000, 0.000000000000000000 ) ) ;
#30361=CARTESIAN_POINT ( 'NONE',  ( 11.99999999999999822, 0.000000000000000000, 0.000000000000000000 ) ) ;
#30362=DIRECTION ( 'NONE',  ( 0.000000000000000000, 0.000000000000000000, -1.000000000000000000 ) ) ;
#30363=EDGE_CURVE ( 'NONE', #52399, #71078, #47758, .T. ) ;
#30364=DIRECTION ( 'NONE',  ( -1.000000000000000000, 0.000000000000000000, -0.000000000000000000 ) ) ;
#30368=CARTESIAN_POINT ( 'NONE',  ( 0.000000000000000000, -66.50666863322028632, 39.78640506895582973 ) ) ;
#30370=CARTESIAN_POINT ( 'NONE',  ( 12.00000000000000000, -14.54903810567644484, 22.19967320028775504 ) ) ;
#30375=AXIS2_PLACEMENT_3D ( 'NONE', #29832, #59170, #52789 ) ;
#30380=DIRECTION ( 'NONE',  ( -0.000000000000000000, 0.9135454576426060846, 0.4067366430757888285 ) ) ;
#30382=CARTESIAN_POINT ( 'NONE',  ( 0.000000000000000000, 0.000000000000000000, 0.000000000000000000 ) ) ;
#30388=ORIENTED_EDGE ( 'NONE', *, *, #11475, .F. ) ;
#30393=EDGE_CURVE ( 'NONE', #47808, #24268, #49114, .T. ) ;
#30400=ORIENTED_EDGE ( 'NONE', *, *, #31884, .F. ) ;
#30401=ORIENTED_EDGE ( 'NONE', *, *, #56433, .T. ) ;
#30403=DIRECTION ( 'NONE',  ( -1.000000000000000000, 0.000000000000000000, 0.000000000000000000 ) ) ;
#30408=ORIENTED_EDGE ( 'NONE', *, *, #70232, .T. ) ;
#30411=AXIS2_PLACEMENT_3D ( 'NONE', #54057, #58962, #20195 ) ;
#30413=VERTEX_POINT ( 'NONE', #54882 ) ;
#30426=DIRECTION ( 'NONE',  ( 0.000000000000000000, 1.445602896647339410E-16, -1.000000000000000000 ) ) ;
#30431=VECTOR ( 'NONE', #17290, 999.9999999999998863 ) ;
#30432=CARTESIAN_POINT ( 'NONE',  ( 0.000000000000000000, 68.26794271651307611, -31.47745569255064169 ) ) ;
#30439=DIRECTION ( 'NONE',  ( 1.000000000000000000, 0.000000000000000000, 0.000000000000000000 ) ) ;
#30444=AXIS2_PLACEMENT_3D ( 'NONE', #18993, #35554, #29906 ) ;
#30447=LINE ( 'NONE', #14271, #8459 ) ;
#30454=PLANE ( 'NONE',  #23052 ) ;
#30462=DIRECTION ( 'NONE',  ( 0.000000000000000000, 1.000000000000000000, 3.469446951953616555E-15 ) ) ;
#30467=ORIENTED_EDGE ( 'NONE', *, *, #40948, .F. ) ;
#30468=DIRECTION ( 'NONE',  ( -1.000000000000000000, -0.000000000000000000, -0.000000000000000000 ) ) ;
#30475=AXIS2_PLACEMENT_3D ( 'NONE', #62439, #27447, #57160 ) ;
#30485=AXIS2_PLACEMENT_3D ( 'NONE', #12541, #29449, #46772 ) ;
#30497=ORIENTED_EDGE ( 'NONE', *, *, #35735, .F. ) ;
#30499=DIRECTION ( 'NONE',  ( -1.000000000000000000, -0.000000000000000000, -0.000000000000000000 ) ) ;
#30500=ORIENTED_EDGE ( 'NONE', *, *, #38217, .T. ) ;
#30504=ORIENTED_EDGE ( 'NONE', *, *, #64446, .T. ) ;
#30513=CYLINDRICAL_SURFACE ( 'NONE', #14955, 31.99999999999998579 ) ;
#30514=DIRECTION ( 'NONE',  ( 1.000000000000000000, 0.000000000000000000, 0.000000000000000000 ) ) ;
#30519=ORIENTED_EDGE ( 'NONE', *, *, #53815, .F. ) ;
#30527=DIRECTION ( 'NONE',  ( 0.000000000000000000, -0.3090169943749560555, -0.9510565162951506446 ) ) ;
#30536=ORIENTED_EDGE ( 'NONE', *, *, #10078, .T. ) ;
#30537=EDGE_CURVE ( 'NONE', #48253, #44200, #55630, .T. ) ;
#30539=DIRECTION ( 'NONE',  ( 0.000000000000000000, 0.000000000000000000, 1.000000000000000000 ) ) ;
#30548=VERTEX_POINT ( 'NONE', #28909 ) ;
#30552=LINE ( 'NONE', #13633, #50153 ) ;
#30558=EDGE_CURVE ( 'NONE', #27167, #27292, #37105, .T. ) ;
#30559=DIRECTION ( 'NONE',  ( 0.000000000000000000, -0.7431448254773862505, 0.6691306063588672304 ) ) ;
#30563=AXIS2_PLACEMENT_3D ( 'NONE', #71473, #65125, #60231 ) ;
#30571=ADVANCED_FACE ( 'NONE', ( #16900 ), #69500, .T. ) ;
#30586=EDGE_LOOP ( 'NONE', ( #12219, #5229, #29511, #26440 ) ) ;
#30594=EDGE_LOOP ( 'NONE', ( #56641, #36129, #1471, #26055 ) ) ;
#30595=FACE_OUTER_BOUND ( 'NONE', #56795, .T. ) ;
#30596=ORIENTED_EDGE ( 'NONE', *, *, #14495, .T. ) ;
#30610=ORIENTED_EDGE ( 'NONE', *, *, #33971, .F. ) ;
#30613=CARTESIAN_POINT ( 'NONE',  ( 15.00000000000000000, -22.67460108101774452, 6.353146135318220367 ) ) ;
#30623=EDGE_CURVE ( 'NONE', #59348, #35612, #29629, .T. ) ;
#30638=FACE_OUTER_BOUND ( 'NONE', #50050, .T. ) ;
#30645=DIRECTION ( 'NONE',  ( -1.000000000000000000, 0.000000000000000000, -0.000000000000000000 ) ) ;
#30647=VECTOR ( 'NONE', #26176, 1000.000000000000114 ) ;
#30661=CARTESIAN_POINT ( 'NONE',  ( 11.99999999999999822, -8.966570791701281351, 81.50828551894223040 ) ) ;
#30664=VERTEX_POINT ( 'NONE', #41304 ) ;
#30666=DIRECTION ( 'NONE',  ( -1.000000000000000000, -0.000000000000000000, -0.000000000000000000 ) ) ;
#30668=ORIENTED_EDGE ( 'NONE', *, *, #45182, .T. ) ;
#30670=DIRECTION ( 'NONE',  ( 0.000000000000000000, -0.3090169943749549453, 0.9510565162951511997 ) ) ;
#30687=EDGE_CURVE ( 'NONE', #23480, #40077, #27532, .T. ) ;
#30700=CIRCLE ( 'NONE', #18681, 77.49899999999999523 ) ;
#30703=FACE_OUTER_BOUND ( 'NONE', #30023, .T. ) ;
#30714=DIRECTION ( 'NONE',  ( 0.000000000000000000, 0.000000000000000000, -1.000000000000000000 ) ) ;
#30715=AXIS2_PLACEMENT_3D ( 'NONE', #59975, #13709, #36646 ) ;
#30721=ORIENTED_EDGE ( 'NONE', *, *, #36150, .F. ) ;
#30723=DIRECTION ( 'NONE',  ( 0.000000000000000000, -0.4539904997395351471, -0.8910065241883738940 ) ) ;
#30726=CYLINDRICAL_SURFACE ( 'NONE', #19343, 82.00000000000000000 ) ;
#30728=CARTESIAN_POINT ( 'NONE',  ( 11.99999999999999822, 20.41045688087824317, 72.35160999960824313 ) ) ;
#30729=DIRECTION ( 'NONE',  ( 0.000000000000000000, 0.000000000000000000, 1.000000000000000000 ) ) ;
#30730=CARTESIAN_POINT ( 'NONE',  ( 6.000000000000000000, 16.65972982744933972, 80.28980883073764119 ) ) ;
#30736=EDGE_CURVE ( 'NONE', #10762, #31821, #53322, .T. ) ;
#30750=ORIENTED_EDGE ( 'NONE', *, *, #9099, .T. ) ;
#30759=FACE_OUTER_BOUND ( 'NONE', #13001, .T. ) ;
#30766=CARTESIAN_POINT ( 'NONE',  ( 11.99999999999999822, 0.000000000000000000, 0.000000000000000000 ) ) ;
#30775=ORIENTED_EDGE ( 'NONE', *, *, #22226, .F. ) ;
#30777=CARTESIAN_POINT ( 'NONE',  ( 11.99999999999999822, 0.000000000000000000, 0.000000000000000000 ) ) ;
#30779=ORIENTED_EDGE ( 'NONE', *, *, #3744, .T. ) ;
#30787=ORIENTED_EDGE ( 'NONE', *, *, #53153, .T. ) ;
#30789=ORIENTED_EDGE ( 'NONE', *, *, #2981, .F. ) ;
#30796=DIRECTION ( 'NONE',  ( -1.000000000000000000, -0.000000000000000000, -0.000000000000000000 ) ) ;
#30798=EDGE_LOOP ( 'NONE', ( #10242, #47379, #74070, #30851 ) ) ;
#30799=FACE_OUTER_BOUND ( 'NONE', #22292, .T. ) ;
#30811=DIRECTION ( 'NONE',  ( -1.000000000000000000, 0.000000000000000000, 0.000000000000000000 ) ) ;
#30815=CARTESIAN_POINT ( 'NONE',  ( 11.99999999999999822, -36.72794159290288718, 65.59268652807197952 ) ) ;
#30817=EDGE_CURVE ( 'NONE', #24340, #52404, #52773, .T. ) ;
#30820=CARTESIAN_POINT ( 'NONE',  ( 11.99999999999999822, -60.67117009219176538, 55.16347631943021668 ) ) ;
#30823=CIRCLE ( 'NONE', #878, 31.99999999999998579 ) ;
#30840=VERTEX_POINT ( 'NONE', #42412 ) ;
#30851=ORIENTED_EDGE ( 'NONE', *, *, #4780, .T. ) ;
#30853=ORIENTED_EDGE ( 'NONE', *, *, #39205, .F. ) ;
#30856=ORIENTED_EDGE ( 'NONE', *, *, #44414, .F. ) ;
#30857=AXIS2_PLACEMENT_3D ( 'NONE', #53389, #65780, #24445 ) ;
#30858=VERTEX_POINT ( 'NONE', #60817 ) ;
#30861=ADVANCED_FACE ( 'NONE', ( #32215 ), #72804, .T. ) ;
#30862=VERTEX_POINT ( 'NONE', #3692 ) ;
#30867=CARTESIAN_POINT ( 'NONE',  ( 11.99999999999999822, 36.73666225445988687, -65.58780272294035285 ) ) ;
#30871=ORIENTED_EDGE ( 'NONE', *, *, #71253, .F. ) ;
#30872=ADVANCED_FACE ( 'NONE', ( #66457 ), #72446, .T. ) ;
#30874=ORIENTED_EDGE ( 'NONE', *, *, #47603, .F. ) ;
#30879=VECTOR ( 'NONE', #50279, 1000.000000000000000 ) ;
#30883=DIRECTION ( 'NONE',  ( 0.000000000000000000, 0.000000000000000000, 1.000000000000000000 ) ) ;
#30893=DIRECTION ( 'NONE',  ( -1.000000000000000000, 0.000000000000000000, -0.000000000000000000 ) ) ;
#30894=DIRECTION ( 'NONE',  ( -1.000000000000000000, -0.000000000000000000, -0.000000000000000000 ) ) ;
#30895=ADVANCED_FACE ( 'NONE', ( #49885 ), #49521, .F. ) ;
#30897=DIRECTION ( 'NONE',  ( 0.000000000000000000, 0.000000000000000000, -1.000000000000000000 ) ) ;
#30901=EDGE_CURVE ( 'NONE', #45600, #15888, #61187, .T. ) ;
#30913=CIRCLE ( 'NONE', #18894, 82.00000000000000000 ) ;
#30918=EDGE_CURVE ( 'NONE', #57888, #69736, #55544, .T. ) ;
#30922=DIRECTION ( 'NONE',  ( 0.000000000000000000, 0.000000000000000000, -1.000000000000000000 ) ) ;
#30932=DIRECTION ( 'NONE',  ( -1.000000000000000000, -0.000000000000000000, 0.000000000000000000 ) ) ;
#30934=DIRECTION ( 'NONE',  ( -1.000000000000000000, -0.000000000000000000, -0.000000000000000000 ) ) ;
#30942=FACE_BOUND ( 'NONE', #50610, .T. ) ;
#30948=ADVANCED_FACE ( 'NONE', ( #44265 ), #4424, .T. ) ;
#30954=ORIENTED_EDGE ( 'NONE', *, *, #4249, .T. ) ;
#30957=ORIENTED_EDGE ( 'NONE', *, *, #64511, .F. ) ;
#30965=ORIENTED_EDGE ( 'NONE', *, *, #68534, .T. ) ;
#30966=ORIENTED_EDGE ( 'NONE', *, *, #58068, .F. ) ;
#30983=VERTEX_POINT ( 'NONE', #20078 ) ;
#30996=ORIENTED_EDGE ( 'NONE', *, *, #839, .T. ) ;
#30999=CARTESIAN_POINT ( 'NONE',  ( 11.99999999999999822, 24.73286445877808148, -73.44644590900034586 ) ) ;
#31004=CYLINDRICAL_SURFACE ( 'NONE', #57715, 31.99999999999998579 ) ;
#31006=AXIS2_PLACEMENT_3D ( 'NONE', #42509, #56005, #39469 ) ;
#31011=CARTESIAN_POINT ( 'NONE',  ( 11.99999999999999822, 76.66974797899837313, 11.30684508768366747 ) ) ;
#31013=CYLINDRICAL_SURFACE ( 'NONE', #64904, 77.49899999999999523 ) ;
#31017=FACE_OUTER_BOUND ( 'NONE', #17906, .T. ) ;
#31021=AXIS2_PLACEMENT_3D ( 'NONE', #57584, #74111, #46295 ) ;
#31024=ORIENTED_EDGE ( 'NONE', *, *, #69365, .T. ) ;
#31025=CYLINDRICAL_SURFACE ( 'NONE', #36496, 77.49899999999999523 ) ;
#31032=( NAMED_UNIT ( * ) PLANE_ANGLE_UNIT ( ) SI_UNIT ( $, .RADIAN. ) );
#31049=DIRECTION ( 'NONE',  ( 0.000000000000000000, 0.000000000000000000, -1.000000000000000000 ) ) ;
#31051=LINE ( 'NONE', #61125, #9369 ) ;
#31055=ORIENTED_EDGE ( 'NONE', *, *, #30110, .T. ) ;
#31064=CIRCLE ( 'NONE', #73084, 31.99999999999999645 ) ;
#31074=VECTOR ( 'NONE', #45481, 1000.000000000000000 ) ;
#31076=CARTESIAN_POINT ( 'NONE',  ( 12.00000000000000000, -4.261787119645322974, -26.19803753235774479 ) ) ;
#31078=ORIENTED_EDGE ( 'NONE', *, *, #61542, .F. ) ;
#31086=CIRCLE ( 'NONE', #14225, 82.00000000000000000 ) ;
#31088=CARTESIAN_POINT ( 'NONE',  ( 12.00000000000000000, -18.13022148937262656, -15.02647892043543898 ) ) ;
#31092=ORIENTED_EDGE ( 'NONE', *, *, #68374, .F. ) ;
#31104=DIRECTION ( 'NONE',  ( 0.000000000000000000, 0.3090169943749411785, 0.9510565162951556406 ) ) ;
#31105=CIRCLE ( 'NONE', #32276, 31.99999999999998579 ) ;
#31113=VERTEX_POINT ( 'NONE', #59965 ) ;
#31116=EDGE_CURVE ( 'NONE', #42164, #4487, #38382, .T. ) ;
#31129=EDGE_CURVE ( 'NONE', #60548, #62864, #8386, .T. ) ;
#31135=CARTESIAN_POINT ( 'NONE',  ( 11.99999999999999822, -70.52718814184277107, 26.02418014898285037 ) ) ;
#31137=EDGE_CURVE ( 'NONE', #64009, #48915, #72014, .T. ) ;
#31138=ORIENTED_EDGE ( 'NONE', *, *, #10877, .F. ) ;
#31141=AXIS2_PLACEMENT_3D ( 'NONE', #41721, #30796, #53380 ) ;
#31143=DIRECTION ( 'NONE',  ( 1.000000000000000000, -0.000000000000000000, 0.000000000000000000 ) ) ;
#31150=ORIENTED_EDGE ( 'NONE', *, *, #51354, .F. ) ;
#31156=VERTEX_POINT ( 'NONE', #67807 ) ;
#31169=ORIENTED_EDGE ( 'NONE', *, *, #38347, .T. ) ;
#31170=ORIENTED_EDGE ( 'NONE', *, *, #18984, .F. ) ;
#31173=CARTESIAN_POINT ( 'NONE',  ( -10.00000000000000000, 0.000000000000000000, 0.000000000000000000 ) ) ;
#31192=AXIS2_PLACEMENT_3D ( 'NONE', #16069, #44274, #33729 ) ;
#31193=DIRECTION ( 'NONE',  ( 0.000000000000000000, 0.6494480483301849905, -0.7604059656000298206 ) ) ;
#31194=CARTESIAN_POINT ( 'NONE',  ( 11.99999999999999822, -21.60688246758642705, 79.10210256391358996 ) ) ;
#31195=DIRECTION ( 'NONE',  ( 0.000000000000000000, -0.2334453638559128297, 0.9723699203976748917 ) ) ;
#31210=DIRECTION ( 'NONE',  ( 0.000000000000000000, 0.9876883405951371042, 0.1564344650402346715 ) ) ;
#31218=VERTEX_POINT ( 'NONE', #61056 ) ;
#31220=DIRECTION ( 'NONE',  ( -1.000000000000000000, -0.000000000000000000, -0.000000000000000000 ) ) ;
#31222=DIRECTION ( 'NONE',  ( -1.000000000000000000, -0.000000000000000000, 0.000000000000000000 ) ) ;
#31223=EDGE_CURVE ( 'NONE', #64494, #51571, #52832, .T. ) ;
#31229=DIRECTION ( 'NONE',  ( -1.000000000000000000, 0.000000000000000000, 0.000000000000000000 ) ) ;
#31230=EDGE_CURVE ( 'NONE', #20377, #15161, #24014, .T. ) ;
#31231=VERTEX_POINT ( 'NONE', #38495 ) ;
#31239=ORIENTED_EDGE ( 'NONE', *, *, #5565, .F. ) ;
#31246=EDGE_CURVE ( 'NONE', #62092, #14951, #61435, .T. ) ;
#31247=ORIENTED_EDGE ( 'NONE', *, *, #72110, .T. ) ;
#31248=DIRECTION ( 'NONE',  ( -1.000000000000000000, -0.000000000000000000, 0.000000000000000000 ) ) ;
#31249=ORIENTED_EDGE ( 'NONE', *, *, #66628, .T. ) ;
#31253=ORIENTED_EDGE ( 'NONE', *, *, #13300, .T. ) ;
#31262=FACE_OUTER_BOUND ( 'NONE', #64185, .T. ) ;
#31263=DIRECTION ( 'NONE',  ( -1.000000000000000000, -0.000000000000000000, -0.000000000000000000 ) ) ;
#31265=CIRCLE ( 'NONE', #46898, 31.99999999999998934 ) ;
#31279=CARTESIAN_POINT ( 'NONE',  ( 11.99999999999999822, 58.39081064771822582, -50.95692526931267707 ) ) ;
#31289=DIRECTION ( 'NONE',  ( 1.000000000000000000, -0.000000000000000000, 0.000000000000000000 ) ) ;
#31293=VECTOR ( 'NONE', #73549, 1000.000000000000000 ) ;
#31302=CARTESIAN_POINT ( 'NONE',  ( 5.999999999999999112, -67.80270845531921964, 46.11716303203162681 ) ) ;
#31310=CARTESIAN_POINT ( 'NONE',  ( 11.99999999999999822, 59.46389618802034960, -49.70050353004825894 ) ) ;
#31312=AXIS2_PLACEMENT_3D ( 'NONE', #31364, #8815, #14450 ) ;
#31326=DIRECTION ( 'NONE',  ( 0.000000000000000000, 0.8090169943749486725, -0.5877852522924714718 ) ) ;
#31332=VERTEX_POINT ( 'NONE', #73751 ) ;
#31342=DIRECTION ( 'NONE',  ( -1.000000000000000000, 0.000000000000000000, 0.000000000000000000 ) ) ;
#31343=AXIS2_PLACEMENT_3D ( 'NONE', #42770, #35279, #30729 ) ;
#31347=CARTESIAN_POINT ( 'NONE',  ( 11.99999999999999822, -51.02545421589285723, -55.20638768913812555 ) ) ;
#31358=FACE_OUTER_BOUND ( 'NONE', #35056, .T. ) ;
#31364=CARTESIAN_POINT ( 'NONE',  ( 11.99999999999999822, 0.000000000000000000, 0.000000000000000000 ) ) ;
#31375=DIRECTION ( 'NONE',  ( -1.000000000000000000, 0.000000000000000000, -0.000000000000000000 ) ) ;
#31379=LINE ( 'NONE', #54329, #6735 ) ;
#31381=EDGE_CURVE ( 'NONE', #55085, #10768, #68125, .T. ) ;
#31382=DIRECTION ( 'NONE',  ( 0.000000000000000000, 0.2079116908177664758, 0.9781476007338042455 ) ) ;
#31396=EDGE_CURVE ( 'NONE', #18486, #28736, #29525, .T. ) ;
#31399=AXIS2_PLACEMENT_3D ( 'NONE', #47826, #19620, #48928 ) ;
#31402=AXIS2_PLACEMENT_3D ( 'NONE', #58959, #7448, #30362 ) ;
#31403=AXIS2_PLACEMENT_3D ( 'NONE', #69216, #46285, #24458 ) ;
#31415=ADVANCED_FACE ( 'NONE', ( #49705 ), #4623, .T. ) ;
#31423=CARTESIAN_POINT ( 'NONE',  ( 11.99999999999999822, -6.903761155837269570, -77.19088730480530103 ) ) ;
#31447=DIRECTION ( 'NONE',  ( -1.000000000000000000, -0.000000000000000000, 0.000000000000000000 ) ) ;
#31454=FACE_OUTER_BOUND ( 'NONE', #38542, .T. ) ;
#31457=AXIS2_PLACEMENT_3D ( 'NONE', #21777, #43977, #49230 ) ;
#31459=DIRECTION ( 'NONE',  ( 0.000000000000000000, 0.000000000000000000, 1.000000000000000000 ) ) ;
#31460=AXIS2_PLACEMENT_3D ( 'NONE', #12598, #58101, #63378 ) ;
#31473=EDGE_CURVE ( 'NONE', #23551, #65491, #5525, .T. ) ;
#31479=DIRECTION ( 'NONE',  ( 0.000000000000000000, -0.9969173337331287410, 0.07845909572783489605 ) ) ;
#31480=EDGE_CURVE ( 'NONE', #7284, #27292, #21099, .T. ) ;
#31482=EDGE_CURVE ( 'NONE', #49792, #15852, #15097, .T. ) ;
#31494=DIRECTION ( 'NONE',  ( -1.000000000000000000, 0.000000000000000000, 0.000000000000000000 ) ) ;
#31495=ADVANCED_FACE ( 'NONE', ( #64345 ), #63239, .T. ) ;
#31509=ORIENTED_EDGE ( 'NONE', *, *, #81, .F. ) ;
#31531=DIRECTION ( 'NONE',  ( -1.000000000000000000, -0.000000000000000000, -0.000000000000000000 ) ) ;
#31532=ORIENTED_EDGE ( 'NONE', *, *, #24472, .F. ) ;
#31535=ORIENTED_EDGE ( 'NONE', *, *, #70936, .F. ) ;
#31544=CARTESIAN_POINT ( 'NONE',  ( 11.99999999999999822, 62.20884554314085335, -46.21855187248562657 ) ) ;
#31546=ORIENTED_EDGE ( 'NONE', *, *, #36170, .F. ) ;
#31550=CARTESIAN_POINT ( 'NONE',  ( 0.000000000000000000, 60.67117009219215618, -55.16347631942977614 ) ) ;
#31561=DIRECTION ( 'NONE',  ( -1.000000000000000000, 0.000000000000000000, -0.000000000000000000 ) ) ;
#31564=DIRECTION ( 'NONE',  ( 0.000000000000000000, 0.8660254037844432595, 0.4999999999999919509 ) ) ;
#31571=CARTESIAN_POINT ( 'NONE',  ( 0.000000000000000000, -75.11764819372145041, 29.05362095685286050 ) ) ;
#31575=CARTESIAN_POINT ( 'NONE',  ( 11.99999999999999822, 20.40083707022882820, 72.35432306680490910 ) ) ;
#31588=CYLINDRICAL_SURFACE ( 'NONE', #13921, 77.49899999999999523 ) ;
#31594=VERTEX_POINT ( 'NONE', #7563 ) ;
#31601=AXIS2_PLACEMENT_3D ( 'NONE', #72465, #8205, #14588 ) ;
#31610=AXIS2_PLACEMENT_3D ( 'NONE', #72009, #55474, #55095 ) ;
#31613=VECTOR ( 'NONE', #46118, 1000.000000000000000 ) ;
#31614=ORIENTED_EDGE ( 'NONE', *, *, #35043, .T. ) ;
#31623=ORIENTED_EDGE ( 'NONE', *, *, #63134, .F. ) ;
#31632=EDGE_CURVE ( 'NONE', #44223, #61399, #41505, .T. ) ;
#31634=ORIENTED_EDGE ( 'NONE', *, *, #12280, .T. ) ;
#31637=LINE ( 'NONE', #54580, #8324 ) ;
#31644=DIRECTION ( 'NONE',  ( -0.000000000000000000, 0.9781476007338067991, 0.2079116908177533474 ) ) ;
#31646=PLANE ( 'NONE',  #5906 ) ;
#31660=PRODUCT_DEFINITION_FORMATION_WITH_SPECIFIED_SOURCE ( 'ANY', '', #3780, .NOT_KNOWN. ) ;
#31661=DIRECTION ( 'NONE',  ( -1.000000000000000000, 0.000000000000000000, -0.000000000000000000 ) ) ;
#31662=AXIS2_PLACEMENT_3D ( 'NONE', #46142, #35217, #40126 ) ;
#31663=DIRECTION ( 'NONE',  ( 0.000000000000000000, -0.7604059656000369261, 0.6494480483301766638 ) ) ;
#31681=CIRCLE ( 'NONE', #29309, 82.00000000000000000 ) ;
#31695=ORIENTED_EDGE ( 'NONE', *, *, #69035, .T. ) ;
#31697=ORIENTED_EDGE ( 'NONE', *, *, #30623, .F. ) ;
#31701=DIRECTION ( 'NONE',  ( -1.000000000000000000, 0.000000000000000000, 0.000000000000000000 ) ) ;
#31702=DIRECTION ( 'NONE',  ( 0.000000000000000000, 0.000000000000000000, 1.000000000000000000 ) ) ;
#31707=DIRECTION ( 'NONE',  ( 0.000000000000000000, 0.000000000000000000, 1.000000000000000000 ) ) ;
#31711=DIRECTION ( 'NONE',  ( -0.000000000000000000, -0.6691306063588570163, 0.7431448254773953543 ) ) ;
#31724=AXIS2_PLACEMENT_3D ( 'NONE', #7493, #30403, #1887 ) ;
#31725=ORIENTED_EDGE ( 'NONE', *, *, #46196, .T. ) ;
#31728=DIRECTION ( 'NONE',  ( -1.000000000000000000, -0.000000000000000000, -0.000000000000000000 ) ) ;
#31735=LINE ( 'NONE', #8071, #1377 ) ;
#31741=DIRECTION ( 'NONE',  ( -1.000000000000000000, 0.000000000000000000, 0.000000000000000000 ) ) ;
#31743=AXIS2_PLACEMENT_3D ( 'NONE', #31135, #55557, #20968 ) ;
#31754=DIRECTION ( 'NONE',  ( -1.000000000000000000, 0.000000000000000000, 0.000000000000000000 ) ) ;
#31764=VERTEX_POINT ( 'NONE', #28829 ) ;
#31771=DIRECTION ( 'NONE',  ( 0.000000000000000000, -0.8090169943749531134, 0.5877852522924653655 ) ) ;
#31773=AXIS2_PLACEMENT_3D ( 'NONE', #6012, #11994, #34188 ) ;
#31774=CARTESIAN_POINT ( 'NONE',  ( 11.99999999999999822, 0.000000000000000000, 0.000000000000000000 ) ) ;
#31781=AXIS2_PLACEMENT_3D ( 'NONE', #3552, #27176, #38103 ) ;
#31798=CARTESIAN_POINT ( 'NONE',  ( 11.99999999999999822, 46.21855187248719687, -62.20884554313968806 ) ) ;
#31801=DIRECTION ( 'NONE',  ( 0.000000000000000000, -0.6691306063588661202, -0.7431448254773871387 ) ) ;
#31816=DIRECTION ( 'NONE',  ( -1.000000000000000000, 0.000000000000000000, 0.000000000000000000 ) ) ;
#31821=VERTEX_POINT ( 'NONE', #73568 ) ;
#31837=AXIS2_PLACEMENT_3D ( 'NONE', #24385, #70222, #13465 ) ;
#31842=CARTESIAN_POINT ( 'NONE',  ( 11.99999999999999822, 71.91182617369230456, -28.89263327155667938 ) ) ;
#31843=CIRCLE ( 'NONE', #27009, 77.49900000000000944 ) ;
#31844=CARTESIAN_POINT ( 'NONE',  ( 15.00000000000000000, -14.54903810567644484, 22.19967320028775504 ) ) ;
#31848=EDGE_CURVE ( 'NONE', #73707, #55862, #44660, .T. ) ;
#31851=AXIS2_PLACEMENT_3D ( 'NONE', #9916, #32837, #5419 ) ;
#31852=EDGE_CURVE ( 'NONE', #31895, #26439, #8304, .T. ) ;
#31854=ORIENTED_EDGE ( 'NONE', *, *, #24459, .F. ) ;
#31856=DIRECTION ( 'NONE',  ( 0.000000000000000000, 0.9781476007338045786, -0.2079116908177641720 ) ) ;
#31858=CYLINDRICAL_SURFACE ( 'NONE', #22271, 77.49899999999999523 ) ;
#31866=AXIS2_PLACEMENT_3D ( 'NONE', #28763, #24250, #1359 ) ;
#31881=CIRCLE ( 'NONE', #42746, 31.99999999999998579 ) ;
#31883=DIRECTION ( 'NONE',  ( 0.000000000000000000, 0.000000000000000000, 1.000000000000000000 ) ) ;
#31884=EDGE_CURVE ( 'NONE', #1062, #64295, #36963, .T. ) ;
#31888=AXIS2_PLACEMENT_3D ( 'NONE', #61543, #73541, #4041 ) ;
#31895=VERTEX_POINT ( 'NONE', #59254 ) ;
#31897=CARTESIAN_POINT ( 'NONE',  ( 5.999999999999999112, 63.97538442413498672, -51.29473840253155004 ) ) ;
#31898=AXIS2_PLACEMENT_3D ( 'NONE', #73813, #11053, #68192 ) ;
#31899=ORIENTED_EDGE ( 'NONE', *, *, #37262, .F. ) ;
#31904=VERTEX_POINT ( 'NONE', #12640 ) ;
#31907=EDGE_LOOP ( 'NONE', ( #20616, #38012, #67391, #52096 ) ) ;
#31913=DIRECTION ( 'NONE',  ( 1.000000000000000000, 0.000000000000000000, 0.000000000000000000 ) ) ;
#31915=VERTEX_POINT ( 'NONE', #64165 ) ;
#31925=FACE_OUTER_BOUND ( 'NONE', #40209, .T. ) ;
#31935=LINE ( 'NONE', #3397, #53900 ) ;
#31944=CARTESIAN_POINT ( 'NONE',  ( 11.99999999999999822, -62.50884508063453637, 41.76106447765467777 ) ) ;
#31950=AXIS2_PLACEMENT_3D ( 'NONE', #73716, #4960, #5696 ) ;
#31953=CARTESIAN_POINT ( 'NONE',  ( 0.000000000000000000, 0.000000000000000000, 0.000000000000000000 ) ) ;
#31956=ORIENTED_EDGE ( 'NONE', *, *, #49725, .F. ) ;
#31958=CARTESIAN_POINT ( 'NONE',  ( 15.00000000000000000, -11.95096189432345746, -23.69967320028757030 ) ) ;
#31979=CARTESIAN_POINT ( 'NONE',  ( 11.99999999999999822, 0.000000000000000000, 0.000000000000000000 ) ) ;
#31981=CARTESIAN_POINT ( 'NONE',  ( 11.99999999999999822, 80.28980883073758434, 16.65972982744962749 ) ) ;
#31987=ORIENTED_EDGE ( 'NONE', *, *, #37091, .T. ) ;
#31989=CARTESIAN_POINT ( 'NONE',  ( 11.99999999999999822, 0.000000000000000000, 0.000000000000000000 ) ) ;
#31991=DIRECTION ( 'NONE',  ( 0.000000000000000000, 0.000000000000000000, 1.000000000000000000 ) ) ;
#31994=CIRCLE ( 'NONE', #58410, 31.99999999999998579 ) ;
#31999=EDGE_CURVE ( 'NONE', #42708, #29316, #14139, .T. ) ;
#32001=EDGE_CURVE ( 'NONE', #5496, #46961, #40480, .T. ) ;
#32012=CARTESIAN_POINT ( 'NONE',  ( 5.999999999999999112, -27.74655509720726698, 77.16300072079651784 ) ) ;
#32013=CARTESIAN_POINT ( 'NONE',  ( 11.99999999999999822, -46.21855187248585395, -62.20884554314068993 ) ) ;
#32025=VERTEX_POINT ( 'NONE', #48709 ) ;
#32028=DIRECTION ( 'NONE',  ( -1.000000000000000000, -0.000000000000000000, -0.000000000000000000 ) ) ;
#32038=CIRCLE ( 'NONE', #39263, 31.99999999999999645 ) ;
#32044=EDGE_CURVE ( 'NONE', #61944, #36401, #61111, .T. ) ;
#32059=LINE ( 'NONE', #59922, #74211 ) ;
#32069=ORIENTED_EDGE ( 'NONE', *, *, #58489, .T. ) ;
#32078=ORIENTED_EDGE ( 'NONE', *, *, #36099, .T. ) ;
#32089=CARTESIAN_POINT ( 'NONE',  ( 0.000000000000000000, -65.59268652807237743, 36.72794159290217664 ) ) ;
#32095=ORIENTED_EDGE ( 'NONE', *, *, #38991, .T. ) ;
#32097=DIRECTION ( 'NONE',  ( 0.000000000000000000, 0.000000000000000000, 1.000000000000000000 ) ) ;
#32102=CARTESIAN_POINT ( 'NONE',  ( 11.99999999999999822, -72.35160999960831418, 20.41045688087797672 ) ) ;
#32106=VERTEX_POINT ( 'NONE', #20127 ) ;
#32107=AXIS2_PLACEMENT_3D ( 'NONE', #56936, #44914, #17440 ) ;
#32115=VERTEX_POINT ( 'NONE', #37063 ) ;
#32121=DIRECTION ( 'NONE',  ( 0.000000000000000000, 0.9723699203976756689, 0.2334453638559093602 ) ) ;
#32129=VERTEX_POINT ( 'NONE', #2532 ) ;
#32135=VERTEX_POINT ( 'NONE', #19759 ) ;
#32142=AXIS2_PLACEMENT_3D ( 'NONE', #7367, #30645, #2132 ) ;
#32143=EDGE_CURVE ( 'NONE', #65173, #68158, #15617, .T. ) ;
#32144=ADVANCED_FACE ( 'NONE', ( #61853 ), #73485, .T. ) ;
#32160=CIRCLE ( 'NONE', #54982, 82.00000000000000000 ) ;
#32190=VERTEX_POINT ( 'NONE', #39669 ) ;
#32193=DIRECTION ( 'NONE',  ( -1.000000000000000000, 0.000000000000000000, 0.000000000000000000 ) ) ;
#32202=CARTESIAN_POINT ( 'NONE',  ( 11.99999999999999822, 2.946379043146343246, 75.11764819372150725 ) ) ;
#32203=CIRCLE ( 'NONE', #49004, 31.99999999999998934 ) ;
#32215=FACE_OUTER_BOUND ( 'NONE', #46247, .T. ) ;
#32217=AXIS2_PLACEMENT_3D ( 'NONE', #31979, #56032, #44391 ) ;
#32218=EDGE_CURVE ( 'NONE', #26486, #35261, #27340, .T. ) ;
#32226=CARTESIAN_POINT ( 'NONE',  ( 11.99999999999999822, -78.73519480814938731, -22.90783923731713045 ) ) ;
#32233=EDGE_CURVE ( 'NONE', #72308, #18859, #40032, .T. ) ;
#32237=EDGE_CURVE ( 'NONE', #6493, #54754, #33641, .T. ) ;
#32241=CIRCLE ( 'NONE', #50236, 31.99999999999999289 ) ;
#32251=DIRECTION ( 'NONE',  ( 1.000000000000000000, -0.000000000000000000, 0.000000000000000000 ) ) ;
#32253=ORIENTED_EDGE ( 'NONE', *, *, #37086, .F. ) ;
#32258=CARTESIAN_POINT ( 'NONE',  ( 0.000000000000000000, 65.59268652807210742, 36.72794159290264560 ) ) ;
#32269=VERTEX_POINT ( 'NONE', #5095 ) ;
#32273=EDGE_LOOP ( 'NONE', ( #28198, #20142, #51582, #27926 ) ) ;
#32276=AXIS2_PLACEMENT_3D ( 'NONE', #7112, #18751, #25875 ) ;
#32278=ORIENTED_EDGE ( 'NONE', *, *, #41522, .T. ) ;
#32286=CARTESIAN_POINT ( 'NONE',  ( 11.99999999999999822, -30.41916302227062019, -71.27951684758059514 ) ) ;
#32287=DIRECTION ( 'NONE',  ( 0.000000000000000000, 1.000000000000000000, 3.469446951953616555E-15 ) ) ;
#32296=DIRECTION ( 'NONE',  ( 0.000000000000000000, 0.000000000000000000, -1.000000000000000000 ) ) ;
#32305=AXIS2_PLACEMENT_3D ( 'NONE', #5630, #56759, #5265 ) ;
#32307=VECTOR ( 'NONE', #43509, 1000.000000000000114 ) ;
#32308=FACE_OUTER_BOUND ( 'NONE', #42819, .T. ) ;
#32328=AXIS2_PLACEMENT_3D ( 'NONE', #25579, #42507, #54167 ) ;
#32329=DIRECTION ( 'NONE',  ( 0.000000000000000000, -0.8090169943749433434, 0.5877852522924787992 ) ) ;
#32340=ADVANCED_FACE ( 'NONE', ( #40776 ), #7302, .T. ) ;
#32347=DIRECTION ( 'NONE',  ( -1.000000000000000000, -0.000000000000000000, -0.000000000000000000 ) ) ;
#32348=CYLINDRICAL_SURFACE ( 'NONE', #926, 31.99999999999998579 ) ;
#32349=ORIENTED_EDGE ( 'NONE', *, *, #48147, .F. ) ;
#32350=CARTESIAN_POINT ( 'NONE',  ( 0.000000000000000000, -14.66109333815513160, 73.73191006444567108 ) ) ;
#32354=CIRCLE ( 'NONE', #47989, 82.00000000000000000 ) ;
#32357=CIRCLE ( 'NONE', #68407, 77.49899999999999523 ) ;
#32366=ORIENTED_EDGE ( 'NONE', *, *, #7336, .T. ) ;
#32370=EDGE_LOOP ( 'NONE', ( #55421, #20775, #31509, #50923 ) ) ;
#32372=ORIENTED_EDGE ( 'NONE', *, *, #64797, .F. ) ;
#32373=CARTESIAN_POINT ( 'NONE',  ( -10.00000000000000000, 0.000000000000000000, 0.000000000000000000 ) ) ;
#32384=AXIS2_PLACEMENT_3D ( 'NONE', #64468, #12942, #17853 ) ;
#32387=DIRECTION ( 'NONE',  ( -1.000000000000000000, 0.000000000000000000, -0.000000000000000000 ) ) ;
#32388=AXIS2_PLACEMENT_3D ( 'NONE', #14788, #71556, #26066 ) ;
#32394=DIRECTION ( 'NONE',  ( 0.000000000000000000, -0.1564344650402170744, -0.9876883405951398798 ) ) ;
#32398=PLANE ( 'NONE',  #61001 ) ;
#32399=EDGE_CURVE ( 'NONE', #66021, #56438, #41876, .T. ) ;
#32405=ADVANCED_FACE ( 'NONE', ( #69705 ), #18929, .F. ) ;
#32413=CARTESIAN_POINT ( 'NONE',  ( 11.99999999999999822, -77.19088730480518734, -6.903761155838607166 ) ) ;
#32415=CARTESIAN_POINT ( 'NONE',  ( 15.00000000000000000, -22.67460108101782978, -6.353146135317906840 ) ) ;
#32422=DIRECTION ( 'NONE',  ( 0.000000000000000000, 0.000000000000000000, 1.000000000000000000 ) ) ;
#32424=CYLINDRICAL_SURFACE ( 'NONE', #62831, 82.00000000000000000 ) ;
#32427=DIRECTION ( 'NONE',  ( -1.000000000000000000, -0.000000000000000000, -0.000000000000000000 ) ) ;
#32432=AXIS2_PLACEMENT_3D ( 'NONE', #7326, #70829, #65584 ) ;
#32433=EDGE_CURVE ( 'NONE', #18122, #38079, #35491, .T. ) ;
#32434=EDGE_CURVE ( 'NONE', #53274, #2804, #32059, .T. ) ;
#32445=CARTESIAN_POINT ( 'NONE',  ( 11.99999999999999822, -39.47590169984896846, 71.87247863392398983 ) ) ;
#32448=VERTEX_POINT ( 'NONE', #71911 ) ;
#32462=UNCERTAINTY_MEASURE_WITH_UNIT (LENGTH_MEASURE( 1.000000000000000082E-05 ), #17078, 'distance_accuracy_value', 'NONE');
#32471=AXIS2_PLACEMENT_3D ( 'NONE', #63497, #62773, #34171 ) ;
#32472=DIRECTION ( 'NONE',  ( -1.000000000000000000, 0.000000000000000000, 0.000000000000000000 ) ) ;
#32475=VERTEX_POINT ( 'NONE', #65191 ) ;
#32484=DIRECTION ( 'NONE',  ( 1.000000000000000000, 0.000000000000000000, 0.000000000000000000 ) ) ;
#32486=DIRECTION ( 'NONE',  ( 0.000000000000000000, -0.4539904997395541875, 0.8910065241883641241 ) ) ;
#32487=ORIENTED_EDGE ( 'NONE', *, *, #8054, .F. ) ;
#32492=AXIS2_PLACEMENT_3D ( 'NONE', #50773, #62835, #11656 ) ;
#32494=AXIS2_PLACEMENT_3D ( 'NONE', #58277, #28961, #69557 ) ;
#32500=CARTESIAN_POINT ( 'NONE',  ( 11.99999999999999822, 0.000000000000000000, 0.000000000000000000 ) ) ;
#32502=DIRECTION ( 'NONE',  ( 1.000000000000000000, 0.000000000000000000, -0.000000000000000000 ) ) ;
#32503=EDGE_CURVE ( 'NONE', #69736, #68378, #17801, .T. ) ;
#32508=ORIENTED_EDGE ( 'NONE', *, *, #4684, .F. ) ;
#32525=VERTEX_POINT ( 'NONE', #14776 ) ;
#32528=CARTESIAN_POINT ( 'NONE',  ( 0.000000000000000000, 73.44644590900092851, -24.73286445877629092 ) ) ;
#32540=CIRCLE ( 'NONE', #42169, 77.49899999999999523 ) ;
#32550=ORIENTED_EDGE ( 'NONE', *, *, #68532, .T. ) ;
#32559=CYLINDRICAL_SURFACE ( 'NONE', #19827, 31.99999999999998579 ) ;
#32563=FACE_OUTER_BOUND ( 'NONE', #18026, .T. ) ;
#32565=ORIENTED_EDGE ( 'NONE', *, *, #4006, .F. ) ;
#32568=CARTESIAN_POINT ( 'NONE',  ( 11.99999999999999822, -69.42325613327415113, -34.44570377933671779 ) ) ;
#32570=DIRECTION ( 'NONE',  ( 0.000000000000000000, 0.000000000000000000, 1.000000000000000000 ) ) ;
#32572=ORIENTED_EDGE ( 'NONE', *, *, #71288, .F. ) ;
#32578=FACE_OUTER_BOUND ( 'NONE', #70728, .T. ) ;
#32579=VECTOR ( 'NONE', #18529, 1000.000000000000000 ) ;
#32580=CARTESIAN_POINT ( 'NONE',  ( 11.99999999999999822, 59.75363087400075557, 56.15606465354979093 ) ) ;
#32581=AXIS2_PLACEMENT_3D ( 'NONE', #29071, #58019, #28702 ) ;
#32585=DIRECTION ( 'NONE',  ( -0.000000000000000000, 0.9781476007338064660, 0.2079116908177554846 ) ) ;
#32590=AXIS2_PLACEMENT_3D ( 'NONE', #33677, #50215, #55504 ) ;
#32604=ORIENTED_EDGE ( 'NONE', *, *, #8088, .T. ) ;
#32607=DIRECTION ( 'NONE',  ( -1.000000000000000000, -0.000000000000000000, -0.000000000000000000 ) ) ;
#32608=FACE_OUTER_BOUND ( 'NONE', #43757, .T. ) ;
#32612=ORIENTED_EDGE ( 'NONE', *, *, #14868, .F. ) ;
#32614=DIRECTION ( 'NONE',  ( -1.000000000000000000, 0.000000000000000000, 0.000000000000000000 ) ) ;
#32634=ORIENTED_EDGE ( 'NONE', *, *, #51021, .F. ) ;
#32637=CYLINDRICAL_SURFACE ( 'NONE', #74052, 82.00000000000000000 ) ;
#32642=EDGE_CURVE ( 'NONE', #39400, #28422, #58643, .T. ) ;
#32652=EDGE_CURVE ( 'NONE', #13516, #6672, #26218, .T. ) ;
#32654=DIRECTION ( 'NONE',  ( -1.000000000000000000, 0.000000000000000000, 0.000000000000000000 ) ) ;
#32659=EDGE_LOOP ( 'NONE', ( #42823, #49464, #6878, #57801 ) ) ;
#32663=CARTESIAN_POINT ( 'NONE',  ( 6.000000000000000000, 81.90746397400387480, 3.894527615418180044 ) ) ;
#32666=CARTESIAN_POINT ( 'NONE',  ( 11.99999999999999822, 0.000000000000000000, 0.000000000000000000 ) ) ;
#32673=CARTESIAN_POINT ( 'NONE',  ( 11.99999999999999822, 39.78640506895604290, 66.50666863322015843 ) ) ;
#32683=EDGE_CURVE ( 'NONE', #23343, #58541, #50836, .T. ) ;
#32686=CYLINDRICAL_SURFACE ( 'NONE', #9543, 31.99999999999998579 ) ;
#32690=AXIS2_PLACEMENT_3D ( 'NONE', #20970, #56310, #22093 ) ;
#32693=ORIENTED_EDGE ( 'NONE', *, *, #25058, .T. ) ;
#32695=CARTESIAN_POINT ( 'NONE',  ( 15.00000000000000000, -18.13022148937242761, 15.02647892043569122 ) ) ;
#32703=DIRECTION ( 'NONE',  ( -1.000000000000000000, 0.000000000000000000, 0.000000000000000000 ) ) ;
#32704=ORIENTED_EDGE ( 'NONE', *, *, #57887, .T. ) ;
#32712=ORIENTED_EDGE ( 'NONE', *, *, #17370, .F. ) ;
#32713=DIRECTION ( 'NONE',  ( 0.000000000000000000, 0.6494480483301848794, -0.7604059656000299317 ) ) ;
#32717=ADVANCED_FACE ( 'NONE', ( #61395 ), #73013, .T. ) ;
#32723=CARTESIAN_POINT ( 'NONE',  ( 11.99999999999999822, 0.000000000000000000, 0.000000000000000000 ) ) ;
#32724=EDGE_LOOP ( 'NONE', ( #70521, #3453, #27430, #27361 ) ) ;
#32738=FACE_OUTER_BOUND ( 'NONE', #18936, .T. ) ;
#32743=DIRECTION ( 'NONE',  ( 0.000000000000000000, 0.000000000000000000, 1.000000000000000000 ) ) ;
#32746=DIRECTION ( 'NONE',  ( 0.000000000000000000, 0.000000000000000000, 1.000000000000000000 ) ) ;
#32766=CARTESIAN_POINT ( 'NONE',  ( -10.00000000000000000, 0.000000000000000000, 0.000000000000000000 ) ) ;
#32772=ORIENTED_EDGE ( 'NONE', *, *, #29982, .F. ) ;
#32774=DIRECTION ( 'NONE',  ( 0.000000000000000000, -0.9723699203976789995, 0.2334453638558957322 ) ) ;
#32791=ORIENTED_EDGE ( 'NONE', *, *, #56433, .F. ) ;
#32795=DIRECTION ( 'NONE',  ( 0.000000000000000000, -0.5224985647159561264, 0.8526401643540878483 ) ) ;
#32799=ORIENTED_EDGE ( 'NONE', *, *, #20978, .T. ) ;
#32801=ORIENTED_EDGE ( 'NONE', *, *, #65443, .F. ) ;
#32807=CARTESIAN_POINT ( 'NONE',  ( 15.00000000000000000, -3.948201729842032215, 23.21447184625297666 ) ) ;
#32808=ORIENTED_EDGE ( 'NONE', *, *, #45182, .F. ) ;
#32813=VERTEX_POINT ( 'NONE', #68887 ) ;
#32819=FACE_OUTER_BOUND ( 'NONE', #46974, .T. ) ;
#32837=DIRECTION ( 'NONE',  ( -1.000000000000000000, 0.000000000000000000, 0.000000000000000000 ) ) ;
#32839=DIRECTION ( 'NONE',  ( -1.000000000000000000, 0.000000000000000000, 0.000000000000000000 ) ) ;
#32849=CARTESIAN_POINT ( 'NONE',  ( 11.99999999999999822, 70.53064760720316428, -26.01480285779861035 ) ) ;
#32858=CIRCLE ( 'NONE', #498, 31.99999999999998934 ) ;
#32871=ORIENTED_EDGE ( 'NONE', *, *, #7562, .T. ) ;
#32876=ORIENTED_EDGE ( 'NONE', *, *, #31223, .T. ) ;
#32897=ORIENTED_EDGE ( 'NONE', *, *, #40999, .F. ) ;
#32900=ORIENTED_EDGE ( 'NONE', *, *, #38636, .T. ) ;
#32901=VECTOR ( 'NONE', #31754, 1000.000000000000000 ) ;
#32903=CARTESIAN_POINT ( 'NONE',  ( 11.99999999999999822, -46.53671651293991118, 59.03961581697383565 ) ) ;
#32905=CARTESIAN_POINT ( 'NONE',  ( 5.999999999999999112, 60.67117009219215618, -55.16347631942977614 ) ) ;
#32913=CARTESIAN_POINT ( 'NONE',  ( 11.99999999999999822, 0.000000000000000000, 0.000000000000000000 ) ) ;
#32920=DIRECTION ( 'NONE',  ( 1.000000000000000000, 0.000000000000000000, -0.000000000000000000 ) ) ;
#32922=CIRCLE ( 'NONE', #59345, 82.00000000000000000 ) ;
#32932=EDGE_CURVE ( 'NONE', #54637, #26934, #43092, .T. ) ;
#32934=DIRECTION ( 'NONE',  ( -1.000000000000000000, -0.000000000000000000, 0.000000000000000000 ) ) ;
#32942=EDGE_CURVE ( 'NONE', #32025, #12008, #36501, .T. ) ;
#32944=CIRCLE ( 'NONE', #42574, 77.49899999999999523 ) ;
#32945=DIRECTION ( 'NONE',  ( 1.000000000000000000, 0.000000000000000000, 0.000000000000000000 ) ) ;
#32950=DIRECTION ( 'NONE',  ( 0.000000000000000000, 0.000000000000000000, 1.000000000000000000 ) ) ;
#32965=FACE_OUTER_BOUND ( 'NONE', #7503, .T. ) ;
#32980=CARTESIAN_POINT ( 'NONE',  ( 11.99999999999999822, 74.65491531819105830, 8.830959090343693418 ) ) ;
#32985=DIRECTION ( 'NONE',  ( -1.000000000000000000, 0.000000000000000000, 0.000000000000000000 ) ) ;
#32991=ORIENTED_EDGE ( 'NONE', *, *, #47047, .F. ) ;
#32992=CARTESIAN_POINT ( 'NONE',  ( 0.000000000000000000, 26.01480285779933510, -70.53064760720289428 ) ) ;
#33001=ORIENTED_EDGE ( 'NONE', *, *, #56527, .F. ) ;
#33006=CARTESIAN_POINT ( 'NONE',  ( 15.00000000000000000, 16.83928648764922542, -16.46020748918050458 ) ) ;
#33011=AXIS2_PLACEMENT_3D ( 'NONE', #66946, #9068, #39131 ) ;
#33013=CARTESIAN_POINT ( 'NONE',  ( 5.999999999999999112, -56.15606465355000410, 59.75363087400056372 ) ) ;
#33014=CYLINDRICAL_SURFACE ( 'NONE', #60585, 77.49899999999999523 ) ;
#33021=CIRCLE ( 'NONE', #49813, 31.99999999999998579 ) ;
#33034=CARTESIAN_POINT ( 'NONE',  ( 11.99999999999999822, -50.23322058963393744, 64.81221759200325039 ) ) ;
#33035=CARTESIAN_POINT ( 'NONE',  ( 0.000000000000000000, -67.80270845531855173, -46.11716303203260736 ) ) ;
#33036=LINE ( 'NONE', #4496, #36623 ) ;
#33044=CARTESIAN_POINT ( 'NONE',  ( 11.99999999999999822, 51.29473840253317007, -63.97538442413369353 ) ) ;
#33049=LINE ( 'NONE', #43353, #63765 ) ;
#33053=ADVANCED_FACE ( 'NONE', ( #68049 ), #26696, .T. ) ;
#33059=CARTESIAN_POINT ( 'NONE',  ( 11.99999999999999822, -76.41127070299262414, -12.93880638057396304 ) ) ;
#33061=AXIS2_PLACEMENT_3D ( 'NONE', #51757, #67946, #45773 ) ;
#33063=ORIENTED_EDGE ( 'NONE', *, *, #63252, .T. ) ;
#33065=AXIS2_PLACEMENT_3D ( 'NONE', #12610, #17886, #6974 ) ;
#33079=EDGE_LOOP ( 'NONE', ( #59974, #9657, #48074, #18372 ) ) ;
#33085=DIRECTION ( 'NONE',  ( -1.000000000000000000, 0.000000000000000000, 0.000000000000000000 ) ) ;
#33087=CARTESIAN_POINT ( 'NONE',  ( 0.000000000000000000, -41.76106447765443619, -62.50884508063471401 ) ) ;
#33089=VERTEX_POINT ( 'NONE', #61303 ) ;
#33097=CARTESIAN_POINT ( 'NONE',  ( 0.000000000000000000, 0.000000000000000000, 0.000000000000000000 ) ) ;
#33103=CARTESIAN_POINT ( 'NONE',  ( 15.00000000000000000, 16.61724383029390140, 20.69703378468902955 ) ) ;
#33105=EDGE_CURVE ( 'NONE', #41779, #19829, #46674, .T. ) ;
#33106=EDGE_CURVE ( 'NONE', #3442, #12401, #39110, .T. ) ;
#33109=ORIENTED_EDGE ( 'NONE', *, *, #26124, .T. ) ;
#33133=AXIS2_PLACEMENT_3D ( 'NONE', #6881, #35810, #58766 ) ;
#33140=CARTESIAN_POINT ( 'NONE',  ( 11.99999999999999822, 0.000000000000000000, 0.000000000000000000 ) ) ;
#33151=CARTESIAN_POINT ( 'NONE',  ( 12.00000000000000000, 23.59884966291538433, 12.14883922797231186 ) ) ;
#33154=AXIS2_PLACEMENT_3D ( 'NONE', #4851, #49561, #4101 ) ;
#33159=CARTESIAN_POINT ( 'NONE',  ( 15.00000000000000000, 22.07842321921480888, -8.187992925817425771 ) ) ;
#33179=ORIENTED_EDGE ( 'NONE', *, *, #28336, .T. ) ;
#33193=LINE ( 'NONE', #3551, #24711 ) ;
#33206=PLANE ( 'NONE',  #7035 ) ;
#33214=ORIENTED_EDGE ( 'NONE', *, *, #59252, .F. ) ;
#33221=CARTESIAN_POINT ( 'NONE',  ( 12.00000000000000000, -14.54903810567676636, -22.19967320028756674 ) ) ;
#33239=ORIENTED_EDGE ( 'NONE', *, *, #7877, .F. ) ;
#33254=ORIENTED_EDGE ( 'NONE', *, *, #37794, .T. ) ;
#33255=DIRECTION ( 'NONE',  ( 0.000000000000000000, 0.000000000000000000, 1.000000000000000000 ) ) ;
#33256=ORIENTED_EDGE ( 'NONE', *, *, #24029, .F. ) ;
#33258=ORIENTED_EDGE ( 'NONE', *, *, #12900, .F. ) ;
#33261=CARTESIAN_POINT ( 'NONE',  ( 0.000000000000000000, -26.02418014898359289, 70.52718814184250107 ) ) ;
#33262=DIRECTION ( 'NONE',  ( -1.000000000000000000, 0.000000000000000000, -0.000000000000000000 ) ) ;
#33275=DIRECTION ( 'NONE',  ( 0.000000000000000000, -0.8090169943749402348, -0.5877852522924830181 ) ) ;
#33277=DIRECTION ( 'NONE',  ( 0.000000000000000000, 0.000000000000000000, 1.000000000000000000 ) ) ;
#33294=CARTESIAN_POINT ( 'NONE',  ( 11.99999999999999822, -71.87247863392441616, 39.47590169984818687 ) ) ;
#33295=DIRECTION ( 'NONE',  ( 0.000000000000000000, -0.7071067811865389130, -0.7071067811865561215 ) ) ;
#33296=ORIENTED_EDGE ( 'NONE', *, *, #19104, .F. ) ;
#33301=ORIENTED_EDGE ( 'NONE', *, *, #14574, .F. ) ;
#33309=EDGE_LOOP ( 'NONE', ( #42615, #49766, #5380, #22543 ) ) ;
#33311=CARTESIAN_POINT ( 'NONE',  ( 0.000000000000000000, -68.55367621811173251, 44.99326035066031437 ) ) ;
#33312=DIRECTION ( 'NONE',  ( -1.000000000000000000, 0.000000000000000000, 0.000000000000000000 ) ) ;
#33314=LINE ( 'NONE', #51360, #16070 ) ;
#33323=CIRCLE ( 'NONE', #62174, 31.99999999999999289 ) ;
#33324=FACE_OUTER_BOUND ( 'NONE', #44675, .T. ) ;
#33341=AXIS2_PLACEMENT_3D ( 'NONE', #69073, #53257, #13397 ) ;
#33344=VERTEX_POINT ( 'NONE', #2628 ) ;
#33346=EDGE_CURVE ( 'NONE', #4389, #34691, #1882, .T. ) ;
#33350=CYLINDRICAL_SURFACE ( 'NONE', #56764, 77.49899999999999523 ) ;
#33352=CARTESIAN_POINT ( 'NONE',  ( 15.00000000000000000, 23.49999999999999645, 1.499999999999995337 ) ) ;
#33356=EDGE_LOOP ( 'NONE', ( #68968, #48555, #38768, #54937 ) ) ;
#33361=EDGE_CURVE ( 'NONE', #366, #70501, #31105, .T. ) ;
#33363=FACE_OUTER_BOUND ( 'NONE', #60914, .T. ) ;
#33370=DIRECTION ( 'NONE',  ( -1.000000000000000000, 0.000000000000000000, -0.000000000000000000 ) ) ;
#33374=AXIS2_PLACEMENT_3D ( 'NONE', #10735, #45329, #67506 ) ;
#33376=ORIENTED_EDGE ( 'NONE', *, *, #51631, .T. ) ;
#33377=CYLINDRICAL_SURFACE ( 'NONE', #10548, 31.99999999999998579 ) ;
#33397=CARTESIAN_POINT ( 'NONE',  ( 15.00000000000000000, -11.95096189432345746, -23.69967320028757030 ) ) ;
#33398=CARTESIAN_POINT ( 'NONE',  ( 15.00000000000000000, -25.60904388321925040, -6.976881207771165272 ) ) ;
#33400=CARTESIAN_POINT ( 'NONE',  ( 11.99999999999999822, -73.95703589263990807, 23.16143007188399139 ) ) ;
#33407=DIRECTION ( 'NONE',  ( 1.000000000000000000, 0.000000000000000000, 0.000000000000000000 ) ) ;
#33413=CARTESIAN_POINT ( 'NONE',  ( 12.00000000000000000, 23.49999999999999645, 1.499999999999995337 ) ) ;
#33414=DIRECTION ( 'NONE',  ( 0.000000000000000000, 0.000000000000000000, 1.000000000000000000 ) ) ;
#33420=EDGE_CURVE ( 'NONE', #40627, #1606, #59731, .T. ) ;
#33421=DIRECTION ( 'NONE',  ( -1.000000000000000000, -0.000000000000000000, -0.000000000000000000 ) ) ;
#33428=CIRCLE ( 'NONE', #62282, 31.99999999999997868 ) ;
#33432=AXIS2_PLACEMENT_3D ( 'NONE', #1669, #52764, #34727 ) ;
#33440=EDGE_CURVE ( 'NONE', #9966, #30983, #24402, .T. ) ;
#33447=CIRCLE ( 'NONE', #65898, 31.99999999999998579 ) ;
#33450=ORIENTED_EDGE ( 'NONE', *, *, #20949, .T. ) ;
#33452=CIRCLE ( 'NONE', #49079, 82.00000000000000000 ) ;
#33457=DIRECTION ( 'NONE',  ( -1.000000000000000000, 0.000000000000000000, 0.000000000000000000 ) ) ;
#33465=VERTEX_POINT ( 'NONE', #36412 ) ;
#33472=VERTEX_POINT ( 'NONE', #48439 ) ;
#33473=CARTESIAN_POINT ( 'NONE',  ( 0.000000000000000000, 73.95703589264006439, -23.16143007188350822 ) ) ;
#33478=VERTEX_POINT ( 'NONE', #15717 ) ;
#33480=ORIENTED_EDGE ( 'NONE', *, *, #30110, .F. ) ;
#33483=CIRCLE ( 'NONE', #65926, 31.99999999999999289 ) ;
#33490=CYLINDRICAL_SURFACE ( 'NONE', #31950, 31.99999999999997868 ) ;
#33501=CARTESIAN_POINT ( 'NONE',  ( 0.000000000000000000, 3.894527615419050903, -81.90746397400384637 ) ) ;
#33506=AXIS2_PLACEMENT_3D ( 'NONE', #56439, #83, #50777 ) ;
#33508=VECTOR ( 'NONE', #32329, 1000.000000000000114 ) ;
#33513=DIRECTION ( 'NONE',  ( 0.000000000000000000, 0.000000000000000000, 1.000000000000000000 ) ) ;
#33521=DIRECTION ( 'NONE',  ( 0.000000000000000000, -0.4539904997395350916, -0.8910065241883738940 ) ) ;
#33524=DIRECTION ( 'NONE',  ( -1.000000000000000000, 0.000000000000000000, 0.000000000000000000 ) ) ;
#33540=DIRECTION ( 'NONE',  ( 0.000000000000000000, -0.9510565162951565288, 0.3090169943749382919 ) ) ;
#33546=VERTEX_POINT ( 'NONE', #55935 ) ;
#33563=VECTOR ( 'NONE', #40802, 1000.000000000000000 ) ;
#33579=ORIENTED_EDGE ( 'NONE', *, *, #19170, .T. ) ;
#33584=DIRECTION ( 'NONE',  ( -1.000000000000000000, -0.000000000000000000, -0.000000000000000000 ) ) ;
#33586=EDGE_CURVE ( 'NONE', #2804, #28446, #57524, .T. ) ;
#33587=DIRECTION ( 'NONE',  ( 0.000000000000000000, 0.000000000000000000, 1.000000000000000000 ) ) ;
#33597=CARTESIAN_POINT ( 'NONE',  ( 12.00000000000000000, 20.85821328998741109, -10.92862929874522671 ) ) ;
#33610=CARTESIAN_POINT ( 'NONE',  ( 11.99999999999999822, 50.95692526931414790, -58.39081064771693974 ) ) ;
#33614=DIRECTION ( 'NONE',  ( 0.000000000000000000, 0.2079116908177555123, -0.9781476007338064660 ) ) ;
#33618=AXIS2_PLACEMENT_3D ( 'NONE', #40110, #16060, #28075 ) ;
#33624=CARTESIAN_POINT ( 'NONE',  ( 11.99999999999999822, 0.000000000000000000, 0.000000000000000000 ) ) ;
#33628=AXIS2_PLACEMENT_3D ( 'NONE', #12511, #41461, #12873 ) ;
#33633=ORIENTED_EDGE ( 'NONE', *, *, #32642, .F. ) ;
#33637=VERTEX_POINT ( 'NONE', #29476 ) ;
#33641=LINE ( 'NONE', #38918, #2227 ) ;
#33654=CIRCLE ( 'NONE', #63725, 31.99999999999998224 ) ;
#33655=VERTEX_POINT ( 'NONE', #7310 ) ;
#33656=ORIENTED_EDGE ( 'NONE', *, *, #5009, .T. ) ;
#33660=DIRECTION ( 'NONE',  ( -1.000000000000000000, 0.000000000000000000, -0.000000000000000000 ) ) ;
#33672=EDGE_LOOP ( 'NONE', ( #67761, #11713, #51694, #67863 ) ) ;
#33677=CARTESIAN_POINT ( 'NONE',  ( 11.99999999999999822, 0.000000000000000000, 0.000000000000000000 ) ) ;
#33679=CYLINDRICAL_SURFACE ( 'NONE', #18602, 31.99999999999998579 ) ;
#33680=CARTESIAN_POINT ( 'NONE',  ( 11.99999999999999822, 59.03961581697465277, -46.53671651293886669 ) ) ;
#33682=CARTESIAN_POINT ( 'NONE',  ( 11.99999999999999822, -33.71516098798793593, 74.74816331893418919 ) ) ;
#33683=DIRECTION ( 'NONE',  ( -1.000000000000000000, 0.000000000000000000, -0.000000000000000000 ) ) ;
#33687=ADVANCED_FACE ( 'NONE', ( #51038 ), #6573, .F. ) ;
#33702=DIRECTION ( 'NONE',  ( 0.000000000000000000, 0.000000000000000000, 1.000000000000000000 ) ) ;
#33710=EDGE_CURVE ( 'NONE', #17023, #55763, #19134, .T. ) ;
#33725=EDGE_CURVE ( 'NONE', #5745, #21153, #29847, .T. ) ;
#33727=CARTESIAN_POINT ( 'NONE',  ( 12.00000000000000000, -13.04903810567646971, 19.60159698893442126 ) ) ;
#33729=DIRECTION ( 'NONE',  ( 0.000000000000000000, 0.000000000000000000, 1.000000000000000000 ) ) ;
#33735=AXIS2_PLACEMENT_3D ( 'NONE', #41718, #22973, #51896 ) ;
#33742=DIRECTION ( 'NONE',  ( 1.000000000000000000, 0.000000000000000000, 0.000000000000000000 ) ) ;
#33743=DIRECTION ( 'NONE',  ( 0.000000000000000000, 0.6691306063588661202, 0.7431448254773871387 ) ) ;
#33765=DIRECTION ( 'NONE',  ( -1.000000000000000000, 0.000000000000000000, -0.000000000000000000 ) ) ;
#33766=CARTESIAN_POINT ( 'NONE',  ( 11.99999999999999822, -24.73286445877655382, -73.44644590900085745 ) ) ;
#33770=VERTEX_POINT ( 'NONE', #70433 ) ;
#33771=DIRECTION ( 'NONE',  ( -1.000000000000000000, -0.000000000000000000, -0.000000000000000000 ) ) ;
#33777=ORIENTED_EDGE ( 'NONE', *, *, #81, .T. ) ;
#33781=VECTOR ( 'NONE', #35250, 1000.000000000000227 ) ;
#33783=CARTESIAN_POINT ( 'NONE',  ( 11.99999999999999822, -28.89263327155796190, 71.91182617369179297 ) ) ;
#33784=ORIENTED_EDGE ( 'NONE', *, *, #48583, .T. ) ;
#33788=DIRECTION ( 'NONE',  ( 0.000000000000000000, 0.2334453638558989796, 0.9723699203976782224 ) ) ;
#33796=FACE_OUTER_BOUND ( 'NONE', #19222, .T. ) ;
#33806=DIRECTION ( 'NONE',  ( -1.000000000000000000, 0.000000000000000000, 0.000000000000000000 ) ) ;
#33807=CARTESIAN_POINT ( 'NONE',  ( 0.000000000000000000, -27.74655509720617985, -77.16300072079690153 ) ) ;
#33817=CARTESIAN_POINT ( 'NONE',  ( 11.99999999999999822, -23.16143007188376757, -73.95703589263997912 ) ) ;
#33827=CARTESIAN_POINT ( 'NONE',  ( 11.99999999999999822, 64.81221759200343513, 50.23322058963371006 ) ) ;
#33830=ORIENTED_EDGE ( 'NONE', *, *, #33420, .T. ) ;
#33835=CIRCLE ( 'NONE', #44648, 31.99999999999998224 ) ;
#33837=DIRECTION ( 'NONE',  ( 0.000000000000000000, 0.6691306063588569053, -0.7431448254773954654 ) ) ;
#33839=CARTESIAN_POINT ( 'NONE',  ( 15.00000000000000000, -23.29833615347104470, 3.418703333116808629 ) ) ;
#33840=CIRCLE ( 'NONE', #67443, 82.00000000000000000 ) ;
#33844=VERTEX_POINT ( 'NONE', #32445 ) ;
#33845=DIRECTION ( 'NONE',  ( -1.000000000000000000, 0.000000000000000000, 0.000000000000000000 ) ) ;
#33846=ORIENTED_EDGE ( 'NONE', *, *, #59736, .F. ) ;
#33851=VERTEX_POINT ( 'NONE', #26442 ) ;
#33858=ORIENTED_EDGE ( 'NONE', *, *, #14842, .T. ) ;
#33860=LINE ( 'NONE', #15834, #46699 ) ;
#33868=CARTESIAN_POINT ( 'NONE',  ( 11.99999999999999822, 0.000000000000000000, 0.000000000000000000 ) ) ;
#33870=EDGE_CURVE ( 'NONE', #3810, #13922, #13185, .T. ) ;
#33877=DIRECTION ( 'NONE',  ( 0.000000000000000000, 0.9510565162951504226, -0.3090169943749573322 ) ) ;
#33880=CYLINDRICAL_SURFACE ( 'NONE', #28845, 31.99999999999998579 ) ;
#33882=EDGE_CURVE ( 'NONE', #61698, #56516, #48993, .T. ) ;
#33884=CIRCLE ( 'NONE', #31460, 82.00000000000000000 ) ;
#33885=EDGE_CURVE ( 'NONE', #9195, #40982, #65941, .T. ) ;
#33892=DIRECTION ( 'NONE',  ( 0.000000000000000000, 0.000000000000000000, 1.000000000000000000 ) ) ;
#33895=VECTOR ( 'NONE', #35521, 1000.000000000000000 ) ;
#33896=EDGE_CURVE ( 'NONE', #37374, #57268, #40783, .T. ) ;
#33897=DIRECTION ( 'NONE',  ( 0.000000000000000000, -0.3826834323650969427, 0.9238795325112837409 ) ) ;
#33898=DIRECTION ( 'NONE',  ( -1.000000000000000000, -0.000000000000000000, -0.000000000000000000 ) ) ;
#33905=CARTESIAN_POINT ( 'NONE',  ( 15.00000000000000000, 20.85821328998756385, 10.92862929874494249 ) ) ;
#33908=CARTESIAN_POINT ( 'NONE',  ( 11.99999999999999822, -59.03342792756231461, -46.54456581323868392 ) ) ;
#33909=ORIENTED_EDGE ( 'NONE', *, *, #6534, .F. ) ;
#33912=ORIENTED_EDGE ( 'NONE', *, *, #38272, .F. ) ;
#33921=ORIENTED_EDGE ( 'NONE', *, *, #3324, .F. ) ;
#33924=ORIENTED_EDGE ( 'NONE', *, *, #17344, .F. ) ;
#33926=EDGE_CURVE ( 'NONE', #61974, #51872, #8366, .T. ) ;
#33927=EDGE_LOOP ( 'NONE', ( #50929, #4478, #43741, #18412 ) ) ;
#33928=DIRECTION ( 'NONE',  ( 0.000000000000000000, 0.000000000000000000, 1.000000000000000000 ) ) ;
#33933=ORIENTED_EDGE ( 'NONE', *, *, #37785, .F. ) ;
#33958=FACE_OUTER_BOUND ( 'NONE', #46625, .T. ) ;
#33961=CARTESIAN_POINT ( 'NONE',  ( 11.99999999999999822, 76.66974797899852945, -11.30684508768257679 ) ) ;
#33965=DIRECTION ( 'NONE',  ( 0.000000000000000000, -0.5000000000000039968, -0.8660254037844363761 ) ) ;
#33968=EDGE_LOOP ( 'NONE', ( #29603, #58014, #4404, #17564 ) ) ;
#33971=EDGE_CURVE ( 'NONE', #29677, #14426, #61406, .T. ) ;
#33972=DIRECTION ( 'NONE',  ( 0.000000000000000000, 0.000000000000000000, 1.000000000000000000 ) ) ;
#33976=DIRECTION ( 'NONE',  ( 0.000000000000000000, 0.3826834323650904479, -0.9238795325112865164 ) ) ;
#33980=ORIENTED_EDGE ( 'NONE', *, *, #41370, .T. ) ;
#33985=AXIS2_PLACEMENT_3D ( 'NONE', #71720, #49540, #13837 ) ;
#33987=DIRECTION ( 'NONE',  ( -1.000000000000000000, 0.000000000000000000, -0.000000000000000000 ) ) ;
#34004=FACE_OUTER_BOUND ( 'NONE', #22975, .T. ) ;
#34005=ORIENTED_EDGE ( 'NONE', *, *, #45680, .T. ) ;
#34010=ORIENTED_EDGE ( 'NONE', *, *, #28622, .T. ) ;
#34012=VERTEX_POINT ( 'NONE', #61777 ) ;
#34019=DIRECTION ( 'NONE',  ( 0.000000000000000000, 0.000000000000000000, 1.000000000000000000 ) ) ;
#34023=EDGE_CURVE ( 'NONE', #48419, #30862, #16269, .T. ) ;
#34028=ORIENTED_EDGE ( 'NONE', *, *, #6039, .F. ) ;
#34029=DIRECTION ( 'NONE',  ( -1.000000000000000000, 0.000000000000000000, 0.000000000000000000 ) ) ;
#34039=DIRECTION ( 'NONE',  ( 0.000000000000000000, 0.000000000000000000, 1.000000000000000000 ) ) ;
#34048=DIRECTION ( 'NONE',  ( 0.000000000000000000, -0.9510565162951499785, -0.3090169943749582204 ) ) ;
#34050=DIRECTION ( 'NONE',  ( -1.000000000000000000, 0.000000000000000000, 0.000000000000000000 ) ) ;
#34051=CARTESIAN_POINT ( 'NONE',  ( 11.99999999999999822, 0.000000000000000000, 0.000000000000000000 ) ) ;
#34073=CARTESIAN_POINT ( 'NONE',  ( 15.00000000000000000, 24.81905959214275370, 9.408202855044498492 ) ) ;
#34075=DIRECTION ( 'NONE',  ( -1.000000000000000000, 0.000000000000000000, 0.000000000000000000 ) ) ;
#34079=CYLINDRICAL_SURFACE ( 'NONE', #24963, 31.99999999999998579 ) ;
#34080=CIRCLE ( 'NONE', #62931, 31.99999999999998579 ) ;
#34083=CIRCLE ( 'NONE', #480, 77.49899999999998101 ) ;
#34092=EDGE_CURVE ( 'NONE', #57897, #9142, #43203, .T. ) ;
#34095=PLANE ( 'NONE',  #48646 ) ;
#34096=AXIS2_PLACEMENT_3D ( 'NONE', #1682, #46034, #29822 ) ;
#34097=PLANE ( 'NONE',  #27568 ) ;
#34098=LINE ( 'NONE', #45024, #10763 ) ;
#34106=ORIENTED_EDGE ( 'NONE', *, *, #15438, .T. ) ;
#34108=DIRECTION ( 'NONE',  ( -1.000000000000000000, -0.000000000000000000, -0.000000000000000000 ) ) ;
#34113=AXIS2_PLACEMENT_3D ( 'NONE', #64380, #30150, #41082 ) ;
#34122=CARTESIAN_POINT ( 'NONE',  ( 0.000000000000000000, -70.52718814184240159, -26.02418014898383802 ) ) ;
#34127=ORIENTED_EDGE ( 'NONE', *, *, #12900, .T. ) ;
#34137=CARTESIAN_POINT ( 'NONE',  ( 0.000000000000000000, 0.000000000000000000, 0.000000000000000000 ) ) ;
#34141=ORIENTED_EDGE ( 'NONE', *, *, #1674, .F. ) ;
#34142=DIRECTION ( 'NONE',  ( 0.000000000000000000, 0.5877852522924689183, -0.8090169943749504489 ) ) ;
#34146=ORIENTED_EDGE ( 'NONE', *, *, #68358, .F. ) ;
#34148=FACE_BOUND ( 'NONE', #62057, .T. ) ;
#34149=ORIENTED_EDGE ( 'NONE', *, *, #29627, .T. ) ;
#34151=DIRECTION ( 'NONE',  ( 0.000000000000000000, 0.000000000000000000, 1.000000000000000000 ) ) ;
#34156=ORIENTED_EDGE ( 'NONE', *, *, #12984, .F. ) ;
#34159=CARTESIAN_POINT ( 'NONE',  ( 11.99999999999999822, -46.21855187248673502, 62.20884554314003623 ) ) ;
#34162=EDGE_CURVE ( 'NONE', #60745, #60196, #18131, .T. ) ;
#34171=DIRECTION ( 'NONE',  ( 0.000000000000000000, -0.5877852522924624790, -0.8090169943749551118 ) ) ;
#34176=VECTOR ( 'NONE', #46, 1000.000000000000000 ) ;
#34181=DIRECTION ( 'NONE',  ( 0.000000000000000000, 0.8090169943749438985, -0.5877852522924780221 ) ) ;
#34186=DIRECTION ( 'NONE',  ( -1.000000000000000000, -0.000000000000000000, 0.000000000000000000 ) ) ;
#34187=DIRECTION ( 'NONE',  ( -1.000000000000000000, 0.000000000000000000, 0.000000000000000000 ) ) ;
#34188=DIRECTION ( 'NONE',  ( 0.000000000000000000, 0.9945218953682740670, 0.1045284632676459352 ) ) ;
#34192=ADVANCED_FACE ( 'NONE', ( #46332 ), #150, .T. ) ;
#34194=EDGE_CURVE ( 'NONE', #68106, #45130, #16845, .T. ) ;
#34196=EDGE_CURVE ( 'NONE', #69865, #23551, #30139, .T. ) ;
#34202=VERTEX_POINT ( 'NONE', #2725 ) ;
#34206=ORIENTED_EDGE ( 'NONE', *, *, #27240, .F. ) ;
#34208=ORIENTED_EDGE ( 'NONE', *, *, #25229, .T. ) ;
#34218=DIRECTION ( 'NONE',  ( -1.000000000000000000, -0.000000000000000000, 0.000000000000000000 ) ) ;
#34219=EDGE_LOOP ( 'NONE', ( #20125, #21720, #71820, #527 ) ) ;
#34221=ORIENTED_EDGE ( 'NONE', *, *, #13300, .F. ) ;
#34225=EDGE_CURVE ( 'NONE', #69166, #29201, #37243, .T. ) ;
#34230=ORIENTED_EDGE ( 'NONE', *, *, #879, .F. ) ;
#34234=ORIENTED_EDGE ( 'NONE', *, *, #17879, .T. ) ;
#34241=DIRECTION ( 'NONE',  ( 0.000000000000000000, 0.1564344650402311743, -0.9876883405951376593 ) ) ;
#34242=FACE_OUTER_BOUND ( 'NONE', #20046, .T. ) ;
#34254=AXIS2_PLACEMENT_3D ( 'NONE', #47980, #32427, #55742 ) ;
#34257=AXIS2_PLACEMENT_3D ( 'NONE', #61503, #33660, #56229 ) ;
#34258=CARTESIAN_POINT ( 'NONE',  ( 0.000000000000000000, 69.42325613327489009, -34.44570377933524696 ) ) ;
#34268=AXIS2_PLACEMENT_3D ( 'NONE', #25370, #9555, #65976 ) ;
#34270=LINE ( 'NONE', #62500, #63395 ) ;
#34272=EDGE_CURVE ( 'NONE', #70197, #24794, #66223, .T. ) ;
#34276=VERTEX_POINT ( 'NONE', #31981 ) ;
#34287=ORIENTED_EDGE ( 'NONE', *, *, #12635, .F. ) ;
#34294=ORIENTED_EDGE ( 'NONE', *, *, #38991, .F. ) ;
#34307=AXIS2_PLACEMENT_3D ( 'NONE', #32903, #56613, #62248 ) ;
#34318=DIRECTION ( 'NONE',  ( -1.000000000000000000, 0.000000000000000000, 0.000000000000000000 ) ) ;
#34329=CARTESIAN_POINT ( 'NONE',  ( 12.00000000000000000, 14.60985201121729737, 18.46759930825687590 ) ) ;
#34336=DIRECTION ( 'NONE',  ( 0.000000000000000000, 0.9969173337331276308, 0.07845909572784864894 ) ) ;
#34339=ORIENTED_EDGE ( 'NONE', *, *, #12373, .F. ) ;
#34345=DIRECTION ( 'NONE',  ( 0.000000000000000000, 0.9969173337331281859, -0.07845909572784168229 ) ) ;
#34346=CARTESIAN_POINT ( 'NONE',  ( 11.99999999999999822, -8.840884882374576037, -74.65374052328658649 ) ) ;
#34350=DIRECTION ( 'NONE',  ( -1.000000000000000000, 0.000000000000000000, -0.000000000000000000 ) ) ;
#34360=EDGE_CURVE ( 'NONE', #54220, #19667, #72570, .T. ) ;
#34362=CARTESIAN_POINT ( 'NONE',  ( 11.99999999999999822, 0.000000000000000000, 0.000000000000000000 ) ) ;
#34363=ORIENTED_EDGE ( 'NONE', *, *, #51705, .F. ) ;
#34367=VECTOR ( 'NONE', #70737, 1000.000000000000000 ) ;
#34368=EDGE_CURVE ( 'NONE', #58109, #44775, #50427, .T. ) ;
#34369=AXIS2_PLACEMENT_3D ( 'NONE', #67277, #4893, #10880 ) ;
#34378=VERTEX_POINT ( 'NONE', #39504 ) ;
#34385=ADVANCED_FACE ( 'NONE', ( #28205 ), #68447, .T. ) ;
#34395=CARTESIAN_POINT ( 'NONE',  ( 11.99999999999999822, -56.15606465354916566, -59.75363087400133111 ) ) ;
#34397=DIRECTION ( 'NONE',  ( -1.000000000000000000, -0.000000000000000000, 0.000000000000000000 ) ) ;
#34400=FACE_OUTER_BOUND ( 'NONE', #10798, .T. ) ;
#34402=DIRECTION ( 'NONE',  ( 0.000000000000000000, 0.000000000000000000, 1.000000000000000000 ) ) ;
#34406=DIRECTION ( 'NONE',  ( -1.000000000000000000, -0.000000000000000000, 0.000000000000000000 ) ) ;
#34407=ORIENTED_EDGE ( 'NONE', *, *, #46101, .T. ) ;
#34412=VECTOR ( 'NONE', #13155, 1000.000000000000000 ) ;
#34414=LINE ( 'NONE', #35893, #38620 ) ;
#34418=CARTESIAN_POINT ( 'NONE',  ( 0.000000000000000000, 15.33399622253483408, 80.55351364060595643 ) ) ;
#34424=AXIS2_PLACEMENT_3D ( 'NONE', #45098, #5257, #68402 ) ;
#34427=DIRECTION ( 'NONE',  ( 1.000000000000000000, 0.000000000000000000, 0.000000000000000000 ) ) ;
#34429=CARTESIAN_POINT ( 'NONE',  ( 5.999999999999999112, 67.80270845531956070, -46.11716303203111522 ) ) ;
#34439=DIRECTION ( 'NONE',  ( -1.000000000000000000, 0.000000000000000000, 0.000000000000000000 ) ) ;
#34461=EDGE_CURVE ( 'NONE', #24497, #19214, #55297, .T. ) ;
#34464=AXIS2_PLACEMENT_3D ( 'NONE', #10466, #72496, #72854 ) ;
#34469=AXIS2_PLACEMENT_3D ( 'NONE', #47176, #47911, #46433 ) ;
#34474=CYLINDRICAL_SURFACE ( 'NONE', #26730, 82.00000000000000000 ) ;
#34477=ADVANCED_FACE ( 'NONE', ( #4185 ), #72930, .T. ) ;
#34481=EDGE_LOOP ( 'NONE', ( #61559, #46176, #60495, #12637 ) ) ;
#34494=ORIENTED_EDGE ( 'NONE', *, *, #14750, .T. ) ;
#34495=CARTESIAN_POINT ( 'NONE',  ( 0.000000000000000000, -72.35160999960801576, -20.41045688087902121 ) ) ;
#34501=DIRECTION ( 'NONE',  ( -1.000000000000000000, 0.000000000000000000, 0.000000000000000000 ) ) ;
#34502=CARTESIAN_POINT ( 'NONE',  ( 0.000000000000000000, 0.000000000000000000, 0.000000000000000000 ) ) ;
#34510=FACE_BOUND ( 'NONE', #35773, .T. ) ;
#34512=CYLINDRICAL_SURFACE ( 'NONE', #47961, 82.00000000000000000 ) ;
#34524=CARTESIAN_POINT ( 'NONE',  ( 12.00000000000000000, 22.07842321921492612, 8.187992925817123790 ) ) ;
#34528=AXIS2_PLACEMENT_3D ( 'NONE', #60720, #14471, #9200 ) ;
#34531=EDGE_CURVE ( 'NONE', #62864, #69166, #39657, .T. ) ;
#34536=LINE ( 'NONE', #6356, #17888 ) ;
#34539=EDGE_CURVE ( 'NONE', #61251, #41269, #26498, .T. ) ;
#34544=VECTOR ( 'NONE', #39949, 1000.000000000000000 ) ;
#34547=ADVANCED_FACE ( 'NONE', ( #46612 ), #6759, .T. ) ;
#34550=EDGE_CURVE ( 'NONE', #15874, #3632, #68528, .T. ) ;
#34552=SURFACE_SIDE_STYLE ('',( #40571 ) ) ;
#34555=EDGE_CURVE ( 'NONE', #15732, #19667, #31265, .T. ) ;
#34561=ORIENTED_EDGE ( 'NONE', *, *, #72967, .T. ) ;
#34571=ORIENTED_EDGE ( 'NONE', *, *, #73671, .F. ) ;
#34573=CARTESIAN_POINT ( 'NONE',  ( 12.00000000000000000, 5.835314593368777558, 22.81335362449846471 ) ) ;
#34593=ORIENTED_EDGE ( 'NONE', *, *, #54636, .F. ) ;
#34599=VECTOR ( 'NONE', #29818, 1000.000000000000000 ) ;
#34606=VERTEX_POINT ( 'NONE', #51511 ) ;
#34626=CARTESIAN_POINT ( 'NONE',  ( 11.99999999999999822, 62.20884554314020676, 46.21855187248652896 ) ) ;
#34628=VECTOR ( 'NONE', #27881, 1000.000000000000000 ) ;
#34655=CIRCLE ( 'NONE', #57533, 77.49900000000000944 ) ;
#34658=ORIENTED_EDGE ( 'NONE', *, *, #56527, .T. ) ;
#34659=DIRECTION ( 'NONE',  ( 0.000000000000000000, 0.000000000000000000, 1.000000000000000000 ) ) ;
#34666=ORIENTED_EDGE ( 'NONE', *, *, #4147, .T. ) ;
#34673=AXIS2_PLACEMENT_3D ( 'NONE', #15951, #51653, #38892 ) ;
#34674=ORIENTED_EDGE ( 'NONE', *, *, #7083, .T. ) ;
#34681=DIRECTION ( 'NONE',  ( -1.000000000000000000, 0.000000000000000000, 0.000000000000000000 ) ) ;
#34687=CARTESIAN_POINT ( 'NONE',  ( 5.999999999999999112, 27.74655509720779989, -77.16300072079631889 ) ) ;
#34688=CARTESIAN_POINT ( 'NONE',  ( 0.000000000000000000, 71.87247863392471459, -39.47590169984771080 ) ) ;
#34691=VERTEX_POINT ( 'NONE', #57310 ) ;
#34699=CIRCLE ( 'NONE', #58753, 31.99999999999998579 ) ;
#34720=CYLINDRICAL_SURFACE ( 'NONE', #46931, 31.99999999999998579 ) ;
#34723=VERTEX_POINT ( 'NONE', #37350 ) ;
#34727=DIRECTION ( 'NONE',  ( 0.000000000000000000, 0.000000000000000000, 1.000000000000000000 ) ) ;
#34731=( NAMED_UNIT ( * ) SI_UNIT ( $, .STERADIAN. ) SOLID_ANGLE_UNIT ( ) );
#34732=EDGE_CURVE ( 'NONE', #51812, #38728, #14476, .T. ) ;
#34734=EDGE_CURVE ( 'NONE', #36787, #68327, #14398, .T. ) ;
#34746=CARTESIAN_POINT ( 'NONE',  ( 11.99999999999999822, 0.000000000000000000, 0.000000000000000000 ) ) ;
#34761=AXIS2_PLACEMENT_3D ( 'NONE', #36340, #47269, #13411 ) ;
#34765=ORIENTED_EDGE ( 'NONE', *, *, #11231, .T. ) ;
#34769=ORIENTED_EDGE ( 'NONE', *, *, #1935, .T. ) ;
#34773=ORIENTED_EDGE ( 'NONE', *, *, #67032, .F. ) ;
#34781=LINE ( 'NONE', #41529, #42675 ) ;
#34792=ORIENTED_EDGE ( 'NONE', *, *, #26540, .F. ) ;
#34795=CARTESIAN_POINT ( 'NONE',  ( 11.99999999999999822, 75.11725578898472122, -2.956366410619845730 ) ) ;
#34802=CARTESIAN_POINT ( 'NONE',  ( 0.000000000000000000, 34.94270380257639630, 74.18225833017899618 ) ) ;
#34805=ORIENTED_EDGE ( 'NONE', *, *, #20042, .F. ) ;
#34808=AXIS2_PLACEMENT_3D ( 'NONE', #16317, #4687, #29701 ) ;
#34809=EDGE_CURVE ( 'NONE', #65173, #9528, #13287, .T. ) ;
#34811=CARTESIAN_POINT ( 'NONE',  ( 11.99999999999999822, -51.29473840253269401, 63.97538442413408433 ) ) ;
#34817=CARTESIAN_POINT ( 'NONE',  ( 11.99999999999999822, 73.72996012237460661, -14.67089635893632504 ) ) ;
#34831=DIRECTION ( 'NONE',  ( -1.000000000000000000, -0.000000000000000000, 0.000000000000000000 ) ) ;
#34832=ADVANCED_FACE ( 'NONE', ( #65919 ), #8020, .T. ) ;
#34835=CARTESIAN_POINT ( 'NONE',  ( 0.000000000000000000, 76.66974797899852945, -11.30684508768257679 ) ) ;
#34844=AXIS2_PLACEMENT_3D ( 'NONE', #59694, #30364, #25104 ) ;
#34858=VECTOR ( 'NONE', #32387, 1000.000000000000000 ) ;
#34864=CARTESIAN_POINT ( 'NONE',  ( 0.000000000000000000, -71.27951684758005513, -30.41916302227188851 ) ) ;
#34870=AXIS2_PLACEMENT_3D ( 'NONE', #14763, #9123, #59910 ) ;
#34886=EDGE_CURVE ( 'NONE', #72362, #18854, #24098, .T. ) ;
#34890=ORIENTED_EDGE ( 'NONE', *, *, #11525, .F. ) ;
#34893=ORIENTED_EDGE ( 'NONE', *, *, #63875, .T. ) ;
#34897=CARTESIAN_POINT ( 'NONE',  ( 15.00000000000000000, 5.835314593368777558, 22.81335362449846471 ) ) ;
#34901=ORIENTED_EDGE ( 'NONE', *, *, #34225, .F. ) ;
#34902=CARTESIAN_POINT ( 'NONE',  ( 11.99999999999999822, 0.000000000000000000, 0.000000000000000000 ) ) ;
#34909=DIRECTION ( 'NONE',  ( -1.000000000000000000, 0.000000000000000000, 0.000000000000000000 ) ) ;
#34913=DIRECTION ( 'NONE',  ( 0.000000000000000000, -0.2334453638559126909, 0.9723699203976748917 ) ) ;
#34932=DIRECTION ( 'NONE',  ( -1.000000000000000000, -0.000000000000000000, 0.000000000000000000 ) ) ;
#34943=DIRECTION ( 'NONE',  ( 0.000000000000000000, 0.000000000000000000, 1.000000000000000000 ) ) ;
#34944=VERTEX_POINT ( 'NONE', #59518 ) ;
#34948=AXIS2_PLACEMENT_3D ( 'NONE', #13697, #49019, #14443 ) ;
#34961=EDGE_CURVE ( 'NONE', #61399, #21904, #33049, .T. ) ;
#34963=CARTESIAN_POINT ( 'NONE',  ( 11.99999999999999822, -62.50329211542465657, 41.76937507738766442 ) ) ;
#34970=ORIENTED_EDGE ( 'NONE', *, *, #26808, .T. ) ;
#34971=DIRECTION ( 'NONE',  ( -1.000000000000000000, 0.000000000000000000, 0.000000000000000000 ) ) ;
#34972=VECTOR ( 'NONE', #65881, 1000.000000000000000 ) ;
#34977=ORIENTED_EDGE ( 'NONE', *, *, #6625, .F. ) ;
#34978=CARTESIAN_POINT ( 'NONE',  ( 11.99999999999999822, 72.35432306680455383, 20.40083707023012494 ) ) ;
#34985=VERTEX_POINT ( 'NONE', #20011 ) ;
#34996=DIRECTION ( 'NONE',  ( -1.000000000000000000, 0.000000000000000000, 0.000000000000000000 ) ) ;
#34998=CARTESIAN_POINT ( 'NONE',  ( 12.00000000000000000, -18.13022148937242761, 15.02647892043569122 ) ) ;
#35002=DIRECTION ( 'NONE',  ( 0.000000000000000000, 1.000000000000000000, 3.491481338843133355E-15 ) ) ;
#35005=ORIENTED_EDGE ( 'NONE', *, *, #5448, .T. ) ;
#35025=DIRECTION ( 'NONE',  ( 1.000000000000000000, 0.000000000000000000, 0.000000000000000000 ) ) ;
#35035=DIRECTION ( 'NONE',  ( 1.000000000000000000, 0.000000000000000000, 0.000000000000000000 ) ) ;
#35040=EDGE_CURVE ( 'NONE', #21350, #19673, #36146, .T. ) ;
#35041=ORIENTED_EDGE ( 'NONE', *, *, #18076, .F. ) ;
#35043=EDGE_CURVE ( 'NONE', #8298, #29646, #13345, .T. ) ;
#35044=ORIENTED_EDGE ( 'NONE', *, *, #14190, .T. ) ;
#35045=DIRECTION ( 'NONE',  ( 1.000000000000000000, 0.000000000000000000, 0.000000000000000000 ) ) ;
#35056=EDGE_LOOP ( 'NONE', ( #28218, #55013, #50638, #42527 ) ) ;
#35076=DIRECTION ( 'NONE',  ( -1.000000000000000000, 0.000000000000000000, -0.000000000000000000 ) ) ;
#35084=EDGE_CURVE ( 'NONE', #34944, #37007, #74021, .T. ) ;
#35102=LINE ( 'NONE', #29811, #39470 ) ;
#35113=CARTESIAN_POINT ( 'NONE',  ( 12.00000000000000000, 8.688484142254226938, 21.88630264137359305 ) ) ;
#35121=CARTESIAN_POINT ( 'NONE',  ( 11.99999999999999822, 75.11725578898467859, 2.956366410620910656 ) ) ;
#35131=VERTEX_POINT ( 'NONE', #16514 ) ;
#35132=EDGE_CURVE ( 'NONE', #32115, #63620, #57487, .T. ) ;
#35134=EDGE_LOOP ( 'NONE', ( #41047, #63380, #10239, #69335 ) ) ;
#35138=VERTEX_POINT ( 'NONE', #33807 ) ;
#35141=CYLINDRICAL_SURFACE ( 'NONE', #14282, 31.99999999999998579 ) ;
#35144=CARTESIAN_POINT ( 'NONE',  ( 0.000000000000000000, 46.54456581323888997, -59.03342792756214408 ) ) ;
#35145=CARTESIAN_POINT ( 'NONE',  ( 11.99999999999999822, 6.903761155837791819, 77.19088730480525840 ) ) ;
#35146=EDGE_CURVE ( 'NONE', #30862, #21153, #51466, .T. ) ;
#35148=DIRECTION ( 'NONE',  ( 0.000000000000000000, 0.000000000000000000, 1.000000000000000000 ) ) ;
#35152=EDGE_LOOP ( 'NONE', ( #34658, #70919, #8022, #5674 ) ) ;
#35154=ORIENTED_EDGE ( 'NONE', *, *, #48525, .F. ) ;
#35162=FACE_OUTER_BOUND ( 'NONE', #8307, .T. ) ;
#35169=EDGE_CURVE ( 'NONE', #16367, #1257, #4946, .T. ) ;
#35172=VECTOR ( 'NONE', #71567, 1000.000000000000000 ) ;
#35184=DIRECTION ( 'NONE',  ( -0.000000000000000000, -2.312964634635746211E-15, 1.000000000000000000 ) ) ;
#35185=CARTESIAN_POINT ( 'NONE',  ( 0.000000000000000000, 73.73191006444551476, 14.66109333815590254 ) ) ;
#35187=DIRECTION ( 'NONE',  ( 0.000000000000000000, 0.000000000000000000, -1.000000000000000000 ) ) ;
#35196=ORIENTED_EDGE ( 'NONE', *, *, #16028, .F. ) ;
#35205=EDGE_CURVE ( 'NONE', #40611, #21247, #17627, .T. ) ;
#35214=CARTESIAN_POINT ( 'NONE',  ( 11.99999999999999822, 51.02545421589402252, -55.20638768913705263 ) ) ;
#35217=DIRECTION ( 'NONE',  ( -1.000000000000000000, 0.000000000000000000, -0.000000000000000000 ) ) ;
#35220=VECTOR ( 'NONE', #12805, 1000.000000000000000 ) ;
#35229=VECTOR ( 'NONE', #18443, 1000.000000000000227 ) ;
#35234=DIRECTION ( 'NONE',  ( 0.000000000000000000, 0.000000000000000000, 1.000000000000000000 ) ) ;
#35237=EDGE_CURVE ( 'NONE', #20511, #63342, #24377, .T. ) ;
#35238=EDGE_LOOP ( 'NONE', ( #12600, #10946, #3995, #68498 ) ) ;
#35241=ADVANCED_FACE ( 'NONE', ( #70216 ), #25847, .T. ) ;
#35244=DIRECTION ( 'NONE',  ( 0.000000000000000000, 0.000000000000000000, 1.000000000000000000 ) ) ;
#35249=CIRCLE ( 'NONE', #6492, 82.00000000000000000 ) ;
#35250=DIRECTION ( 'NONE',  ( -0.000000000000000000, 0.8090169943749503378, 0.5877852522924690293 ) ) ;
#35252=CARTESIAN_POINT ( 'NONE',  ( 11.99999999999999822, -11.30684508768284680, -76.66974797899850103 ) ) ;
#35253=ORIENTED_EDGE ( 'NONE', *, *, #69323, .T. ) ;
#35254=DIRECTION ( 'NONE',  ( 0.000000000000000000, 0.000000000000000000, 1.000000000000000000 ) ) ;
#35261=VERTEX_POINT ( 'NONE', #47671 ) ;
#35262=DIRECTION ( 'NONE',  ( -1.000000000000000000, 0.000000000000000000, 0.000000000000000000 ) ) ;
#35265=ORIENTED_EDGE ( 'NONE', *, *, #20806, .T. ) ;
#35272=DIRECTION ( 'NONE',  ( 0.000000000000000000, 0.000000000000000000, 1.000000000000000000 ) ) ;
#35276=DIRECTION ( 'NONE',  ( -1.000000000000000000, -0.000000000000000000, -0.000000000000000000 ) ) ;
#35278=CYLINDRICAL_SURFACE ( 'NONE', #25614, 31.99999999999998579 ) ;
#35279=DIRECTION ( 'NONE',  ( -1.000000000000000000, -0.000000000000000000, -0.000000000000000000 ) ) ;
#35295=DIRECTION ( 'NONE',  ( 1.000000000000000000, -0.000000000000000000, 0.000000000000000000 ) ) ;
#35298=CARTESIAN_POINT ( 'NONE',  ( 11.99999999999999822, 20.40083707022987625, -72.35432306680462489 ) ) ;
#35303=EDGE_CURVE ( 'NONE', #61251, #21350, #47316, .T. ) ;
#35309=ORIENTED_EDGE ( 'NONE', *, *, #65721, .F. ) ;
#35314=DIRECTION ( 'NONE',  ( -1.000000000000000000, -0.000000000000000000, 0.000000000000000000 ) ) ;
#35325=DIRECTION ( 'NONE',  ( 0.000000000000000000, -0.3090169943749549453, 0.9510565162951511997 ) ) ;
#35326=ORIENTED_EDGE ( 'NONE', *, *, #28923, .T. ) ;
#35334=AXIS2_PLACEMENT_3D ( 'NONE', #22103, #21723, #45799 ) ;
#35337=DIRECTION ( 'NONE',  ( -1.000000000000000000, -0.000000000000000000, 0.000000000000000000 ) ) ;
#35343=ORIENTED_EDGE ( 'NONE', *, *, #18162, .T. ) ;
#35344=CARTESIAN_POINT ( 'NONE',  ( 11.99999999999999822, -14.67089635893658794, -73.72996012237454977 ) ) ;
#35352=CARTESIAN_POINT ( 'NONE',  ( 11.99999999999999822, 5.256550761633951296, -77.32052557432835727 ) ) ;
#35354=ORIENTED_EDGE ( 'NONE', *, *, #48781, .T. ) ;
#35355=CARTESIAN_POINT ( 'NONE',  ( 0.000000000000000000, -55.38113227695745167, -54.21277698773732823 ) ) ;
#35357=DIRECTION ( 'NONE',  ( 1.000000000000000000, 0.000000000000000000, 0.000000000000000000 ) ) ;
#35361=ORIENTED_EDGE ( 'NONE', *, *, #1849, .F. ) ;
#35363=DIRECTION ( 'NONE',  ( -1.000000000000000000, -0.000000000000000000, -0.000000000000000000 ) ) ;
#35377=CARTESIAN_POINT ( 'NONE',  ( 0.000000000000000000, 0.000000000000000000, 0.000000000000000000 ) ) ;
#35378=LINE ( 'NONE', #7547, #74258 ) ;
#35380=DIRECTION ( 'NONE',  ( -1.000000000000000000, -0.000000000000000000, -0.000000000000000000 ) ) ;
#35389=AXIS2_PLACEMENT_3D ( 'NONE', #73786, #50492, #39597 ) ;
#35398=ORIENTED_EDGE ( 'NONE', *, *, #30537, .F. ) ;
#35402=ADVANCED_FACE ( 'NONE', ( #26587 ), #44261, .T. ) ;
#35403=ORIENTED_EDGE ( 'NONE', *, *, #4434, .F. ) ;
#35422=ORIENTED_EDGE ( 'NONE', *, *, #41917, .F. ) ;
#35426=DIRECTION ( 'NONE',  ( 0.000000000000000000, 0.000000000000000000, 1.000000000000000000 ) ) ;
#35441=VECTOR ( 'NONE', #36075, 1000.000000000000000 ) ;
#35443=DIRECTION ( 'NONE',  ( -1.000000000000000000, 0.000000000000000000, 0.000000000000000000 ) ) ;
#35449=ORIENTED_EDGE ( 'NONE', *, *, #27846, .F. ) ;
#35450=AXIS2_PLACEMENT_3D ( 'NONE', #48764, #25470, #36745 ) ;
#35466=CYLINDRICAL_SURFACE ( 'NONE', #13042, 31.99999999999998579 ) ;
#35467=PLANE ( 'NONE',  #21361 ) ;
#35471=EDGE_CURVE ( 'NONE', #20819, #29677, #43431, .T. ) ;
#35474=CARTESIAN_POINT ( 'NONE',  ( 0.000000000000000000, 0.000000000000000000, 0.000000000000000000 ) ) ;
#35475=ORIENTED_EDGE ( 'NONE', *, *, #17134, .T. ) ;
#35477=LINE ( 'NONE', #5817, #40114 ) ;
#35480=CIRCLE ( 'NONE', #31866, 31.99999999999998579 ) ;
#35486=VERTEX_POINT ( 'NONE', #4055 ) ;
#35491=LINE ( 'NONE', #58422, #1049 ) ;
#35493=AXIS2_PLACEMENT_3D ( 'NONE', #50577, #73877, #45330 ) ;
#35510=DIRECTION ( 'NONE',  ( -1.000000000000000000, 0.000000000000000000, 0.000000000000000000 ) ) ;
#35514=DIRECTION ( 'NONE',  ( -1.000000000000000000, -0.000000000000000000, -0.000000000000000000 ) ) ;
#35521=DIRECTION ( 'NONE',  ( -1.000000000000000000, -0.000000000000000000, -0.000000000000000000 ) ) ;
#35525=ORIENTED_EDGE ( 'NONE', *, *, #63417, .T. ) ;
#35529=CYLINDRICAL_SURFACE ( 'NONE', #30224, 82.00000000000000000 ) ;
#35534=ORIENTED_EDGE ( 'NONE', *, *, #31116, .F. ) ;
#35535=ORIENTED_EDGE ( 'NONE', *, *, #13725, .F. ) ;
#35541=ORIENTED_EDGE ( 'NONE', *, *, #29134, .F. ) ;
#35546=ADVANCED_FACE ( 'NONE', ( #46479 ), #16805, .T. ) ;
#35550=CARTESIAN_POINT ( 'NONE',  ( 15.00000000000000000, 5.835314593368777558, 22.81335362449846471 ) ) ;
#35554=DIRECTION ( 'NONE',  ( -1.000000000000000000, 0.000000000000000000, 0.000000000000000000 ) ) ;
#35563=CARTESIAN_POINT ( 'NONE',  ( 11.99999999999999822, -31.46837873495025306, 68.27212725128265447 ) ) ;
#35572=EDGE_CURVE ( 'NONE', #47715, #9195, #65041, .T. ) ;
#35573=EDGE_CURVE ( 'NONE', #72747, #25082, #51011, .T. ) ;
#35582=DIRECTION ( 'NONE',  ( 0.000000000000000000, 0.000000000000000000, 1.000000000000000000 ) ) ;
#35586=ORIENTED_EDGE ( 'NONE', *, *, #7336, .F. ) ;
#35595=AXIS2_PLACEMENT_3D ( 'NONE', #4511, #39456, #51463 ) ;
#35603=AXIS2_PLACEMENT_3D ( 'NONE', #28519, #40191, #17989 ) ;
#35604=VERTEX_POINT ( 'NONE', #34835 ) ;
#35612=VERTEX_POINT ( 'NONE', #23550 ) ;
#35615=EDGE_LOOP ( 'NONE', ( #29844, #14773, #53747, #34010 ) ) ;
#35623=ORIENTED_EDGE ( 'NONE', *, *, #57576, .T. ) ;
#35625=ORIENTED_EDGE ( 'NONE', *, *, #315, .T. ) ;
#35633=FACE_OUTER_BOUND ( 'NONE', #71656, .T. ) ;
#35638=EDGE_CURVE ( 'NONE', #18312, #63042, #27706, .T. ) ;
#35639=CIRCLE ( 'NONE', #22454, 31.99999999999997868 ) ;
#35648=EDGE_CURVE ( 'NONE', #31332, #65728, #57030, .T. ) ;
#35649=AXIS2_PLACEMENT_3D ( 'NONE', #59322, #66091, #54418 ) ;
#35655=LINE ( 'NONE', #41312, #68027 ) ;
#35662=VECTOR ( 'NONE', #30119, 1000.000000000000000 ) ;
#35663=ORIENTED_EDGE ( 'NONE', *, *, #4294, .T. ) ;
#35682=EDGE_LOOP ( 'NONE', ( #73373, #4920, #24589, #28492 ) ) ;
#35686=CIRCLE ( 'NONE', #11645, 31.99999999999998579 ) ;
#35694=VECTOR ( 'NONE', #39148, 1000.000000000000000 ) ;
#35696=VECTOR ( 'NONE', #18902, 1000.000000000000114 ) ;
#35697=CARTESIAN_POINT ( 'NONE',  ( 0.000000000000000000, 8.966570791701871102, -81.50828551894218776 ) ) ;
#35711=DIRECTION ( 'NONE',  ( 0.000000000000000000, 0.000000000000000000, 1.000000000000000000 ) ) ;
#35713=DIRECTION ( 'NONE',  ( 1.000000000000000000, 0.000000000000000000, 0.000000000000000000 ) ) ;
#35718=DIRECTION ( 'NONE',  ( 0.000000000000000000, 0.000000000000000000, 1.000000000000000000 ) ) ;
#35721=EDGE_CURVE ( 'NONE', #69158, #50412, #19395, .T. ) ;
#35723=DIRECTION ( 'NONE',  ( 0.000000000000000000, 0.000000000000000000, 1.000000000000000000 ) ) ;
#35735=EDGE_CURVE ( 'NONE', #68616, #45600, #38631, .T. ) ;
#35741=CIRCLE ( 'NONE', #4540, 77.49900000000000944 ) ;
#35743=VECTOR ( 'NONE', #51078, 1000.000000000000000 ) ;
#35748=DIRECTION ( 'NONE',  ( 0.000000000000000000, 0.000000000000000000, 1.000000000000000000 ) ) ;
#35756=ORIENTED_EDGE ( 'NONE', *, *, #31246, .T. ) ;
#35762=CYLINDRICAL_SURFACE ( 'NONE', #54485, 77.49899999999999523 ) ;
#35768=VERTEX_POINT ( 'NONE', #42691 ) ;
#35773=EDGE_LOOP ( 'NONE', ( #56402, #19262, #25962, #7350 ) ) ;
#35804=CARTESIAN_POINT ( 'NONE',  ( 11.99999999999999822, 10.30890764327382136, 81.34940948281339956 ) ) ;
#35810=DIRECTION ( 'NONE',  ( -1.000000000000000000, 0.000000000000000000, -0.000000000000000000 ) ) ;
#35811=CARTESIAN_POINT ( 'NONE',  ( 0.000000000000000000, -81.90746397400391743, 3.894527615417586741 ) ) ;
#35812=DIRECTION ( 'NONE',  ( 1.000000000000000000, -0.000000000000000000, 0.000000000000000000 ) ) ;
#35836=LINE ( 'NONE', #6545, #27825 ) ;
#35855=AXIS2_PLACEMENT_3D ( 'NONE', #14667, #31220, #25580 ) ;
#35858=ORIENTED_EDGE ( 'NONE', *, *, #68405, .T. ) ;
#35866=EDGE_LOOP ( 'NONE', ( #9428, #62324, #14756, #16633 ) ) ;
#35869=CARTESIAN_POINT ( 'NONE',  ( 0.000000000000000000, 55.19960302592141232, -51.03279382321027668 ) ) ;
#35871=AXIS2_PLACEMENT_3D ( 'NONE', #63917, #47351, #12385 ) ;
#35876=CARTESIAN_POINT ( 'NONE',  ( 0.000000000000000000, -39.78640506895651185, 66.50666863321987421 ) ) ;
#35884=ORIENTED_EDGE ( 'NONE', *, *, #58666, .T. ) ;
#35893=CARTESIAN_POINT ( 'NONE',  ( 5.999999999999999112, -63.97538442413463855, 51.29473840253199057 ) ) ;
#35900=ORIENTED_EDGE ( 'NONE', *, *, #67536, .T. ) ;
#35910=ORIENTED_EDGE ( 'NONE', *, *, #59072, .T. ) ;
#35912=CIRCLE ( 'NONE', #9508, 77.49899999999999523 ) ;
#35917=AXIS2_PLACEMENT_3D ( 'NONE', #52581, #6011, #70224 ) ;
#35918=CARTESIAN_POINT ( 'NONE',  ( 0.000000000000000000, -34.44570377933549565, -69.42325613327476219 ) ) ;
#35919=CARTESIAN_POINT ( 'NONE',  ( 0.000000000000000000, 29.01471420065673712, -76.69515212745984911 ) ) ;
#35921=CARTESIAN_POINT ( 'NONE',  ( 0.000000000000000000, 73.72996012237440766, 14.67089635893739619 ) ) ;
#35924=EDGE_CURVE ( 'NONE', #41826, #37007, #21771, .T. ) ;
#35930=AXIS2_PLACEMENT_3D ( 'NONE', #50322, #42839, #66515 ) ;
#35932=DIRECTION ( 'NONE',  ( 1.000000000000000000, 0.000000000000000000, 0.000000000000000000 ) ) ;
#35945=ORIENTED_EDGE ( 'NONE', *, *, #42872, .F. ) ;
#35947=LINE ( 'NONE', #65281, #70664 ) ;
#35951=CARTESIAN_POINT ( 'NONE',  ( 11.99999999999999822, 46.54456581323888997, -59.03342792756214408 ) ) ;
#35952=DIRECTION ( 'NONE',  ( -1.000000000000000000, 0.000000000000000000, 0.000000000000000000 ) ) ;
#35958=ORIENTED_EDGE ( 'NONE', *, *, #70662, .T. ) ;
#35960=VERTEX_POINT ( 'NONE', #43074 ) ;
#35965=FACE_OUTER_BOUND ( 'NONE', #72386, .T. ) ;
#35967=FACE_OUTER_BOUND ( 'NONE', #70621, .T. ) ;
#35969=ADVANCED_FACE ( 'NONE', ( #25763 ), #50159, .T. ) ;
#35979=CYLINDRICAL_SURFACE ( 'NONE', #21379, 77.49899999999999523 ) ;
#35981=AXIS2_PLACEMENT_3D ( 'NONE', #17512, #28045, #22803 ) ;
#35991=ORIENTED_EDGE ( 'NONE', *, *, #62393, .F. ) ;
#35992=FACE_OUTER_BOUND ( 'NONE', #33079, .T. ) ;
#36006=ADVANCED_FACE ( 'NONE', ( #10694 ), #11788, .T. ) ;
#36010=DIRECTION ( 'NONE',  ( -1.000000000000000000, 0.000000000000000000, -0.000000000000000000 ) ) ;
#36013=DIRECTION ( 'NONE',  ( -0.000000000000000000, 0.9945218953682744001, 0.1045284632676437842 ) ) ;
#36018=VECTOR ( 'NONE', #22304, 1000.000000000000000 ) ;
#36025=AXIS2_PLACEMENT_3D ( 'NONE', #54843, #31531, #66506 ) ;
#36036=ORIENTED_EDGE ( 'NONE', *, *, #33926, .T. ) ;
#36041=EDGE_LOOP ( 'NONE', ( #30965, #58437, #53729, #11499 ) ) ;
#36045=ORIENTED_EDGE ( 'NONE', *, *, #66628, .F. ) ;
#36047=ORIENTED_EDGE ( 'NONE', *, *, #33346, .F. ) ;
#36048=ADVANCED_FACE ( 'NONE', ( #63326 ), #50915, .T. ) ;
#36066=ORIENTED_EDGE ( 'NONE', *, *, #47358, .F. ) ;
#36075=DIRECTION ( 'NONE',  ( -1.000000000000000000, 0.000000000000000000, 0.000000000000000000 ) ) ;
#36081=FACE_OUTER_BOUND ( 'NONE', #17310, .T. ) ;
#36093=CARTESIAN_POINT ( 'NONE',  ( 0.000000000000000000, 50.23322058963348979, 64.81221759200361987 ) ) ;
#36094=FACE_OUTER_BOUND ( 'NONE', #26353, .T. ) ;
#36097=AXIS2_PLACEMENT_3D ( 'NONE', #10934, #804, #58276 ) ;
#36099=EDGE_CURVE ( 'NONE', #9267, #55524, #45298, .T. ) ;
#36100=AXIS2_PLACEMENT_3D ( 'NONE', #31173, #54125, #66149 ) ;
#36106=CARTESIAN_POINT ( 'NONE',  ( 0.000000000000000000, 55.16347631943131802, -60.67117009219074930 ) ) ;
#36114=CARTESIAN_POINT ( 'NONE',  ( 11.99999999999999822, -50.95692526931372157, 58.39081064771733054 ) ) ;
#36119=DIRECTION ( 'NONE',  ( -0.000000000000000000, -0.6691306063588570163, 0.7431448254773953543 ) ) ;
#36123=CIRCLE ( 'NONE', #27759, 31.99999999999998934 ) ;
#36129=ORIENTED_EDGE ( 'NONE', *, *, #52531, .F. ) ;
#36132=ORIENTED_EDGE ( 'NONE', *, *, #24464, .T. ) ;
#36142=ORIENTED_EDGE ( 'NONE', *, *, #50846, .F. ) ;
#36144=ORIENTED_EDGE ( 'NONE', *, *, #22838, .F. ) ;
#36146=CIRCLE ( 'NONE', #43367, 82.00000000000000000 ) ;
#36147=ORIENTED_EDGE ( 'NONE', *, *, #30901, .F. ) ;
#36148=FACE_OUTER_BOUND ( 'NONE', #41425, .T. ) ;
#36150=EDGE_CURVE ( 'NONE', #69052, #71472, #3868, .T. ) ;
#36157=EDGE_LOOP ( 'NONE', ( #6390, #58057, #13490, #17966 ) ) ;
#36162=PLANE ( 'NONE',  #72470 ) ;
#36163=DIRECTION ( 'NONE',  ( -1.000000000000000000, 0.000000000000000000, 0.000000000000000000 ) ) ;
#36170=EDGE_CURVE ( 'NONE', #19829, #63637, #41045, .T. ) ;
#36171=EDGE_LOOP ( 'NONE', ( #50367, #57975, #19447, #74063 ) ) ;
#36181=AXIS2_PLACEMENT_3D ( 'NONE', #52734, #47104, #17411 ) ;
#36183=DIRECTION ( 'NONE',  ( -1.000000000000000000, 0.000000000000000000, 0.000000000000000000 ) ) ;
#36184=VECTOR ( 'NONE', #46934, 1000.000000000000000 ) ;
#36188=EDGE_CURVE ( 'NONE', #25161, #30315, #35836, .T. ) ;
#36195=CARTESIAN_POINT ( 'NONE',  ( 5.999999999999999112, 60.67117009219134616, 55.16347631943062879 ) ) ;
#36200=CARTESIAN_POINT ( 'NONE',  ( 0.000000000000000000, -77.32052557432845674, 5.256550761632577284 ) ) ;
#36202=DIRECTION ( 'NONE',  ( -1.000000000000000000, 0.000000000000000000, 0.000000000000000000 ) ) ;
#36205=CARTESIAN_POINT ( 'NONE',  ( 11.99999999999999822, -73.44644590900043113, -24.73286445877782924 ) ) ;
#36209=CARTESIAN_POINT ( 'NONE',  ( -10.00000000000000000, 0.000000000000000000, 0.000000000000000000 ) ) ;
#36218=DIRECTION ( 'NONE',  ( -1.000000000000000000, 0.000000000000000000, 0.000000000000000000 ) ) ;
#36220=EDGE_LOOP ( 'NONE', ( #64832, #51868, #10262, #29232 ) ) ;
#36221=EDGE_CURVE ( 'NONE', #7371, #57888, #33840, .T. ) ;
#36222=DIRECTION ( 'NONE',  ( 0.000000000000000000, 0.3090169943749480064, -0.9510565162951534202 ) ) ;
#36227=EDGE_CURVE ( 'NONE', #41513, #44013, #13450, .T. ) ;
#36230=AXIS2_PLACEMENT_3D ( 'NONE', #54874, #2681, #24826 ) ;
#36232=EDGE_LOOP ( 'NONE', ( #23879, #8364, #23954, #65009 ) ) ;
#36246=DIRECTION ( 'NONE',  ( 0.000000000000000000, 0.000000000000000000, 1.000000000000000000 ) ) ;
#36247=CIRCLE ( 'NONE', #65085, 77.49900000000002365 ) ;
#36251=DIRECTION ( 'NONE',  ( -1.000000000000000000, 0.000000000000000000, 0.000000000000000000 ) ) ;
#36256=LINE ( 'NONE', #37387, #53982 ) ;
#36259=ADVANCED_FACE ( 'NONE', ( #12903 ), #59154, .T. ) ;
#36261=EDGE_CURVE ( 'NONE', #10620, #68386, #66276, .T. ) ;
#36272=FACE_OUTER_BOUND ( 'NONE', #43274, .T. ) ;
#36295=AXIS2_PLACEMENT_3D ( 'NONE', #39439, #41929, #62385 ) ;
#36307=EDGE_CURVE ( 'NONE', #51749, #7392, #44079, .T. ) ;
#36315=DIRECTION ( 'NONE',  ( 0.000000000000000000, 0.7071067811865437980, 0.7071067811865513475 ) ) ;
#36324=DIRECTION ( 'NONE',  ( -1.000000000000000000, -0.000000000000000000, -0.000000000000000000 ) ) ;
#36331=VERTEX_POINT ( 'NONE', #60641 ) ;
#36338=CARTESIAN_POINT ( 'NONE',  ( 11.99999999999999822, 74.74816331893477184, -33.71516098798660011 ) ) ;
#36339=ORIENTED_EDGE ( 'NONE', *, *, #28248, .T. ) ;
#36340=CARTESIAN_POINT ( 'NONE',  ( -10.00000000000000000, 0.000000000000000000, 0.000000000000000000 ) ) ;
#36344=FACE_OUTER_BOUND ( 'NONE', #27183, .T. ) ;
#36357=AXIS2_PLACEMENT_3D ( 'NONE', #6354, #46564, #28153 ) ;
#36361=CARTESIAN_POINT ( 'NONE',  ( 11.99999999999999822, 59.46389618802034960, -49.70050353004825894 ) ) ;
#36366=ORIENTED_EDGE ( 'NONE', *, *, #11228, .F. ) ;
#36378=DIRECTION ( 'NONE',  ( -1.000000000000000000, 0.000000000000000000, 0.000000000000000000 ) ) ;
#36382=DIRECTION ( 'NONE',  ( -1.000000000000000000, -0.000000000000000000, 0.000000000000000000 ) ) ;
#36387=VECTOR ( 'NONE', #70236, 1000.000000000000000 ) ;
#36389=CARTESIAN_POINT ( 'NONE',  ( 6.000000000000000000, 81.34940948281351325, -10.30890764327295450 ) ) ;
#36397=CARTESIAN_POINT ( 'NONE',  ( 11.99999999999999822, 74.18225833017937987, -34.94270380257559339 ) ) ;
#36398=VECTOR ( 'NONE', #47303, 1000.000000000000000 ) ;
#36399=AXIS2_PLACEMENT_3D ( 'NONE', #2129, #64885, #53589 ) ;
#36401=VERTEX_POINT ( 'NONE', #36955 ) ;
#36404=ORIENTED_EDGE ( 'NONE', *, *, #40467, .T. ) ;
#36407=DIRECTION ( 'NONE',  ( 0.000000000000000000, 0.000000000000000000, 1.000000000000000000 ) ) ;
#36408=EDGE_CURVE ( 'NONE', #34723, #17107, #28586, .T. ) ;
#36412=CARTESIAN_POINT ( 'NONE',  ( 0.000000000000000000, -29.01471420065506379, -76.69515212746047439 ) ) ;
#36428=CIRCLE ( 'NONE', #30411, 77.49899999999999523 ) ;
#36435=EDGE_CURVE ( 'NONE', #44373, #28756, #45580, .T. ) ;
#36439=ORIENTED_EDGE ( 'NONE', *, *, #47187, .F. ) ;
#36440=AXIS2_PLACEMENT_3D ( 'NONE', #27252, #66755, #5105 ) ;
#36446=ORIENTED_EDGE ( 'NONE', *, *, #45611, .T. ) ;
#36448=AXIS2_PLACEMENT_3D ( 'NONE', #43293, #15813, #3808 ) ;
#36450=ORIENTED_EDGE ( 'NONE', *, *, #4522, .T. ) ;
#36451=DIRECTION ( 'NONE',  ( -1.000000000000000000, -0.000000000000000000, -0.000000000000000000 ) ) ;
#36453=ORIENTED_EDGE ( 'NONE', *, *, #66376, .F. ) ;
#36454=CIRCLE ( 'NONE', #14830, 31.99999999999998579 ) ;
#36456=DIRECTION ( 'NONE',  ( 0.000000000000000000, 0.000000000000000000, 1.000000000000000000 ) ) ;
#36458=PLANE ( 'NONE',  #39853 ) ;
#36459=DIRECTION ( 'NONE',  ( 0.000000000000000000, 0.000000000000000000, 1.000000000000000000 ) ) ;
#36460=AXIS2_PLACEMENT_3D ( 'NONE', #42769, #54785, #65703 ) ;
#36461=VECTOR ( 'NONE', #28812, 1000.000000000000000 ) ;
#36462=DIRECTION ( 'NONE',  ( 0.000000000000000000, 0.000000000000000000, 1.000000000000000000 ) ) ;
#36463=DIRECTION ( 'NONE',  ( -1.000000000000000000, 0.000000000000000000, 0.000000000000000000 ) ) ;
#36464=CARTESIAN_POINT ( 'NONE',  ( 0.000000000000000000, -39.47590169984898267, 71.87247863392400404 ) ) ;
#36468=CARTESIAN_POINT ( 'NONE',  ( 12.00000000000000000, 9.615535125379096826, 24.73947219025905042 ) ) ;
#36469=LINE ( 'NONE', #52659, #55795 ) ;
#36475=EDGE_CURVE ( 'NONE', #5289, #60548, #34270, .T. ) ;
#36491=CARTESIAN_POINT ( 'NONE',  ( 11.99999999999999822, -14.66109333815513160, 73.73191006444567108 ) ) ;
#36493=AXIS2_PLACEMENT_3D ( 'NONE', #60122, #55570, #2988 ) ;
#36496=AXIS2_PLACEMENT_3D ( 'NONE', #9211, #43076, #43454 ) ;
#36497=VERTEX_POINT ( 'NONE', #27519 ) ;
#36500=AXIS2_PLACEMENT_3D ( 'NONE', #73831, #38894, #3959 ) ;
#36501=LINE ( 'NONE', #59451, #16687 ) ;
#36508=EDGE_LOOP ( 'NONE', ( #48216, #73253, #59273, #65565 ) ) ;
#36510=ORIENTED_EDGE ( 'NONE', *, *, #68708, .F. ) ;
#36516=AXIS2_PLACEMENT_3D ( 'NONE', #30257, #26467, #37764 ) ;
#36519=EDGE_LOOP ( 'NONE', ( #46637, #16760 ) ) ;
#36528=DIRECTION ( 'NONE',  ( -1.000000000000000000, 0.000000000000000000, -0.000000000000000000 ) ) ;
#36529=DIRECTION ( 'NONE',  ( 0.000000000000000000, 0.000000000000000000, -1.000000000000000000 ) ) ;
#36534=ORIENTED_EDGE ( 'NONE', *, *, #56268, .T. ) ;
#36535=VECTOR ( 'NONE', #22422, 1000.000000000000000 ) ;
#36540=CARTESIAN_POINT ( 'NONE',  ( 15.00000000000000000, -22.32062822937489344, -14.36278369418800160 ) ) ;
#36548=AXIS2_PLACEMENT_3D ( 'NONE', #52241, #53350, #64276 ) ;
#36552=CARTESIAN_POINT ( 'NONE',  ( 0.000000000000000000, 0.000000000000000000, 0.000000000000000000 ) ) ;
#36561=CIRCLE ( 'NONE', #57027, 82.00000000000000000 ) ;
#36566=DIRECTION ( 'NONE',  ( -1.000000000000000000, 0.000000000000000000, 0.000000000000000000 ) ) ;
#36576=CARTESIAN_POINT ( 'NONE',  ( 0.000000000000000000, -50.23322058963299241, -64.81221759200397514 ) ) ;
#36589=EDGE_CURVE ( 'NONE', #46178, #16205, #24839, .T. ) ;
#36590=DIRECTION ( 'NONE',  ( 0.000000000000000000, 0.8660254037844374864, -0.5000000000000019984 ) ) ;
#36605=ORIENTED_EDGE ( 'NONE', *, *, #68281, .F. ) ;
#36611=CARTESIAN_POINT ( 'NONE',  ( 0.000000000000000000, 76.69515212746016175, 29.01471420065590578 ) ) ;
#36623=VECTOR ( 'NONE', #68393, 1000.000000000000000 ) ;
#36637=DIRECTION ( 'NONE',  ( -1.000000000000000000, 0.000000000000000000, 0.000000000000000000 ) ) ;
#36642=CIRCLE ( 'NONE', #13820, 31.99999999999998224 ) ;
#36646=DIRECTION ( 'NONE',  ( 0.000000000000000000, 0.000000000000000000, 1.000000000000000000 ) ) ;
#36654=ORIENTED_EDGE ( 'NONE', *, *, #7083, .F. ) ;
#36661=CARTESIAN_POINT ( 'NONE',  ( 11.99999999999999822, -46.21855187248673502, 62.20884554314003623 ) ) ;
#36667=ADVANCED_FACE ( 'NONE', ( #65083 ), #13555, .F. ) ;
#36672=EDGE_LOOP ( 'NONE', ( #34805, #71340, #9322, #72942 ) ) ;
#36682=DIRECTION ( 'NONE',  ( 0.000000000000000000, 0.000000000000000000, 1.000000000000000000 ) ) ;
#36683=ORIENTED_EDGE ( 'NONE', *, *, #48397, .F. ) ;
#36685=CIRCLE ( 'NONE', #31851, 31.99999999999998224 ) ;
#36701=VERTEX_POINT ( 'NONE', #53054 ) ;
#36707=CYLINDRICAL_SURFACE ( 'NONE', #15023, 82.00000000000000000 ) ;
#36712=ORIENTED_EDGE ( 'NONE', *, *, #31129, .F. ) ;
#36721=CARTESIAN_POINT ( 'NONE',  ( 0.000000000000000000, 59.03342792756263435, 46.54456581323825048 ) ) ;
#36740=DIRECTION ( 'NONE',  ( 0.000000000000000000, 0.000000000000000000, 1.000000000000000000 ) ) ;
#36741=ORIENTED_EDGE ( 'NONE', *, *, #29927, .T. ) ;
#36745=DIRECTION ( 'NONE',  ( 0.000000000000000000, -0.9510565162951502005, -0.3090169943749581094 ) ) ;
#36769=CYLINDRICAL_SURFACE ( 'NONE', #50355, 31.99999999999998579 ) ;
#36771=AXIS2_PLACEMENT_3D ( 'NONE', #72666, #61041, #67421 ) ;
#36782=CYLINDRICAL_SURFACE ( 'NONE', #3336, 77.49899999999999523 ) ;
#36784=ORIENTED_EDGE ( 'NONE', *, *, #16442, .F. ) ;
#36787=VERTEX_POINT ( 'NONE', #65814 ) ;
#36788=CARTESIAN_POINT ( 'NONE',  ( 0.000000000000000000, 75.16055320797057959, -18.89407956138179046 ) ) ;
#36797=CARTESIAN_POINT ( 'NONE',  ( 11.99999999999999822, 76.66974797899852945, -11.30684508768257679 ) ) ;
#36802=ORIENTED_EDGE ( 'NONE', *, *, #7732, .T. ) ;
#36805=DIRECTION ( 'NONE',  ( 0.000000000000000000, 0.000000000000000000, 1.000000000000000000 ) ) ;
#36812=EDGE_CURVE ( 'NONE', #9094, #13137, #57484, .T. ) ;
#36816=ORIENTED_EDGE ( 'NONE', *, *, #72291, .F. ) ;
#36825=LINE ( 'NONE', #24812, #50062 ) ;
#36832=CARTESIAN_POINT ( 'NONE',  ( 0.000000000000000000, 75.11764819372149304, -2.946379043146603482 ) ) ;
#36835=SHAPE_REPRESENTATION ( 'slow gear_ISO - Spur gear 2M 80T 20PA 12FW ---S80A75H50L38.0N', ( #43395 ), #46970 ) ;
#36848=CARTESIAN_POINT ( 'NONE',  ( 11.99999999999999822, 59.03342792756263435, 46.54456581323825048 ) ) ;
#36873=VERTEX_POINT ( 'NONE', #68036 ) ;
#36885=CARTESIAN_POINT ( 'NONE',  ( 12.00000000000000000, -18.13022148937263012, -15.02647892043543898 ) ) ;
#36892=ORIENTED_EDGE ( 'NONE', *, *, #6703, .T. ) ;
#36893=ORIENTED_EDGE ( 'NONE', *, *, #64333, .F. ) ;
#36904=CARTESIAN_POINT ( 'NONE',  ( 15.00000000000000000, 14.60985201121729737, 18.46759930825687235 ) ) ;
#36905=DIRECTION ( 'NONE',  ( 0.000000000000000000, 0.000000000000000000, 1.000000000000000000 ) ) ;
#36911=ORIENTED_EDGE ( 'NONE', *, *, #72531, .F. ) ;
#36914=VERTEX_POINT ( 'NONE', #33059 ) ;
#36915=CARTESIAN_POINT ( 'NONE',  ( 15.00000000000000000, -22.67460108101782978, -6.353146135317906840 ) ) ;
#36932=CARTESIAN_POINT ( 'NONE',  ( 0.000000000000000000, 0.000000000000000000, 0.000000000000000000 ) ) ;
#36938=EDGE_CURVE ( 'NONE', #72049, #50325, #37059, .T. ) ;
#36939=AXIS2_PLACEMENT_3D ( 'NONE', #8173, #13447, #52557 ) ;
#36949=AXIS2_PLACEMENT_3D ( 'NONE', #33140, #27882, #68111 ) ;
#36951=CARTESIAN_POINT ( 'NONE',  ( 11.99999999999999822, 15.33399622253600647, -80.55351364060571484 ) ) ;
#36955=CARTESIAN_POINT ( 'NONE',  ( 11.99999999999999822, -81.90746397400391743, 3.894527615417590294 ) ) ;
#36960=VECTOR ( 'NONE', #2163, 1000.000000000000000 ) ;
#36963=CIRCLE ( 'NONE', #11896, 77.49900000000000944 ) ;
#36967=CARTESIAN_POINT ( 'NONE',  ( 11.99999999999999822, 6.903761155838878061, -77.19088730480517313 ) ) ;
#36971=DIRECTION ( 'NONE',  ( -1.000000000000000000, 0.000000000000000000, 0.000000000000000000 ) ) ;
#36975=VERTEX_POINT ( 'NONE', #57867 ) ;
#36979=ORIENTED_EDGE ( 'NONE', *, *, #1654, .F. ) ;
#36989=ORIENTED_EDGE ( 'NONE', *, *, #61288, .T. ) ;
#36990=CARTESIAN_POINT ( 'NONE',  ( 12.00000000000000000, -1.278221433540507768, -26.51162292216071492 ) ) ;
#36993=CARTESIAN_POINT ( 'NONE',  ( 12.00000000000000000, -13.04903810567675393, -19.60159698893424718 ) ) ;
#36994=VECTOR ( 'NONE', #8740, 1000.000000000000000 ) ;
#36997=CIRCLE ( 'NONE', #71802, 82.00000000000000000 ) ;
#37001=CARTESIAN_POINT ( 'NONE',  ( 0.000000000000000000, 5.256550761633951296, -77.32052557432835727 ) ) ;
#37002=EDGE_CURVE ( 'NONE', #45883, #45327, #25772, .T. ) ;
#37007=VERTEX_POINT ( 'NONE', #30661 ) ;
#37012=LINE ( 'NONE', #53563, #25461 ) ;
#37014=ORIENTED_EDGE ( 'NONE', *, *, #55358, .T. ) ;
#37021=AXIS2_PLACEMENT_3D ( 'NONE', #26789, #62520, #32795 ) ;
#37022=ADVANCED_FACE ( 'NONE', ( #40954 ), #53603, .T. ) ;
#37024=CYLINDRICAL_SURFACE ( 'NONE', #30715, 31.99999999999998579 ) ;
#37025=PLANE ( 'NONE',  #52556 ) ;
#37031=MANIFOLD_SOLID_BREP ( 'CirPattern1', #45204 ) ;
#37033=DIRECTION ( 'NONE',  ( 0.000000000000000000, 0.000000000000000000, -1.000000000000000000 ) ) ;
#37034=EDGE_CURVE ( 'NONE', #20333, #47275, #62315, .T. ) ;
#37036=CARTESIAN_POINT ( 'NONE',  ( 11.99999999999999822, -58.39081064771713869, -50.95692526931392052 ) ) ;
#37037=DIRECTION ( 'NONE',  ( 0.000000000000000000, 0.000000000000000000, 1.000000000000000000 ) ) ;
#37047=CIRCLE ( 'NONE', #2312, 77.49899999999999523 ) ;
#37052=DIRECTION ( 'NONE',  ( 0.000000000000000000, 0.000000000000000000, 1.000000000000000000 ) ) ;
#37058=ORIENTED_EDGE ( 'NONE', *, *, #22263, .T. ) ;
#37059=LINE ( 'NONE', #42700, #73007 ) ;
#37063=CARTESIAN_POINT ( 'NONE',  ( 15.00000000000000000, -25.60904388321916159, 6.976881207771517879 ) ) ;
#37065=ORIENTED_EDGE ( 'NONE', *, *, #12878, .F. ) ;
#37073=DIRECTION ( 'NONE',  ( -0.000000000000000000, 0.9781476007338042455, -0.2079116908177663092 ) ) ;
#37086=EDGE_CURVE ( 'NONE', #15073, #7371, #72723, .T. ) ;
#37087=DIRECTION ( 'NONE',  ( -1.000000000000000000, 0.000000000000000000, -0.000000000000000000 ) ) ;
#37091=EDGE_CURVE ( 'NONE', #57268, #41863, #19095, .T. ) ;
#37096=CARTESIAN_POINT ( 'NONE',  ( 12.00000000000000000, 5.835314593368470248, -22.81335362449854642 ) ) ;
#37100=VECTOR ( 'NONE', #63358, 1000.000000000000000 ) ;
#37101=ORIENTED_EDGE ( 'NONE', *, *, #63347, .T. ) ;
#37104=AXIS2_PLACEMENT_3D ( 'NONE', #21236, #44191, #61491 ) ;
#37105=CIRCLE ( 'NONE', #38271, 82.00000000000000000 ) ;
#37107=FACE_OUTER_BOUND ( 'NONE', #45533, .T. ) ;
#37109=ORIENTED_EDGE ( 'NONE', *, *, #34461, .F. ) ;
#37110=CARTESIAN_POINT ( 'NONE',  ( 12.00000000000000000, -0.9646360437375370855, -23.52805723605590060 ) ) ;
#37117=EDGE_CURVE ( 'NONE', #7584, #54778, #50550, .T. ) ;
#37119=CARTESIAN_POINT ( 'NONE',  ( 11.99999999999999822, 62.50329211542494789, -41.76937507738723099 ) ) ;
#37130=EDGE_CURVE ( 'NONE', #28860, #42708, #59901, .T. ) ;
#37136=DIRECTION ( 'NONE',  ( -1.000000000000000000, 0.000000000000000000, -0.000000000000000000 ) ) ;
#37137=DIRECTION ( 'NONE',  ( 0.000000000000000000, -0.8910065241883722287, 0.4539904997395383113 ) ) ;
#37149=DIRECTION ( 'NONE',  ( -1.000000000000000000, 0.000000000000000000, 0.000000000000000000 ) ) ;
#37152=VECTOR ( 'NONE', #17771, 1000.000000000000114 ) ;
#37158=VECTOR ( 'NONE', #53685, 1000.000000000000000 ) ;
#37175=ORIENTED_EDGE ( 'NONE', *, *, #7901, .F. ) ;
#37178=VECTOR ( 'NONE', #52427, 1000.000000000000000 ) ;
#37201=ORIENTED_EDGE ( 'NONE', *, *, #61454, .F. ) ;
#37209=FACE_OUTER_BOUND ( 'NONE', #16747, .T. ) ;
#37221=AXIS2_PLACEMENT_3D ( 'NONE', #7267, #12884, #17432 ) ;
#37243=CIRCLE ( 'NONE', #40846, 31.99999999999998579 ) ;
#37247=DIRECTION ( 'NONE',  ( -1.000000000000000000, -0.000000000000000000, 0.000000000000000000 ) ) ;
#37248=DIRECTION ( 'NONE',  ( -1.000000000000000000, 0.000000000000000000, 0.000000000000000000 ) ) ;
#37250=DIRECTION ( 'NONE',  ( 0.000000000000000000, 0.000000000000000000, 1.000000000000000000 ) ) ;
#37254=DIRECTION ( 'NONE',  ( -1.000000000000000000, 0.000000000000000000, -0.000000000000000000 ) ) ;
#37257=ORIENTED_EDGE ( 'NONE', *, *, #46212, .F. ) ;
#37262=EDGE_CURVE ( 'NONE', #48721, #66932, #34655, .T. ) ;
#37276=CARTESIAN_POINT ( 'NONE',  ( 0.000000000000000000, -44.88180994100329713, -63.18004540533077318 ) ) ;
#37278=CARTESIAN_POINT ( 'NONE',  ( 15.00000000000000000, -18.13022148937263012, -15.02647892043543898 ) ) ;
#37281=ADVANCED_FACE ( 'NONE', ( #34004 ), #62603, .T. ) ;
#37292=ORIENTED_EDGE ( 'NONE', *, *, #21049, .F. ) ;
#37298=DIRECTION ( 'NONE',  ( 0.000000000000000000, 0.9510565162951536422, 0.3090169943749471182 ) ) ;
#37313=LINE ( 'NONE', #31279, #43943 ) ;
#37323=LINE ( 'NONE', #61633, #58889 ) ;
#37325=CARTESIAN_POINT ( 'NONE',  ( 11.99999999999999822, -23.16143007188479430, 73.95703589263968070 ) ) ;
#37334=PLANE ( 'NONE',  #26878 ) ;
#37335=EDGE_CURVE ( 'NONE', #29463, #23135, #22717, .T. ) ;
#37344=CARTESIAN_POINT ( 'NONE',  ( 0.000000000000000000, 81.34940948281351325, -10.30890764327295450 ) ) ;
#37350=CARTESIAN_POINT ( 'NONE',  ( 11.99999999999999822, 69.42325613327489009, -34.44570377933524696 ) ) ;
#37361=ORIENTED_EDGE ( 'NONE', *, *, #63025, .T. ) ;
#37365=EDGE_LOOP ( 'NONE', ( #57007, #14128, #3826, #62525 ) ) ;
#37374=VERTEX_POINT ( 'NONE', #39287 ) ;
#37376=AXIS2_PLACEMENT_3D ( 'NONE', #61805, #27946, #62554 ) ;
#37377=VERTEX_POINT ( 'NONE', #2437 ) ;
#37378=DIRECTION ( 'NONE',  ( 0.000000000000000000, 0.2079116908177545131, -0.9781476007338066880 ) ) ;
#37379=EDGE_CURVE ( 'NONE', #15888, #47617, #1912, .T. ) ;
#37383=LINE ( 'NONE', #2085, #35172 ) ;
#37385=CARTESIAN_POINT ( 'NONE',  ( 15.00000000000000000, -1.278221433540145391, 26.51162292216073979 ) ) ;
#37387=CARTESIAN_POINT ( 'NONE',  ( 5.999999999999999112, 63.97538442413426907, 51.29473840253246664 ) ) ;
#37398=DIRECTION ( 'NONE',  ( 0.000000000000000000, 0.000000000000000000, 1.000000000000000000 ) ) ;
#37410=VERTEX_POINT ( 'NONE', #48252 ) ;
#37415=DIRECTION ( 'NONE',  ( 0.000000000000000000, 0.000000000000000000, -1.000000000000000000 ) ) ;
#37425=DIRECTION ( 'NONE',  ( -1.000000000000000000, 0.000000000000000000, -0.000000000000000000 ) ) ;
#37444=ORIENTED_EDGE ( 'NONE', *, *, #10185, .F. ) ;
#37445=DIRECTION ( 'NONE',  ( 0.000000000000000000, 0.000000000000000000, 1.000000000000000000 ) ) ;
#37447=ORIENTED_EDGE ( 'NONE', *, *, #1597, .T. ) ;
#37451=ADVANCED_FACE ( 'NONE', ( #6913 ), #47874, .T. ) ;
#37458=DIRECTION ( 'NONE',  ( -1.000000000000000000, -0.000000000000000000, -0.000000000000000000 ) ) ;
#37464=ORIENTED_EDGE ( 'NONE', *, *, #57542, .F. ) ;
#37471=CARTESIAN_POINT ( 'NONE',  ( 0.000000000000000000, -50.95692526931287603, -58.39081064771804819 ) ) ;
#37474=ORIENTED_EDGE ( 'NONE', *, *, #17594, .T. ) ;
#37476=ORIENTED_EDGE ( 'NONE', *, *, #14589, .T. ) ;
#37488=DIRECTION ( 'NONE',  ( 0.000000000000000000, 0.9723699203976756689, 0.2334453638559094157 ) ) ;
#37496=DIRECTION ( 'NONE',  ( -1.000000000000000000, -0.000000000000000000, -0.000000000000000000 ) ) ;
#37503=AXIS2_PLACEMENT_3D ( 'NONE', #15174, #14437, #55402 ) ;
#37510=DIRECTION ( 'NONE',  ( -1.000000000000000000, 0.000000000000000000, 0.000000000000000000 ) ) ;
#37531=AXIS2_PLACEMENT_3D ( 'NONE', #35121, #29461, #6915 ) ;
#37532=ORIENTED_EDGE ( 'NONE', *, *, #6720, .T. ) ;
#37538=DIRECTION ( 'NONE',  ( -1.000000000000000000, -0.000000000000000000, -0.000000000000000000 ) ) ;
#37539=AXIS2_PLACEMENT_3D ( 'NONE', #9503, #55370, #3885 ) ;
#37544=VERTEX_POINT ( 'NONE', #38072 ) ;
#37547=AXIS2_PLACEMENT_3D ( 'NONE', #55051, #4318, #21195 ) ;
#37548=VERTEX_POINT ( 'NONE', #26421 ) ;
#37551=AXIS2_PLACEMENT_3D ( 'NONE', #4219, #73351, #72242 ) ;
#37553=CARTESIAN_POINT ( 'NONE',  ( 5.999999999999999112, 33.71516098798849015, -74.74816331893393340 ) ) ;
#37561=ORIENTED_EDGE ( 'NONE', *, *, #12068, .T. ) ;
#37569=CARTESIAN_POINT ( 'NONE',  ( 15.00000000000000000, 5.835314593368777558, 22.81335362449846471 ) ) ;
#37570=ORIENTED_EDGE ( 'NONE', *, *, #48491, .T. ) ;
#37572=EDGE_LOOP ( 'NONE', ( #66786, #50870, #34208, #24579 ) ) ;
#37582=DIRECTION ( 'NONE',  ( -1.000000000000000000, -0.000000000000000000, -0.000000000000000000 ) ) ;
#37584=CARTESIAN_POINT ( 'NONE',  ( 11.99999999999999822, 2.543863470248389103, 81.96053171279902472 ) ) ;
#37585=DIRECTION ( 'NONE',  ( -1.000000000000000000, 0.000000000000000000, -0.000000000000000000 ) ) ;
#37589=LINE ( 'NONE', #3388, #9685 ) ;
#37593=CARTESIAN_POINT ( 'NONE',  ( 11.99999999999999822, 3.894527615417885169, 81.90746397400390322 ) ) ;
#37594=EDGE_CURVE ( 'NONE', #55761, #15852, #70269, .T. ) ;
#37601=DIRECTION ( 'NONE',  ( -1.000000000000000000, -0.000000000000000000, -0.000000000000000000 ) ) ;
#37606=CARTESIAN_POINT ( 'NONE',  ( 11.99999999999999822, -44.88180994100329713, -63.18004540533077318 ) ) ;
#37607=DIRECTION ( 'NONE',  ( 0.000000000000000000, 0.9510565162951544194, -0.3090169943749446757 ) ) ;
#37609=DIRECTION ( 'NONE',  ( -1.000000000000000000, -0.000000000000000000, -0.000000000000000000 ) ) ;
#37611=DIRECTION ( 'NONE',  ( -1.000000000000000000, -0.000000000000000000, -0.000000000000000000 ) ) ;
#37614=VERTEX_POINT ( 'NONE', #73383 ) ;
#37616=LINE ( 'NONE', #66553, #44322 ) ;
#37618=DIRECTION ( 'NONE',  ( -1.000000000000000000, 0.000000000000000000, 0.000000000000000000 ) ) ;
#37622=LINE ( 'NONE', #55272, #4728 ) ;
#37644=AXIS2_PLACEMENT_3D ( 'NONE', #33261, #41061, #28374 ) ;
#37647=AXIS2_PLACEMENT_3D ( 'NONE', #41214, #35932, #7737 ) ;
#37649=ORIENTED_EDGE ( 'NONE', *, *, #59532, .F. ) ;
#37653=VECTOR ( 'NONE', #67278, 1000.000000000000000 ) ;
#37654=DIRECTION ( 'NONE',  ( 0.000000000000000000, 0.000000000000000000, 1.000000000000000000 ) ) ;
#37676=LINE ( 'NONE', #30168, #44586 ) ;
#37678=CARTESIAN_POINT ( 'NONE',  ( 11.99999999999999822, -10.30890764327441289, 81.34940948281332851 ) ) ;
#37682=ADVANCED_FACE ( 'NONE', ( #11707 ), #40674, .T. ) ;
#37689=VECTOR ( 'NONE', #74340, 1000.000000000000000 ) ;
#37692=VECTOR ( 'NONE', #24205, 1000.000000000000000 ) ;
#37693=ADVANCED_FACE ( 'NONE', ( #57602 ), #27897, .F. ) ;
#37694=ADVANCED_FACE ( 'NONE', ( #488 ), #44836, .T. ) ;
#37697=VECTOR ( 'NONE', #32614, 1000.000000000000000 ) ;
#37703=DIRECTION ( 'NONE',  ( 0.000000000000000000, 0.9135454576426058626, 0.4067366430757889950 ) ) ;
#37705=VECTOR ( 'NONE', #940, 1000.000000000000114 ) ;
#37719=LINE ( 'NONE', #20776, #24038 ) ;
#37723=ADVANCED_FACE ( 'NONE', ( #74131 ), #22640, .T. ) ;
#37729=VERTEX_POINT ( 'NONE', #11344 ) ;
#37736=CARTESIAN_POINT ( 'NONE',  ( 11.99999999999999822, -0.8261519478425843888, -77.49459641780887864 ) ) ;
#37738=ORIENTED_EDGE ( 'NONE', *, *, #70927, .T. ) ;
#37760=CARTESIAN_POINT ( 'NONE',  ( 11.99999999999999822, 0.000000000000000000, 0.000000000000000000 ) ) ;
#37762=CARTESIAN_POINT ( 'NONE',  ( 0.000000000000000000, 0.000000000000000000, 0.000000000000000000 ) ) ;
#37764=DIRECTION ( 'NONE',  ( 0.000000000000000000, -0.5877852522924625900, -0.8090169943749551118 ) ) ;
#37767=CIRCLE ( 'NONE', #41352, 82.00000000000000000 ) ;
#37775=CARTESIAN_POINT ( 'NONE',  ( 0.000000000000000000, -73.44644590900077219, 24.73286445877677764 ) ) ;
#37777=DIRECTION ( 'NONE',  ( 0.000000000000000000, -0.9781476007338065770, -0.2079116908177544853 ) ) ;
#37781=FACE_OUTER_BOUND ( 'NONE', #39896, .T. ) ;
#37785=EDGE_CURVE ( 'NONE', #68051, #66576, #12746, .T. ) ;
#37794=EDGE_CURVE ( 'NONE', #18706, #39724, #58380, .T. ) ;
#37800=ORIENTED_EDGE ( 'NONE', *, *, #18727, .F. ) ;
#37803=DIRECTION ( 'NONE',  ( -1.000000000000000000, 0.000000000000000000, 0.000000000000000000 ) ) ;
#37804=ADVANCED_FACE ( 'NONE', ( #64348 ), #30112, .T. ) ;
#37808=ADVANCED_FACE ( 'NONE', ( #59442 ), #53063, .T. ) ;
#37816=CIRCLE ( 'NONE', #64227, 31.99999999999998224 ) ;
#37819=CARTESIAN_POINT ( 'NONE',  ( -10.00000000000000000, 0.000000000000000000, 0.000000000000000000 ) ) ;
#37826=VECTOR ( 'NONE', #18604, 1000.000000000000000 ) ;
#37840=ORIENTED_EDGE ( 'NONE', *, *, #67565, .F. ) ;
#37856=ORIENTED_EDGE ( 'NONE', *, *, #18856, .F. ) ;
#37857=EDGE_CURVE ( 'NONE', #50325, #30840, #42766, .T. ) ;
#37858=VERTEX_POINT ( 'NONE', #26689 ) ;
#37861=CARTESIAN_POINT ( 'NONE',  ( 15.00000000000000000, 16.61724383029390140, 20.69703378468902955 ) ) ;
#37862=DIRECTION ( 'NONE',  ( -1.000000000000000000, 0.000000000000000000, 0.000000000000000000 ) ) ;
#37874=DIRECTION ( 'NONE',  ( 0.000000000000000000, 0.000000000000000000, -1.000000000000000000 ) ) ;
#37885=ORIENTED_EDGE ( 'NONE', *, *, #39255, .F. ) ;
#37893=EDGE_LOOP ( 'NONE', ( #36893, #58625, #32604, #30156 ) ) ;
#37894=CYLINDRICAL_SURFACE ( 'NONE', #12631, 77.49899999999999523 ) ;
#37899=EDGE_LOOP ( 'NONE', ( #25848, #49476, #35541, #4931 ) ) ;
#37909=EDGE_LOOP ( 'NONE', ( #44241, #63100, #8759, #64372 ) ) ;
#37910=AXIS2_PLACEMENT_3D ( 'NONE', #42283, #65209, #13683 ) ;
#37926=CARTESIAN_POINT ( 'NONE',  ( -10.00000000000000000, 0.000000000000000000, 0.000000000000000000 ) ) ;
#37929=ORIENTED_EDGE ( 'NONE', *, *, #16290, .F. ) ;
#37931=ORIENTED_EDGE ( 'NONE', *, *, #5710, .F. ) ;
#37932=FACE_OUTER_BOUND ( 'NONE', #40534, .T. ) ;
#37938=ADVANCED_FACE ( 'NONE', ( #19938 ), #31588, .T. ) ;
#37947=LINE ( 'NONE', #54862, #69303 ) ;
#37951=LINE ( 'NONE', #61629, #28905 ) ;
#37960=DIRECTION ( 'NONE',  ( -1.000000000000000000, -0.000000000000000000, 0.000000000000000000 ) ) ;
#37969=AXIS2_PLACEMENT_3D ( 'NONE', #21583, #38140, #27602 ) ;
#37970=DIRECTION ( 'NONE',  ( -1.000000000000000000, 0.000000000000000000, 0.000000000000000000 ) ) ;
#37972=CIRCLE ( 'NONE', #21155, 31.99999999999998579 ) ;
#37975=DIRECTION ( 'NONE',  ( 0.000000000000000000, -0.5877852522924797984, -0.8090169943749426773 ) ) ;
#37976=CARTESIAN_POINT ( 'NONE',  ( 11.99999999999999822, 46.21855187248630870, 62.20884554314035597 ) ) ;
#37990=CARTESIAN_POINT ( 'NONE',  ( 11.99999999999999822, -62.50884508063453637, 41.76106447765467777 ) ) ;
#38004=CARTESIAN_POINT ( 'NONE',  ( 11.99999999999999822, 26.02418014898407961, -70.52718814184231633 ) ) ;
#38011=DIRECTION ( 'NONE',  ( 0.000000000000000000, 0.9723699203976756689, 0.2334453638559095823 ) ) ;
#38012=ORIENTED_EDGE ( 'NONE', *, *, #26509, .F. ) ;
#38016=VERTEX_POINT ( 'NONE', #22935 ) ;
#38018=DIRECTION ( 'NONE',  ( -1.000000000000000000, -0.000000000000000000, -0.000000000000000000 ) ) ;
#38033=DIRECTION ( 'NONE',  ( 0.000000000000000000, 0.3826834323650905589, -0.9238795325112864054 ) ) ;
#38035=DIRECTION ( 'NONE',  ( 0.000000000000000000, -0.1045284632676570791, -0.9945218953682730678 ) ) ;
#38037=AXIS2_PLACEMENT_3D ( 'NONE', #58238, #6737, #52586 ) ;
#38042=AXIS2_PLACEMENT_3D ( 'NONE', #19315, #54647, #53912 ) ;
#38043=CARTESIAN_POINT ( 'NONE',  ( 0.000000000000000000, 20.40083707022987625, -72.35432306680462489 ) ) ;
#38049=DIRECTION ( 'NONE',  ( 0.000000000000000000, 0.9969173337331276308, 0.07845909572784874608 ) ) ;
#38050=DIRECTION ( 'NONE',  ( -1.000000000000000000, -0.000000000000000000, -0.000000000000000000 ) ) ;
#38051=DIRECTION ( 'NONE',  ( 1.000000000000000000, -0.000000000000000000, -0.000000000000000000 ) ) ;
#38055=CARTESIAN_POINT ( 'NONE',  ( 11.99999999999999822, 0.000000000000000000, 0.000000000000000000 ) ) ;
#38063=ORIENTED_EDGE ( 'NONE', *, *, #62397, .T. ) ;
#38065=CYLINDRICAL_SURFACE ( 'NONE', #74310, 31.99999999999998579 ) ;
#38072=CARTESIAN_POINT ( 'NONE',  ( 0.000000000000000000, 18.89407956138257205, 75.16055320797038064 ) ) ;
#38074=DIRECTION ( 'NONE',  ( 1.000000000000000000, 0.000000000000000000, -0.000000000000000000 ) ) ;
#38079=VERTEX_POINT ( 'NONE', #27432 ) ;
#38103=DIRECTION ( 'NONE',  ( 0.000000000000000000, 0.2334453638558990629, 0.9723699203976782224 ) ) ;
#38105=FACE_OUTER_BOUND ( 'NONE', #6477, .T. ) ;
#38114=DIRECTION ( 'NONE',  ( 0.000000000000000000, -0.5877852522924787992, -0.8090169943749434545 ) ) ;
#38116=DIRECTION ( 'NONE',  ( 0.000000000000000000, 0.6494480483301848794, -0.7604059656000299317 ) ) ;
#38120=AXIS2_PLACEMENT_3D ( 'NONE', #43590, #4479, #26639 ) ;
#38123=DIRECTION ( 'NONE',  ( 0.000000000000000000, 0.000000000000000000, 1.000000000000000000 ) ) ;
#38132=CARTESIAN_POINT ( 'NONE',  ( 11.99999999999999822, 0.8261519478431255115, 77.49459641780886443 ) ) ;
#38133=CARTESIAN_POINT ( 'NONE',  ( 11.99999999999999822, -65.64334221924882229, -41.19522573413803457 ) ) ;
#38136=EDGE_CURVE ( 'NONE', #45028, #65292, #69226, .T. ) ;
#38140=DIRECTION ( 'NONE',  ( -1.000000000000000000, 0.000000000000000000, 0.000000000000000000 ) ) ;
#38143=CARTESIAN_POINT ( 'NONE',  ( 15.00000000000000000, -23.29833615347104470, 3.418703333116808629 ) ) ;
#38145=CYLINDRICAL_SURFACE ( 'NONE', #12465, 31.99999999999998579 ) ;
#38146=CARTESIAN_POINT ( 'NONE',  ( 11.99999999999999822, 80.28980883073781172, -16.65972982744850128 ) ) ;
#38149=VECTOR ( 'NONE', #2774, 999.9999999999998863 ) ;
#38164=ORIENTED_EDGE ( 'NONE', *, *, #68139, .F. ) ;
#38165=VECTOR ( 'NONE', #28427, 999.9999999999998863 ) ;
#38166=AXIS2_PLACEMENT_3D ( 'NONE', #38990, #10034, #8928 ) ;
#38169=VECTOR ( 'NONE', #35812, 1000.000000000000000 ) ;
#38172=AXIS2_PLACEMENT_3D ( 'NONE', #42590, #49686, #30922 ) ;
#38173=EDGE_CURVE ( 'NONE', #41269, #73384, #70423, .T. ) ;
#38184=ORIENTED_EDGE ( 'NONE', *, *, #37857, .T. ) ;
#38186=CYLINDRICAL_SURFACE ( 'NONE', #33374, 82.00000000000000000 ) ;
#38189=PLANE ( 'NONE',  #45066 ) ;
#38191=FACE_OUTER_BOUND ( 'NONE', #48909, .T. ) ;
#38192=CARTESIAN_POINT ( 'NONE',  ( 0.000000000000000000, 65.59268652807263322, -36.72794159290169347 ) ) ;
#38193=AXIS2_PLACEMENT_3D ( 'NONE', #67392, #16632, #10243 ) ;
#38198=VERTEX_POINT ( 'NONE', #70602 ) ;
#38202=ORIENTED_EDGE ( 'NONE', *, *, #11193, .T. ) ;
#38204=ADVANCED_FACE ( 'NONE', ( #12732 ), #40960, .T. ) ;
#38215=EDGE_CURVE ( 'NONE', #14708, #31218, #7987, .T. ) ;
#38216=DIRECTION ( 'NONE',  ( 0.000000000000000000, 0.000000000000000000, 1.000000000000000000 ) ) ;
#38217=EDGE_CURVE ( 'NONE', #52520, #70963, #74038, .T. ) ;
#38218=LINE ( 'NONE', #26931, #72652 ) ;
#38219=CARTESIAN_POINT ( 'NONE',  ( 11.99999999999999822, 65.64334221924964652, -41.19522573413665611 ) ) ;
#38236=CYLINDRICAL_SURFACE ( 'NONE', #68848, 77.49899999999999523 ) ;
#38237=FACE_OUTER_BOUND ( 'NONE', #45137, .T. ) ;
#38244=CARTESIAN_POINT ( 'NONE',  ( -10.00000000000000000, 0.000000000000000000, 0.000000000000000000 ) ) ;
#38247=AXIS2_PLACEMENT_3D ( 'NONE', #14288, #67937, #37607 ) ;
#38261=EDGE_LOOP ( 'NONE', ( #64048, #55284, #71930, #62910 ) ) ;
#38271=AXIS2_PLACEMENT_3D ( 'NONE', #40943, #46571, #17266 ) ;
#38272=EDGE_CURVE ( 'NONE', #42183, #7988, #45242, .T. ) ;
#38276=ORIENTED_EDGE ( 'NONE', *, *, #71288, .T. ) ;
#38280=AXIS2_PLACEMENT_3D ( 'NONE', #31953, #66554, #3415 ) ;
#38298=ORIENTED_EDGE ( 'NONE', *, *, #42427, .T. ) ;
#38302=VECTOR ( 'NONE', #37254, 1000.000000000000000 ) ;
#38304=ORIENTED_EDGE ( 'NONE', *, *, #1925, .F. ) ;
#38308=EDGE_CURVE ( 'NONE', #43291, #64554, #26011, .T. ) ;
#38310=COLOUR_RGB ( '', 0.40784314, 0.44705882, 0.49803922) ;
#38313=DIRECTION ( 'NONE',  ( 0.000000000000000000, 0.000000000000000000, 1.000000000000000000 ) ) ;
#38324=DIRECTION ( 'NONE',  ( -1.000000000000000000, -0.000000000000000000, -0.000000000000000000 ) ) ;
#38325=CARTESIAN_POINT ( 'NONE',  ( 11.99999999999999822, 75.11764819372142199, 2.946379043147685728 ) ) ;
#38328=AXIS2_PLACEMENT_3D ( 'NONE', #17765, #70000, #29046 ) ;
#38329=FACE_OUTER_BOUND ( 'NONE', #36041, .T. ) ;
#38330=CARTESIAN_POINT ( 'NONE',  ( 15.00000000000000000, 18.84667830672579569, -18.68964196561269375 ) ) ;
#38332=AXIS2_PLACEMENT_3D ( 'NONE', #36915, #13611, #48926 ) ;
#38341=CARTESIAN_POINT ( 'NONE',  ( 11.99999999999999822, 0.000000000000000000, 0.000000000000000000 ) ) ;
#38345=CARTESIAN_POINT ( 'NONE',  ( 0.000000000000000000, 0.000000000000000000, 0.000000000000000000 ) ) ;
#38347=EDGE_CURVE ( 'NONE', #44140, #58013, #57209, .T. ) ;
#38358=DIRECTION ( 'NONE',  ( 0.000000000000000000, 0.000000000000000000, 1.000000000000000000 ) ) ;
#38364=ORIENTED_EDGE ( 'NONE', *, *, #49729, .F. ) ;
#38368=ORIENTED_EDGE ( 'NONE', *, *, #44652, .T. ) ;
#38369=EDGE_CURVE ( 'NONE', #53279, #14313, #20217, .T. ) ;
#38372=ORIENTED_EDGE ( 'NONE', *, *, #43333, .T. ) ;
#38374=DIRECTION ( 'NONE',  ( -1.000000000000000000, -0.000000000000000000, 0.000000000000000000 ) ) ;
#38378=ORIENTED_EDGE ( 'NONE', *, *, #16245, .T. ) ;
#38382=CIRCLE ( 'NONE', #66032, 82.00000000000000000 ) ;
#38383=AXIS2_PLACEMENT_3D ( 'NONE', #2852, #65242, #49417 ) ;
#38384=ORIENTED_EDGE ( 'NONE', *, *, #73580, .T. ) ;
#38396=DIRECTION ( 'NONE',  ( -1.000000000000000000, -0.000000000000000000, 0.000000000000000000 ) ) ;
#38398=ORIENTED_EDGE ( 'NONE', *, *, #61828, .F. ) ;
#38404=CYLINDRICAL_SURFACE ( 'NONE', #65610, 31.99999999999998579 ) ;
#38408=CYLINDRICAL_SURFACE ( 'NONE', #6277, 31.99999999999998579 ) ;
#38417=CIRCLE ( 'NONE', #52798, 77.49900000000000944 ) ;
#38418=FACE_OUTER_BOUND ( 'NONE', #5597, .T. ) ;
#38422=DIRECTION ( 'NONE',  ( 0.000000000000000000, 0.3826834323650840086, 0.9238795325112891810 ) ) ;
#38427=CARTESIAN_POINT ( 'NONE',  ( 0.000000000000000000, -34.94270380257692921, 74.18225833017875459 ) ) ;
#38434=ADVANCED_FACE ( 'NONE', ( #72463 ), #20967, .T. ) ;
#38435=DIRECTION ( 'NONE',  ( 0.000000000000000000, -0.9781476007338043566, 0.2079116908177651712 ) ) ;
#38440=DIRECTION ( 'NONE',  ( 0.000000000000000000, 0.000000000000000000, 1.000000000000000000 ) ) ;
#38445=VERTEX_POINT ( 'NONE', #10060 ) ;
#38446=EDGE_CURVE ( 'NONE', #20162, #46914, #27342, .T. ) ;
#38447=DIRECTION ( 'NONE',  ( 0.000000000000000000, -0.7071067811865536790, 0.7071067811865414665 ) ) ;
#38450=DIRECTION ( 'NONE',  ( -1.000000000000000000, -0.000000000000000000, -0.000000000000000000 ) ) ;
#38457=VECTOR ( 'NONE', #53739, 1000.000000000000114 ) ;
#38463=CARTESIAN_POINT ( 'NONE',  ( 0.000000000000000000, -59.46389618801929089, -49.70050353004953081 ) ) ;
#38467=ORIENTED_EDGE ( 'NONE', *, *, #74077, .T. ) ;
#38472=VERTEX_POINT ( 'NONE', #55926 ) ;
#38479=ADVANCED_FACE ( 'NONE', ( #56307 ), #73206, .T. ) ;
#38481=DIRECTION ( 'NONE',  ( 0.000000000000000000, 0.000000000000000000, 1.000000000000000000 ) ) ;
#38489=ORIENTED_EDGE ( 'NONE', *, *, #46795, .F. ) ;
#38492=VERTEX_POINT ( 'NONE', #51391 ) ;
#38493=CARTESIAN_POINT ( 'NONE',  ( -10.00000000000000000, 0.000000000000000000, 0.000000000000000000 ) ) ;
#38495=CARTESIAN_POINT ( 'NONE',  ( 0.000000000000000000, -12.93880638057260590, -76.41127070299285151 ) ) ;
#38505=FACE_OUTER_BOUND ( 'NONE', #65916, .T. ) ;
#38510=CARTESIAN_POINT ( 'NONE',  ( 11.99999999999999822, 0.000000000000000000, 0.000000000000000000 ) ) ;
#38517=LINE ( 'NONE', #61456, #24627 ) ;
#38520=CARTESIAN_POINT ( 'NONE',  ( 11.99999999999999822, -2.543863470248965086, 81.96053171279902472 ) ) ;
#38521=DIRECTION ( 'NONE',  ( -0.000000000000000000, 0.4067366430757998752, 0.9135454576426010886 ) ) ;
#38532=DIRECTION ( 'NONE',  ( -1.000000000000000000, -0.000000000000000000, -0.000000000000000000 ) ) ;
#38542=EDGE_LOOP ( 'NONE', ( #41068, #47161, #22718, #24254 ) ) ;
#38549=AXIS2_PLACEMENT_3D ( 'NONE', #61822, #28326, #34345 ) ;
#38557=FACE_OUTER_BOUND ( 'NONE', #19152, .T. ) ;
#38566=ORIENTED_EDGE ( 'NONE', *, *, #38446, .T. ) ;
#38569=AXIS2_PLACEMENT_3D ( 'NONE', #1464, #28880, #52538 ) ;
#38571=DIRECTION ( 'NONE',  ( -1.000000000000000000, -0.000000000000000000, -0.000000000000000000 ) ) ;
#38578=ORIENTED_EDGE ( 'NONE', *, *, #19614, .T. ) ;
#38588=LINE ( 'NONE', #61520, #13814 ) ;
#38590=ORIENTED_EDGE ( 'NONE', *, *, #43989, .T. ) ;
#38591=CARTESIAN_POINT ( 'NONE',  ( 0.000000000000000000, 0.000000000000000000, 0.000000000000000000 ) ) ;
#38595=ORIENTED_EDGE ( 'NONE', *, *, #71858, .T. ) ;
#38606=DIRECTION ( 'NONE',  ( -1.000000000000000000, 0.000000000000000000, 0.000000000000000000 ) ) ;
#38615=DIRECTION ( 'NONE',  ( -1.000000000000000000, 0.000000000000000000, 0.000000000000000000 ) ) ;
#38620=VECTOR ( 'NONE', #24263, 1000.000000000000000 ) ;
#38621=FACE_OUTER_BOUND ( 'NONE', #58429, .T. ) ;
#38630=CIRCLE ( 'NONE', #18221, 77.49899999999999523 ) ;
#38631=CIRCLE ( 'NONE', #62632, 31.99999999999998579 ) ;
#38636=EDGE_CURVE ( 'NONE', #8415, #58803, #71674, .T. ) ;
#38640=ORIENTED_EDGE ( 'NONE', *, *, #22132, .F. ) ;
#38642=EDGE_CURVE ( 'NONE', #70171, #5010, #23652, .T. ) ;
#38652=VERTEX_POINT ( 'NONE', #23566 ) ;
#38656=LINE ( 'NONE', #68346, #40583 ) ;
#38658=ORIENTED_EDGE ( 'NONE', *, *, #11353, .T. ) ;
#38662=ORIENTED_EDGE ( 'NONE', *, *, #45201, .T. ) ;
#38673=FACE_OUTER_BOUND ( 'NONE', #41873, .T. ) ;
#38674=CARTESIAN_POINT ( 'NONE',  ( 15.00000000000000000, 20.85821328998756385, 10.92862929874494249 ) ) ;
#38676=DIRECTION ( 'NONE',  ( 0.000000000000000000, 0.000000000000000000, -1.000000000000000000 ) ) ;
#38681=ORIENTED_EDGE ( 'NONE', *, *, #38369, .T. ) ;
#38687=LINE ( 'NONE', #3377, #64707 ) ;
#38692=CARTESIAN_POINT ( 'NONE',  ( 15.00000000000000000, 16.83928648764945635, 16.46020748918027010 ) ) ;
#38701=ADVANCED_FACE ( 'NONE', ( #20518 ), #60384, .T. ) ;
#38704=CARTESIAN_POINT ( 'NONE',  ( 11.99999999999999822, 46.11716303203283474, -67.80270845531838120 ) ) ;
#38719=CARTESIAN_POINT ( 'NONE',  ( 15.00000000000000000, 0.000000000000000000, 0.000000000000000000 ) ) ;
#38726=AXIS2_PLACEMENT_3D ( 'NONE', #1205, #7170, #35718 ) ;
#38728=VERTEX_POINT ( 'NONE', #20133 ) ;
#38748=ORIENTED_EDGE ( 'NONE', *, *, #49895, .T. ) ;
#38752=ORIENTED_EDGE ( 'NONE', *, *, #11231, .F. ) ;
#38758=EDGE_LOOP ( 'NONE', ( #6602, #28551, #6517, #67252 ) ) ;
#38759=CIRCLE ( 'NONE', #30375, 82.00000000000000000 ) ;
#38762=DIRECTION ( 'NONE',  ( 0.000000000000000000, 0.000000000000000000, 1.000000000000000000 ) ) ;
#38763=DIRECTION ( 'NONE',  ( -1.000000000000000000, 0.000000000000000000, 0.000000000000000000 ) ) ;
#38768=ORIENTED_EDGE ( 'NONE', *, *, #50053, .T. ) ;
#38778=FACE_OUTER_BOUND ( 'NONE', #33356, .T. ) ;
#38784=ORIENTED_EDGE ( 'NONE', *, *, #47679, .F. ) ;
#38793=ORIENTED_EDGE ( 'NONE', *, *, #32143, .F. ) ;
#38802=VERTEX_POINT ( 'NONE', #8118 ) ;
#38812=AXIS2_PLACEMENT_3D ( 'NONE', #1334, #70059, #47152 ) ;
#38817=CARTESIAN_POINT ( 'NONE',  ( 0.000000000000000000, 0.000000000000000000, 0.000000000000000000 ) ) ;
#38819=VECTOR ( 'NONE', #47073, 1000.000000000000000 ) ;
#38828=CIRCLE ( 'NONE', #6434, 31.99999999999998224 ) ;
#38831=ORIENTED_EDGE ( 'NONE', *, *, #57917, .T. ) ;
#38834=DIRECTION ( 'NONE',  ( 0.000000000000000000, 0.5877852522924684742, 0.8090169943749507819 ) ) ;
#38835=ORIENTED_EDGE ( 'NONE', *, *, #29359, .T. ) ;
#38836=ORIENTED_EDGE ( 'NONE', *, *, #1597, .F. ) ;
#38842=ORIENTED_EDGE ( 'NONE', *, *, #23929, .T. ) ;
#38849=CARTESIAN_POINT ( 'NONE',  ( 15.00000000000000000, -22.67460108101782978, -6.353146135317906840 ) ) ;
#38856=AXIS2_PLACEMENT_3D ( 'NONE', #48687, #47581, #48321 ) ;
#38859=EDGE_LOOP ( 'NONE', ( #37101, #26221, #17820, #35756 ) ) ;
#38865=AXIS2_PLACEMENT_3D ( 'NONE', #48958, #44821, #15873 ) ;
#38867=ORIENTED_EDGE ( 'NONE', *, *, #21613, .F. ) ;
#38870=DIRECTION ( 'NONE',  ( -1.000000000000000000, -0.000000000000000000, -0.000000000000000000 ) ) ;
#38875=EDGE_CURVE ( 'NONE', #38492, #67492, #17015, .T. ) ;
#38878=CARTESIAN_POINT ( 'NONE',  ( 11.99999999999999822, -24.73286445877757345, 73.44644590900053061 ) ) ;
#38883=CARTESIAN_POINT ( 'NONE',  ( 0.000000000000000000, 12.93880638057315302, 76.41127070299275204 ) ) ;
#38890=CIRCLE ( 'NONE', #4132, 82.00000000000000000 ) ;
#38892=DIRECTION ( 'NONE',  ( 0.000000000000000000, 0.000000000000000000, 1.000000000000000000 ) ) ;
#38893=LINE ( 'NONE', #67834, #9300 ) ;
#38894=DIRECTION ( 'NONE',  ( -1.000000000000000000, 0.000000000000000000, 0.000000000000000000 ) ) ;
#38896=EDGE_CURVE ( 'NONE', #57897, #63122, #40310, .T. ) ;
#38904=CARTESIAN_POINT ( 'NONE',  ( 0.000000000000000000, 0.000000000000000000, 0.000000000000000000 ) ) ;
#38912=CARTESIAN_POINT ( 'NONE',  ( 6.000000000000000000, 44.99326035066052043, 68.55367621811159040 ) ) ;
#38918=CARTESIAN_POINT ( 'NONE',  ( 11.99999999999999822, 41.19522573413733113, 65.64334221924924861 ) ) ;
#38920=ORIENTED_EDGE ( 'NONE', *, *, #35572, .T. ) ;
#38922=ORIENTED_EDGE ( 'NONE', *, *, #10687, .T. ) ;
#38945=VERTEX_POINT ( 'NONE', #9968 ) ;
#38963=ORIENTED_EDGE ( 'NONE', *, *, #32932, .T. ) ;
#38984=DIRECTION ( 'NONE',  ( 0.000000000000000000, 0.000000000000000000, 1.000000000000000000 ) ) ;
#38988=CARTESIAN_POINT ( 'NONE',  ( 11.99999999999999822, -68.67312586195022561, 35.91791733033451806 ) ) ;
#38990=CARTESIAN_POINT ( 'NONE',  ( 0.000000000000000000, 0.000000000000000000, 0.000000000000000000 ) ) ;
#38991=EDGE_CURVE ( 'NONE', #36331, #4121, #20971, .T. ) ;
#38994=DIRECTION ( 'NONE',  ( -1.000000000000000000, -0.000000000000000000, 0.000000000000000000 ) ) ;
#38996=DIRECTION ( 'NONE',  ( -1.000000000000000000, 0.000000000000000000, -0.000000000000000000 ) ) ;
#39001=AXIS2_PLACEMENT_3D ( 'NONE', #50863, #66682, #16660 ) ;
#39008=DIRECTION ( 'NONE',  ( 0.000000000000000000, 0.9876883405951371042, 0.1564344650402347547 ) ) ;
#39010=ORIENTED_EDGE ( 'NONE', *, *, #29100, .T. ) ;
#39013=DIRECTION ( 'NONE',  ( -1.000000000000000000, -0.000000000000000000, 0.000000000000000000 ) ) ;
#39019=ORIENTED_EDGE ( 'NONE', *, *, #22838, .T. ) ;
#39031=ADVANCED_FACE ( 'NONE', ( #54819 ), #36782, .T. ) ;
#39034=ORIENTED_EDGE ( 'NONE', *, *, #39255, .T. ) ;
#39041=AXIS2_PLACEMENT_3D ( 'NONE', #6051, #39510, #798 ) ;
#39043=CARTESIAN_POINT ( 'NONE',  ( 11.99999999999999822, 36.73666225445894185, 65.58780272294090707 ) ) ;
#39049=CYLINDRICAL_SURFACE ( 'NONE', #66885, 31.99999999999998579 ) ;
#39052=ORIENTED_EDGE ( 'NONE', *, *, #30687, .F. ) ;
#39066=DIRECTION ( 'NONE',  ( -1.000000000000000000, 0.000000000000000000, 0.000000000000000000 ) ) ;
#39067=AXIS2_PLACEMENT_3D ( 'NONE', #267, #11124, #56250 ) ;
#39078=PLANE ( 'NONE',  #3530 ) ;
#39082=CYLINDRICAL_SURFACE ( 'NONE', #16401, 31.99999999999998579 ) ;
#39094=DIRECTION ( 'NONE',  ( -1.000000000000000000, -0.000000000000000000, -0.000000000000000000 ) ) ;
#39097=ORIENTED_EDGE ( 'NONE', *, *, #19628, .T. ) ;
#39100=ORIENTED_EDGE ( 'NONE', *, *, #19170, .F. ) ;
#39110=LINE ( 'NONE', #60923, #63498 ) ;
#39119=CARTESIAN_POINT ( 'NONE',  ( 11.99999999999999822, -73.73191006444561424, -14.66109333815538918 ) ) ;
#39125=CARTESIAN_POINT ( 'NONE',  ( 11.99999999999999822, 0.000000000000000000, 0.000000000000000000 ) ) ;
#39128=EDGE_LOOP ( 'NONE', ( #28541, #71623, #47254, #37532 ) ) ;
#39131=DIRECTION ( 'NONE',  ( 0.000000000000000000, 0.000000000000000000, -1.000000000000000000 ) ) ;
#39138=ORIENTED_EDGE ( 'NONE', *, *, #40850, .T. ) ;
#39141=ORIENTED_EDGE ( 'NONE', *, *, #21739, .F. ) ;
#39144=ORIENTED_EDGE ( 'NONE', *, *, #55431, .T. ) ;
#39147=DIRECTION ( 'NONE',  ( 1.000000000000000000, -0.000000000000000000, 0.000000000000000000 ) ) ;
#39148=DIRECTION ( 'NONE',  ( -0.000000000000000000, -0.6691306063588670083, -0.7431448254773863615 ) ) ;
#39163=CARTESIAN_POINT ( 'NONE',  ( 0.000000000000000000, 0.000000000000000000, 0.000000000000000000 ) ) ;
#39165=AXIS2_PLACEMENT_3D ( 'NONE', #19633, #2766, #42956 ) ;
#39173=AXIS2_PLACEMENT_3D ( 'NONE', #65090, #47417, #35748 ) ;
#39176=CARTESIAN_POINT ( 'NONE',  ( 11.99999999999999822, -63.97538442413390669, -51.29473840253292138 ) ) ;
#39189=DIRECTION ( 'NONE',  ( 0.000000000000000000, 0.9135454576426005335, -0.4067366430758010409 ) ) ;
#39194=ORIENTED_EDGE ( 'NONE', *, *, #24069, .F. ) ;
#39197=ORIENTED_EDGE ( 'NONE', *, *, #33710, .T. ) ;
#39202=ORIENTED_EDGE ( 'NONE', *, *, #3344, .F. ) ;
#39205=EDGE_CURVE ( 'NONE', #50648, #24697, #61580, .T. ) ;
#39210=ORIENTED_EDGE ( 'NONE', *, *, #46401, .T. ) ;
#39212=ORIENTED_EDGE ( 'NONE', *, *, #51464, .F. ) ;
#39213=EDGE_CURVE ( 'NONE', #53067, #16620, #51778, .T. ) ;
#39228=CARTESIAN_POINT ( 'NONE',  ( 11.99999999999999822, 68.67312586194995561, 35.91791733033500122 ) ) ;
#39237=ORIENTED_EDGE ( 'NONE', *, *, #48324, .T. ) ;
#39240=EDGE_CURVE ( 'NONE', #24844, #55952, #15713, .T. ) ;
#39242=CARTESIAN_POINT ( 'NONE',  ( 11.99999999999999822, 0.000000000000000000, 0.000000000000000000 ) ) ;
#39245=CARTESIAN_POINT ( 'NONE',  ( 15.00000000000000000, -10.45096189432344502, -21.10159698893425784 ) ) ;
#39251=AXIS2_PLACEMENT_3D ( 'NONE', #67606, #60857, #26255 ) ;
#39255=EDGE_CURVE ( 'NONE', #15890, #12172, #57058, .T. ) ;
#39259=CARTESIAN_POINT ( 'NONE',  ( 0.000000000000000000, 0.000000000000000000, 21.00000000000000000 ) ) ;
#39263=AXIS2_PLACEMENT_3D ( 'NONE', #28649, #45605, #17744 ) ;
#39267=VECTOR ( 'NONE', #61484, 1000.000000000000114 ) ;
#39268=CYLINDRICAL_SURFACE ( 'NONE', #32107, 31.99999999999998579 ) ;
#39282=AXIS2_PLACEMENT_3D ( 'NONE', #37819, #55093, #72378 ) ;
#39286=CIRCLE ( 'NONE', #74098, 82.00000000000000000 ) ;
#39287=CARTESIAN_POINT ( 'NONE',  ( 11.99999999999999822, -46.11716303203136391, -67.80270845531939017 ) ) ;
#39288=ORIENTED_EDGE ( 'NONE', *, *, #64674, .T. ) ;
#39303=DIRECTION ( 'NONE',  ( -1.000000000000000000, 0.000000000000000000, 0.000000000000000000 ) ) ;
#39305=CARTESIAN_POINT ( 'NONE',  ( 15.00000000000000000, -13.04903810567646971, 19.60159698893442481 ) ) ;
#39307=AXIS2_PLACEMENT_3D ( 'NONE', #13511, #47722, #70265 ) ;
#39310=VERTEX_POINT ( 'NONE', #12652 ) ;
#39311=ORIENTED_EDGE ( 'NONE', *, *, #9692, .T. ) ;
#39314=CARTESIAN_POINT ( 'NONE',  ( 12.00000000000000000, -23.29833615347109088, -3.418703333116486665 ) ) ;
#39320=ORIENTED_EDGE ( 'NONE', *, *, #47954, .F. ) ;
#39329=LINE ( 'NONE', #21652, #8188 ) ;
#39336=CARTESIAN_POINT ( 'NONE',  ( 15.00000000000000000, 20.85821328998756385, 10.92862929874494249 ) ) ;
#39344=CARTESIAN_POINT ( 'NONE',  ( 0.000000000000000000, 14.66109333815564852, -73.73191006444555740 ) ) ;
#39352=CARTESIAN_POINT ( 'NONE',  ( 0.000000000000000000, -69.42325613327415113, -34.44570377933671779 ) ) ;
#39360=CARTESIAN_POINT ( 'NONE',  ( 6.000000000000000000, -79.10210256391383155, 21.60688246758558506 ) ) ;
#39362=CARTESIAN_POINT ( 'NONE',  ( 0.000000000000000000, 0.000000000000000000, 0.000000000000000000 ) ) ;
#39365=CARTESIAN_POINT ( 'NONE',  ( 15.00000000000000000, -3.948201729842355068, -23.21447184625292692 ) ) ;
#39366=CARTESIAN_POINT ( 'NONE',  ( 11.99999999999999822, -20.40083707022829174, -72.35432306680507963 ) ) ;
#39370=CIRCLE ( 'NONE', #36949, 77.49900000000000944 ) ;
#39372=EDGE_LOOP ( 'NONE', ( #18283, #48021, #63118, #41445 ) ) ;
#39377=EDGE_CURVE ( 'NONE', #71829, #37544, #3387, .T. ) ;
#39386=EDGE_CURVE ( 'NONE', #49355, #65052, #57409, .T. ) ;
#39400=VERTEX_POINT ( 'NONE', #7014 ) ;
#39414=ORIENTED_EDGE ( 'NONE', *, *, #57625, .F. ) ;
#39415=CARTESIAN_POINT ( 'NONE',  ( 11.99999999999999822, 0.8261519478431255115, 77.49459641780886443 ) ) ;
#39433=ORIENTED_EDGE ( 'NONE', *, *, #70592, .F. ) ;
#39438=DIRECTION ( 'NONE',  ( 0.000000000000000000, -0.4067366430758009854, -0.9135454576426004225 ) ) ;
#39439=CARTESIAN_POINT ( 'NONE',  ( 0.000000000000000000, 0.000000000000000000, 0.000000000000000000 ) ) ;
#39440=AXIS2_PLACEMENT_3D ( 'NONE', #46035, #56194, #5818 ) ;
#39442=CIRCLE ( 'NONE', #15422, 77.49900000000000944 ) ;
#39451=AXIS2_PLACEMENT_3D ( 'NONE', #27704, #8660, #5167 ) ;
#39456=DIRECTION ( 'NONE',  ( -1.000000000000000000, 0.000000000000000000, 0.000000000000000000 ) ) ;
#39464=EDGE_CURVE ( 'NONE', #16205, #37410, #32160, .T. ) ;
#39468=CARTESIAN_POINT ( 'NONE',  ( 12.00000000000000000, 16.83928648764922542, -16.46020748918050458 ) ) ;
#39469=DIRECTION ( 'NONE',  ( 0.000000000000000000, -0.3826834323650772363, -0.9238795325112919565 ) ) ;
#39470=VECTOR ( 'NONE', #46757, 1000.000000000000000 ) ;
#39476=VERTEX_POINT ( 'NONE', #66029 ) ;
#39479=ORIENTED_EDGE ( 'NONE', *, *, #47349, .F. ) ;
#39486=VECTOR ( 'NONE', #68831, 1000.000000000000114 ) ;
#39491=CARTESIAN_POINT ( 'NONE',  ( 15.00000000000000000, 16.83928648764922542, -16.46020748918050458 ) ) ;
#39493=CARTESIAN_POINT ( 'NONE',  ( 11.99999999999999822, -44.88180994100419952, 63.18004540533013369 ) ) ;
#39495=DIRECTION ( 'NONE',  ( 0.000000000000000000, -0.9876883405951394357, 0.1564344650402205716 ) ) ;
#39502=VERTEX_POINT ( 'NONE', #3626 ) ;
#39504=CARTESIAN_POINT ( 'NONE',  ( 0.000000000000000000, 71.21200624218852226, -40.65526001592539984 ) ) ;
#39506=ORIENTED_EDGE ( 'NONE', *, *, #73396, .T. ) ;
#39510=DIRECTION ( 'NONE',  ( -1.000000000000000000, -0.000000000000000000, -0.000000000000000000 ) ) ;
#39511=EDGE_LOOP ( 'NONE', ( #18403, #7944, #55378, #66455 ) ) ;
#39517=VERTEX_POINT ( 'NONE', #60754 ) ;
#39522=ORIENTED_EDGE ( 'NONE', *, *, #70440, .T. ) ;
#39544=CARTESIAN_POINT ( 'NONE',  ( 11.99999999999999822, 36.72794159290241822, 65.59268652807223532 ) ) ;
#39546=DIRECTION ( 'NONE',  ( -1.000000000000000000, -0.000000000000000000, -0.000000000000000000 ) ) ;
#39551=LINE ( 'NONE', #5350, #45294 ) ;
#39561=DIRECTION ( 'NONE',  ( 0.000000000000000000, 0.4539904997395478037, -0.8910065241883673437 ) ) ;
#39567=EDGE_CURVE ( 'NONE', #42672, #1062, #31051, .T. ) ;
#39570=DIRECTION ( 'NONE',  ( 0.000000000000000000, 0.5877852522924689183, -0.8090169943749504489 ) ) ;
#39571=CIRCLE ( 'NONE', #59985, 31.99999999999998579 ) ;
#39572=ORIENTED_EDGE ( 'NONE', *, *, #22263, .F. ) ;
#39575=ORIENTED_EDGE ( 'NONE', *, *, #16539, .T. ) ;
#39578=ORIENTED_EDGE ( 'NONE', *, *, #6732, .T. ) ;
#39579=FACE_OUTER_BOUND ( 'NONE', #28186, .T. ) ;
#39581=ORIENTED_EDGE ( 'NONE', *, *, #46269, .T. ) ;
#39590=ORIENTED_EDGE ( 'NONE', *, *, #36589, .T. ) ;
#39592=ORIENTED_EDGE ( 'NONE', *, *, #9583, .F. ) ;
#39594=AXIS2_PLACEMENT_3D ( 'NONE', #43852, #55489, #66767 ) ;
#39595=AXIS2_PLACEMENT_3D ( 'NONE', #68283, #45357, #57364 ) ;
#39597=DIRECTION ( 'NONE',  ( 0.000000000000000000, 0.000000000000000000, 1.000000000000000000 ) ) ;
#39603=DIRECTION ( 'NONE',  ( 0.000000000000000000, 0.000000000000000000, 1.000000000000000000 ) ) ;
#39607=ORIENTED_EDGE ( 'NONE', *, *, #30736, .F. ) ;
#39620=ORIENTED_EDGE ( 'NONE', *, *, #315, .F. ) ;
#39623=DIRECTION ( 'NONE',  ( -1.000000000000000000, 0.000000000000000000, 0.000000000000000000 ) ) ;
#39626=DIRECTION ( 'NONE',  ( 0.000000000000000000, 0.000000000000000000, 1.000000000000000000 ) ) ;
#39629=DIRECTION ( 'NONE',  ( -1.000000000000000000, -0.000000000000000000, -0.000000000000000000 ) ) ;
#39631=AXIS2_PLACEMENT_3D ( 'NONE', #71255, #65644, #45599 ) ;
#39636=AXIS2_PLACEMENT_3D ( 'NONE', #34346, #16695, #68578 ) ;
#39637=CARTESIAN_POINT ( 'NONE',  ( 11.99999999999999822, -74.74816331893454446, 33.71516098798715433 ) ) ;
#39640=CARTESIAN_POINT ( 'NONE',  ( 0.000000000000000000, -21.60688246758642705, 79.10210256391358996 ) ) ;
#39649=AXIS2_PLACEMENT_3D ( 'NONE', #17972, #7436, #7796 ) ;
#39651=ADVANCED_FACE ( 'NONE', ( #11098 ), #27642, .F. ) ;
#39655=CIRCLE ( 'NONE', #32432, 31.99999999999998579 ) ;
#39657=CIRCLE ( 'NONE', #52857, 77.49899999999999523 ) ;
#39669=CARTESIAN_POINT ( 'NONE',  ( 11.99999999999999822, 49.70050353004975818, -59.46389618801909904 ) ) ;
#39678=CYLINDRICAL_SURFACE ( 'NONE', #19642, 31.99999999999998579 ) ;
#39684=ORIENTED_EDGE ( 'NONE', *, *, #35237, .T. ) ;
#39696=DIRECTION ( 'NONE',  ( 0.000000000000000000, -0.3090169943749349613, -0.9510565162951576390 ) ) ;
#39704=ORIENTED_EDGE ( 'NONE', *, *, #12166, .F. ) ;
#39710=DIRECTION ( 'NONE',  ( -1.000000000000000000, 0.000000000000000000, -0.000000000000000000 ) ) ;
#39724=VERTEX_POINT ( 'NONE', #72742 ) ;
#39734=CARTESIAN_POINT ( 'NONE',  ( 15.00000000000000000, -11.95096189432312350, 23.69967320028773372 ) ) ;
#39743=DIRECTION ( 'NONE',  ( 0.000000000000000000, 0.000000000000000000, 1.000000000000000000 ) ) ;
#39744=ORIENTED_EDGE ( 'NONE', *, *, #35572, .F. ) ;
#39751=ORIENTED_EDGE ( 'NONE', *, *, #13756, .F. ) ;
#39752=CARTESIAN_POINT ( 'NONE',  ( 50.00005079999999680, 0.000000000000000000, 0.000000000000000000 ) ) ;
#39765=DIRECTION ( 'NONE',  ( 0.000000000000000000, -0.6494480483301903195, 0.7604059656000251577 ) ) ;
#39773=ORIENTED_EDGE ( 'NONE', *, *, #67756, .F. ) ;
#39775=DIRECTION ( 'NONE',  ( 0.000000000000000000, 0.7071067811865439090, 0.7071067811865512365 ) ) ;
#39791=CARTESIAN_POINT ( 'NONE',  ( 11.99999999999999822, 62.50884508063487033, -41.76106447765422303 ) ) ;
#39794=VERTEX_POINT ( 'NONE', #37278 ) ;
#39801=AXIS2_PLACEMENT_3D ( 'NONE', #60780, #20165, #25076 ) ;
#39804=LINE ( 'NONE', #16120, #37689 ) ;
#39811=DIRECTION ( 'NONE',  ( 0.000000000000000000, -0.9969173337331287410, 0.07845909572783495156 ) ) ;
#39814=CARTESIAN_POINT ( 'NONE',  ( 11.99999999999999822, 0.000000000000000000, 0.000000000000000000 ) ) ;
#39817=EDGE_CURVE ( 'NONE', #19352, #46404, #7003, .T. ) ;
#39823=DIRECTION ( 'NONE',  ( 0.000000000000000000, 0.9969173337331276308, 0.07845909572784864894 ) ) ;
#39828=CARTESIAN_POINT ( 'NONE',  ( 11.99999999999999822, -55.38113227695820484, 54.21277698773656084 ) ) ;
#39830=CARTESIAN_POINT ( 'NONE',  ( 11.99999999999999822, -65.58780272294100655, 36.73666225445870737 ) ) ;
#39846=AXIS2_PLACEMENT_3D ( 'NONE', #26280, #66880, #15369 ) ;
#39852=EDGE_LOOP ( 'NONE', ( #50302, #16697, #48795, #5584 ) ) ;
#39853=AXIS2_PLACEMENT_3D ( 'NONE', #48486, #59403, #58659 ) ;
#39856=DIRECTION ( 'NONE',  ( -1.000000000000000000, 0.000000000000000000, -0.000000000000000000 ) ) ;
#39859=ORIENTED_EDGE ( 'NONE', *, *, #31480, .F. ) ;
#39864=VECTOR ( 'NONE', #2391, 1000.000000000000000 ) ;
#39888=EDGE_CURVE ( 'NONE', #55524, #11001, #7218, .T. ) ;
#39892=ADVANCED_FACE ( 'NONE', ( #25605 ), #48543, .T. ) ;
#39893=ORIENTED_EDGE ( 'NONE', *, *, #14231, .T. ) ;
#39896=EDGE_LOOP ( 'NONE', ( #5019, #62516, #31078, #37570 ) ) ;
#39906=VECTOR ( 'NONE', #63874, 1000.000000000000000 ) ;
#39907=EDGE_CURVE ( 'NONE', #68386, #15222, #67692, .T. ) ;
#39908=CARTESIAN_POINT ( 'NONE',  ( 6.000000000000000000, -10.30890764327323161, -81.34940948281348483 ) ) ;
#39916=ADVANCED_FACE ( 'NONE', ( #66584 ), #27077, .T. ) ;
#39934=CARTESIAN_POINT ( 'NONE',  ( 0.000000000000000000, 36.73666225445894185, 65.58780272294090707 ) ) ;
#39940=DIRECTION ( 'NONE',  ( 0.000000000000000000, -0.9510565162951566398, 0.3090169943749381809 ) ) ;
#39941=ORIENTED_EDGE ( 'NONE', *, *, #44736, .T. ) ;
#39949=DIRECTION ( 'NONE',  ( -1.000000000000000000, -0.000000000000000000, 0.000000000000000000 ) ) ;
#39952=CARTESIAN_POINT ( 'NONE',  ( 11.99999999999999822, -58.39081064771713869, -50.95692526931392052 ) ) ;
#39958=DIRECTION ( 'NONE',  ( -0.000000000000000000, -0.3090169943749450088, 0.9510565162951543083 ) ) ;
#39960=EDGE_LOOP ( 'NONE', ( #36404, #39311, #69479, #31169 ) ) ;
#39962=VECTOR ( 'NONE', #36463, 1000.000000000000000 ) ;
#39963=VERTEX_POINT ( 'NONE', #10168 ) ;
#39965=CIRCLE ( 'NONE', #7548, 31.99999999999999289 ) ;
#39970=EDGE_CURVE ( 'NONE', #52585, #65473, #1044, .T. ) ;
#39972=FACE_OUTER_BOUND ( 'NONE', #5471, .T. ) ;
#39987=EDGE_CURVE ( 'NONE', #58109, #73300, #39442, .T. ) ;
#39996=FACE_OUTER_BOUND ( 'NONE', #29508, .T. ) ;
#39997=DIRECTION ( 'NONE',  ( 0.000000000000000000, 0.000000000000000000, 1.000000000000000000 ) ) ;
#40014=EDGE_CURVE ( 'NONE', #71829, #27433, #50192, .T. ) ;
#40015=VECTOR ( 'NONE', #9112, 1000.000000000000000 ) ;
#40019=DIRECTION ( 'NONE',  ( 0.000000000000000000, 0.000000000000000000, -1.000000000000000000 ) ) ;
#40022=CIRCLE ( 'NONE', #13591, 82.00000000000000000 ) ;
#40024=CIRCLE ( 'NONE', #3972, 31.99999999999999645 ) ;
#40031=ORIENTED_EDGE ( 'NONE', *, *, #31482, .T. ) ;
#40032=LINE ( 'NONE', #68233, #69423 ) ;
#40037=VERTEX_POINT ( 'NONE', #60579 ) ;
#40043=EDGE_LOOP ( 'NONE', ( #73699, #20417, #42358, #10223 ) ) ;
#40047=CIRCLE ( 'NONE', #44894, 31.99999999999998224 ) ;
#40048=CARTESIAN_POINT ( 'NONE',  ( 0.000000000000000000, -20.41045688087772092, -72.35160999960838524 ) ) ;
#40053=DIRECTION ( 'NONE',  ( -1.000000000000000000, 0.000000000000000000, 0.000000000000000000 ) ) ;
#40059=ORIENTED_EDGE ( 'NONE', *, *, #71691, .T. ) ;
#40063=ORIENTED_EDGE ( 'NONE', *, *, #71858, .F. ) ;
#40065=AXIS2_PLACEMENT_3D ( 'NONE', #29173, #660, #7373 ) ;
#40071=VERTEX_POINT ( 'NONE', #20337 ) ;
#40077=VERTEX_POINT ( 'NONE', #66221 ) ;
#40079=DIRECTION ( 'NONE',  ( -1.000000000000000000, -0.000000000000000000, -0.000000000000000000 ) ) ;
#40084=ORIENTED_EDGE ( 'NONE', *, *, #38215, .T. ) ;
#40085=EDGE_CURVE ( 'NONE', #25988, #23772, #11823, .T. ) ;
#40089=FACE_OUTER_BOUND ( 'NONE', #51218, .T. ) ;
#40099=CARTESIAN_POINT ( 'NONE',  ( 11.99999999999999822, 70.53064760720278059, 26.01480285779964774 ) ) ;
#40107=FACE_OUTER_BOUND ( 'NONE', #11163, .T. ) ;
#40110=CARTESIAN_POINT ( 'NONE',  ( 11.99999999999999822, -2.956366410620109519, -75.11725578898472122 ) ) ;
#40111=ORIENTED_EDGE ( 'NONE', *, *, #10296, .F. ) ;
#40113=CARTESIAN_POINT ( 'NONE',  ( 0.000000000000000000, 22.90783923731629201, 78.73519480814962890 ) ) ;
#40114=VECTOR ( 'NONE', #41858, 1000.000000000000000 ) ;
#40116=DIRECTION ( 'NONE',  ( 0.000000000000000000, 0.000000000000000000, 1.000000000000000000 ) ) ;
#40126=DIRECTION ( 'NONE',  ( 0.000000000000000000, 0.000000000000000000, 1.000000000000000000 ) ) ;
#40130=VECTOR ( 'NONE', #3186, 1000.000000000000000 ) ;
#40133=ORIENTED_EDGE ( 'NONE', *, *, #26712, .T. ) ;
#40134=ORIENTED_EDGE ( 'NONE', *, *, #58068, .T. ) ;
#40136=ADVANCED_FACE ( 'NONE', ( #11639 ), #45138, .T. ) ;
#40139=ADVANCED_FACE ( 'NONE', ( #68060 ), #28561, .T. ) ;
#40160=ORIENTED_EDGE ( 'NONE', *, *, #71758, .F. ) ;
#40164=ORIENTED_EDGE ( 'NONE', *, *, #36812, .T. ) ;
#40166=FACE_BOUND ( 'NONE', #24395, .T. ) ;
#40175=CARTESIAN_POINT ( 'NONE',  ( 0.000000000000000000, -17.28742895386137590, 75.54627589209937355 ) ) ;
#40180=DIRECTION ( 'NONE',  ( 1.000000000000000000, 0.000000000000000000, 0.000000000000000000 ) ) ;
#40189=DIRECTION ( 'NONE',  ( 0.000000000000000000, -6.938893903907231533E-15, 1.000000000000000000 ) ) ;
#40191=DIRECTION ( 'NONE',  ( -1.000000000000000000, 0.000000000000000000, 0.000000000000000000 ) ) ;
#40198=CARTESIAN_POINT ( 'NONE',  ( 6.000000000000000000, -8.966570791701288456, 81.50828551894223040 ) ) ;
#40201=DIRECTION ( 'NONE',  ( 0.000000000000000000, 0.9238795325112851842, 0.3826834323650938896 ) ) ;
#40209=EDGE_LOOP ( 'NONE', ( #51056, #34792, #58351, #43638 ) ) ;
#40210=ORIENTED_EDGE ( 'NONE', *, *, #70662, .F. ) ;
#40212=ORIENTED_EDGE ( 'NONE', *, *, #66552, .F. ) ;
#40216=CIRCLE ( 'NONE', #7802, 31.99999999999998579 ) ;
#40222=EDGE_LOOP ( 'NONE', ( #313, #35398, #63201, #3374 ) ) ;
#40245=ORIENTED_EDGE ( 'NONE', *, *, #26808, .F. ) ;
#40257=DIRECTION ( 'NONE',  ( 0.000000000000000000, 0.8910065241883690090, -0.4539904997395446395 ) ) ;
#40258=CARTESIAN_POINT ( 'NONE',  ( 15.00000000000000000, 16.61724383029390140, 20.69703378468902955 ) ) ;
#40263=EDGE_CURVE ( 'NONE', #3810, #11463, #70626, .T. ) ;
#40270=CARTESIAN_POINT ( 'NONE',  ( 11.99999999999999822, 12.93880638057426502, -76.41127070299258150 ) ) ;
#40271=DIRECTION ( 'NONE',  ( 0.000000000000000000, 0.000000000000000000, -1.000000000000000000 ) ) ;
#40273=VERTEX_POINT ( 'NONE', #59006 ) ;
#40274=CIRCLE ( 'NONE', #61912, 31.99999999999998934 ) ;
#40284=DIRECTION ( 'NONE',  ( -1.000000000000000000, -0.000000000000000000, 0.000000000000000000 ) ) ;
#40288=CIRCLE ( 'NONE', #34268, 82.00000000000000000 ) ;
#40293=CARTESIAN_POINT ( 'NONE',  ( 0.000000000000000000, -8.840884882374576037, -74.65374052328658649 ) ) ;
#40294=ORIENTED_EDGE ( 'NONE', *, *, #58049, .F. ) ;
#40308=ORIENTED_EDGE ( 'NONE', *, *, #26485, .F. ) ;
#40310=LINE ( 'NONE', #57616, #34544 ) ;
#40316=ORIENTED_EDGE ( 'NONE', *, *, #15418, .F. ) ;
#40318=ADVANCED_FACE ( 'NONE', ( #71001 ), #52993, .T. ) ;
#40331=DIRECTION ( 'NONE',  ( 0.000000000000000000, -0.2079116908177641998, -0.9781476007338046896 ) ) ;
#40332=CIRCLE ( 'NONE', #7915, 77.49900000000000944 ) ;
#40333=DIRECTION ( 'NONE',  ( -1.000000000000000000, 0.000000000000000000, 0.000000000000000000 ) ) ;
#40334=DIRECTION ( 'NONE',  ( -1.000000000000000000, 0.000000000000000000, 0.000000000000000000 ) ) ;
#40352=DIRECTION ( 'NONE',  ( -1.000000000000000000, 0.000000000000000000, 0.000000000000000000 ) ) ;
#40353=ORIENTED_EDGE ( 'NONE', *, *, #33361, .F. ) ;
#40385=EDGE_CURVE ( 'NONE', #5496, #25706, #17847, .T. ) ;
#40386=CIRCLE ( 'NONE', #39165, 77.49900000000000944 ) ;
#40387=DIRECTION ( 'NONE',  ( 0.000000000000000000, 0.000000000000000000, 1.000000000000000000 ) ) ;
#40408=CARTESIAN_POINT ( 'NONE',  ( 11.99999999999999822, -39.78640506895651896, 66.50666863321988842 ) ) ;
#40412=DIRECTION ( 'NONE',  ( 0.000000000000000000, 0.000000000000000000, -1.000000000000000000 ) ) ;
#40426=ORIENTED_EDGE ( 'NONE', *, *, #48564, .F. ) ;
#40431=DIRECTION ( 'NONE',  ( 0.000000000000000000, 0.000000000000000000, 1.000000000000000000 ) ) ;
#40440=ORIENTED_EDGE ( 'NONE', *, *, #13986, .F. ) ;
#40443=CARTESIAN_POINT ( 'NONE',  ( 11.99999999999999822, 75.11764819372149304, 29.05362095685338275 ) ) ;
#40444=VECTOR ( 'NONE', #40551, 1000.000000000000000 ) ;
#40460=CARTESIAN_POINT ( 'NONE',  ( 15.00000000000000000, 26.49999999999999645, 1.499999999999995781 ) ) ;
#40464=CARTESIAN_POINT ( 'NONE',  ( 15.00000000000000000, 16.61724383029361718, -20.69703378468926402 ) ) ;
#40467=EDGE_CURVE ( 'NONE', #58013, #11414, #25888, .T. ) ;
#40471=LINE ( 'NONE', #63065, #5074 ) ;
#40474=CARTESIAN_POINT ( 'NONE',  ( 0.000000000000000000, -51.02545421589363883, 55.20638768913742922 ) ) ;
#40478=AXIS2_PLACEMENT_3D ( 'NONE', #55661, #26347, #54919 ) ;
#40479=EDGE_CURVE ( 'NONE', #69052, #59737, #50259, .T. ) ;
#40480=LINE ( 'NONE', #23938, #62200 ) ;
#40489=VECTOR ( 'NONE', #40284, 1000.000000000000000 ) ;
#40491=CYLINDRICAL_SURFACE ( 'NONE', #31662, 31.99999999999998579 ) ;
#40513=EDGE_CURVE ( 'NONE', #28422, #68067, #33452, .T. ) ;
#40518=ORIENTED_EDGE ( 'NONE', *, *, #24759, .T. ) ;
#40524=CARTESIAN_POINT ( 'NONE',  ( 11.99999999999999822, 73.72996012237440766, 14.67089635893739619 ) ) ;
#40528=DIRECTION ( 'NONE',  ( -1.000000000000000000, 0.000000000000000000, -0.000000000000000000 ) ) ;
#40530=CARTESIAN_POINT ( 'NONE',  ( 11.99999999999999822, -29.01471420065506379, -76.69515212746047439 ) ) ;
#40534=EDGE_LOOP ( 'NONE', ( #49371, #51514, #30049, #73397 ) ) ;
#40540=AXIS2_PLACEMENT_3D ( 'NONE', #22053, #16417, #11504 ) ;
#40542=CARTESIAN_POINT ( 'NONE',  ( 0.000000000000000000, 20.41045688087824317, 72.35160999960824313 ) ) ;
#40543=CIRCLE ( 'NONE', #54969, 77.49899999999999523 ) ;
#40549=CARTESIAN_POINT ( 'NONE',  ( 11.99999999999999822, -68.27212725128298132, 31.46837873494953541 ) ) ;
#40551=DIRECTION ( 'NONE',  ( -1.000000000000000000, 0.000000000000000000, 0.000000000000000000 ) ) ;
#40553=DIRECTION ( 'NONE',  ( 0.000000000000000000, 0.000000000000000000, -1.000000000000000000 ) ) ;
#40558=FACE_OUTER_BOUND ( 'NONE', #5594, .T. ) ;
#40559=DIRECTION ( 'NONE',  ( 0.000000000000000000, 0.000000000000000000, 1.000000000000000000 ) ) ;
#40571=SURFACE_STYLE_FILL_AREA ( #2527 ) ;
#40579=ORIENTED_EDGE ( 'NONE', *, *, #15510, .T. ) ;
#40583=VECTOR ( 'NONE', #56320, 1000.000000000000000 ) ;
#40599=VECTOR ( 'NONE', #38435, 1000.000000000000114 ) ;
#40606=ORIENTED_EDGE ( 'NONE', *, *, #6039, .T. ) ;
#40611=VERTEX_POINT ( 'NONE', #57435 ) ;
#40612=DIRECTION ( 'NONE',  ( 0.000000000000000000, 0.000000000000000000, 1.000000000000000000 ) ) ;
#40613=DIRECTION ( 'NONE',  ( 0.000000000000000000, 0.000000000000000000, 1.000000000000000000 ) ) ;
#40618=ORIENTED_EDGE ( 'NONE', *, *, #59641, .T. ) ;
#40620=FACE_OUTER_BOUND ( 'NONE', #7144, .T. ) ;
#40627=VERTEX_POINT ( 'NONE', #51791 ) ;
#40642=DIRECTION ( 'NONE',  ( 1.000000000000000000, 0.000000000000000000, 0.000000000000000000 ) ) ;
#40647=CIRCLE ( 'NONE', #8211, 82.00000000000000000 ) ;
#40650=LINE ( 'NONE', #63599, #61066 ) ;
#40664=DIRECTION ( 'NONE',  ( 0.000000000000000000, 0.9781476007338043566, -0.2079116908177651712 ) ) ;
#40670=EDGE_CURVE ( 'NONE', #66432, #33851, #22109, .T. ) ;
#40674=CYLINDRICAL_SURFACE ( 'NONE', #9111, 31.99999999999998579 ) ;
#40679=DIRECTION ( 'NONE',  ( -1.000000000000000000, 0.000000000000000000, 0.000000000000000000 ) ) ;
#40684=ORIENTED_EDGE ( 'NONE', *, *, #63071, .T. ) ;
#40689=ORIENTED_EDGE ( 'NONE', *, *, #35169, .F. ) ;
#40690=EDGE_LOOP ( 'NONE', ( #46480, #26877, #42199, #72638 ) ) ;
#40698=ORIENTED_EDGE ( 'NONE', *, *, #68139, .T. ) ;
#40705=AXIS2_PLACEMENT_3D ( 'NONE', #67645, #43976, #54873 ) ;
#40710=CARTESIAN_POINT ( 'NONE',  ( 0.000000000000000000, 0.000000000000000000, 0.000000000000000000 ) ) ;
#40718=CARTESIAN_POINT ( 'NONE',  ( 11.99999999999999822, -66.50666863322028632, 39.78640506895582973 ) ) ;
#40721=AXIS2_PLACEMENT_3D ( 'NONE', #14728, #3475, #9458 ) ;
#40728=AXIS2_PLACEMENT_3D ( 'NONE', #49256, #60558, #72180 ) ;
#40731=AXIS2_PLACEMENT_3D ( 'NONE', #49910, #20614, #61956 ) ;
#40732=AXIS2_PLACEMENT_3D ( 'NONE', #63148, #16909, #68785 ) ;
#40741=ORIENTED_EDGE ( 'NONE', *, *, #19427, .T. ) ;
#40743=ADVANCED_FACE ( 'NONE', ( #23967 ), #29956, .T. ) ;
#40744=CARTESIAN_POINT ( 'NONE',  ( 11.99999999999999822, 16.65972982744933972, 80.28980883073764119 ) ) ;
#40745=ADVANCED_FACE ( 'NONE', ( #19048 ), #53640, .T. ) ;
#40747=CARTESIAN_POINT ( 'NONE',  ( 11.99999999999999822, 28.89263327155849126, -71.91182617369157981 ) ) ;
#40753=DIRECTION ( 'NONE',  ( -1.000000000000000000, 0.000000000000000000, 0.000000000000000000 ) ) ;
#40759=DIRECTION ( 'NONE',  ( 0.000000000000000000, 0.9876883405951383255, -0.1564344650402276216 ) ) ;
#40765=AXIS2_PLACEMENT_3D ( 'NONE', #43178, #31494, #8195 ) ;
#40768=EDGE_CURVE ( 'NONE', #33637, #16056, #53654, .T. ) ;
#40774=VERTEX_POINT ( 'NONE', #29590 ) ;
#40776=FACE_OUTER_BOUND ( 'NONE', #4281, .T. ) ;
#40781=VERTEX_POINT ( 'NONE', #19800 ) ;
#40783=CIRCLE ( 'NONE', #62421, 31.99999999999998934 ) ;
#40785=AXIS2_PLACEMENT_3D ( 'NONE', #11991, #34932, #57865 ) ;
#40787=ORIENTED_EDGE ( 'NONE', *, *, #45187, .F. ) ;
#40792=VERTEX_POINT ( 'NONE', #47284 ) ;
#40793=EDGE_LOOP ( 'NONE', ( #27679, #38398, #17681, #49852 ) ) ;
#40796=ORIENTED_EDGE ( 'NONE', *, *, #903, .T. ) ;
#40802=DIRECTION ( 'NONE',  ( 1.000000000000000000, 0.000000000000000000, -0.000000000000000000 ) ) ;
#40806=EDGE_LOOP ( 'NONE', ( #63126, #34287, #48298, #29130 ) ) ;
#40821=DIRECTION ( 'NONE',  ( 0.000000000000000000, 0.3090169943749479509, -0.9510565162951534202 ) ) ;
#40824=AXIS2_PLACEMENT_3D ( 'NONE', #70799, #47873, #2436 ) ;
#40829=CARTESIAN_POINT ( 'NONE',  ( 11.99999999999999822, -65.58780272294100655, 36.73666225445870737 ) ) ;
#40832=ORIENTED_EDGE ( 'NONE', *, *, #34809, .T. ) ;
#40836=VECTOR ( 'NONE', #22064, 1000.000000000000000 ) ;
#40840=DIRECTION ( 'NONE',  ( 0.000000000000000000, 0.000000000000000000, 1.000000000000000000 ) ) ;
#40843=DIRECTION ( 'NONE',  ( -1.000000000000000000, 0.000000000000000000, 0.000000000000000000 ) ) ;
#40846=AXIS2_PLACEMENT_3D ( 'NONE', #38004, #48179, #20339 ) ;
#40850=EDGE_CURVE ( 'NONE', #36873, #45393, #66431, .T. ) ;
#40853=DIRECTION ( 'NONE',  ( 0.000000000000000000, 0.9945218953682732899, -0.1045284632676548031 ) ) ;
#40859=ADVANCED_FACE ( 'NONE', ( #67159 ), #44233, .T. ) ;
#40862=ORIENTED_EDGE ( 'NONE', *, *, #21755, .T. ) ;
#40868=AXIS2_PLACEMENT_3D ( 'NONE', #36832, #47746, #60165 ) ;
#40869=ORIENTED_EDGE ( 'NONE', *, *, #20979, .F. ) ;
#40879=ORIENTED_EDGE ( 'NONE', *, *, #11630, .F. ) ;
#40885=DIRECTION ( 'NONE',  ( 0.000000000000000000, 0.000000000000000000, 1.000000000000000000 ) ) ;
#40890=VERTEX_POINT ( 'NONE', #55511 ) ;
#40901=FACE_OUTER_BOUND ( 'NONE', #35238, .T. ) ;
#40913=ORIENTED_EDGE ( 'NONE', *, *, #44292, .F. ) ;
#40916=ORIENTED_EDGE ( 'NONE', *, *, #5448, .F. ) ;
#40923=EDGE_CURVE ( 'NONE', #11059, #69197, #7117, .T. ) ;
#40931=DIRECTION ( 'NONE',  ( -1.000000000000000000, -0.000000000000000000, -0.000000000000000000 ) ) ;
#40933=CARTESIAN_POINT ( 'NONE',  ( 12.00000000000000000, 23.49999999999999645, 1.499999999999995337 ) ) ;
#40939=AXIS2_PLACEMENT_3D ( 'NONE', #23353, #6074, #51164 ) ;
#40943=CARTESIAN_POINT ( 'NONE',  ( 0.000000000000000000, 0.000000000000000000, 0.000000000000000000 ) ) ;
#40946=CYLINDRICAL_SURFACE ( 'NONE', #27631, 31.99999999999998579 ) ;
#40947=ADVANCED_FACE ( 'NONE', ( #32563 ), #66785, .T. ) ;
#40948=EDGE_CURVE ( 'NONE', #58541, #53812, #55132, .T. ) ;
#40950=CARTESIAN_POINT ( 'NONE',  ( 15.00000000000000000, -3.948201729842355068, -23.21447184625292692 ) ) ;
#40954=FACE_OUTER_BOUND ( 'NONE', #70543, .T. ) ;
#40960=CYLINDRICAL_SURFACE ( 'NONE', #71621, 31.99999999999997868 ) ;
#40964=VERTEX_POINT ( 'NONE', #60064 ) ;
#40974=CYLINDRICAL_SURFACE ( 'NONE', #73739, 82.00000000000000000 ) ;
#40982=VERTEX_POINT ( 'NONE', #8541 ) ;
#40983=ORIENTED_EDGE ( 'NONE', *, *, #17233, .F. ) ;
#40992=DIRECTION ( 'NONE',  ( 0.000000000000000000, 0.5224985647159500202, -0.8526401643540915121 ) ) ;
#40997=DIRECTION ( 'NONE',  ( 0.000000000000000000, 0.9876883405951383255, -0.1564344650402277048 ) ) ;
#40998=AXIS2_PLACEMENT_3D ( 'NONE', #39366, #74309, #39743 ) ;
#40999=EDGE_CURVE ( 'NONE', #63075, #61291, #20379, .T. ) ;
#41008=CARTESIAN_POINT ( 'NONE',  ( 11.99999999999999822, -33.71516098798685590, -74.74816331893465815 ) ) ;
#41022=EDGE_CURVE ( 'NONE', #28741, #64000, #52088, .T. ) ;
#41028=VECTOR ( 'NONE', #25838, 1000.000000000000000 ) ;
#41037=VECTOR ( 'NONE', #62651, 1000.000000000000000 ) ;
#41038=DIRECTION ( 'NONE',  ( -1.000000000000000000, 0.000000000000000000, -0.000000000000000000 ) ) ;
#41044=CARTESIAN_POINT ( 'NONE',  ( 11.99999999999999822, -63.18004540533059554, 44.88180994100355292 ) ) ;
#41045=CIRCLE ( 'NONE', #23078, 77.49900000000000944 ) ;
#41047=ORIENTED_EDGE ( 'NONE', *, *, #65305, .F. ) ;
#41048=CARTESIAN_POINT ( 'NONE',  ( 0.000000000000000000, -77.19088730480527261, 6.903761155837504049 ) ) ;
#41049=DIRECTION ( 'NONE',  ( -1.000000000000000000, 0.000000000000000000, -0.000000000000000000 ) ) ;
#41050=ORIENTED_EDGE ( 'NONE', *, *, #47043, .T. ) ;
#41059=EDGE_LOOP ( 'NONE', ( #69090, #12763, #47899, #9646 ) ) ;
#41061=DIRECTION ( 'NONE',  ( -1.000000000000000000, 0.000000000000000000, 0.000000000000000000 ) ) ;
#41062=ORIENTED_EDGE ( 'NONE', *, *, #1387, .T. ) ;
#41068=ORIENTED_EDGE ( 'NONE', *, *, #60288, .T. ) ;
#41075=ORIENTED_EDGE ( 'NONE', *, *, #5186, .F. ) ;
#41079=EDGE_CURVE ( 'NONE', #20786, #17939, #69588, .T. ) ;
#41081=CARTESIAN_POINT ( 'NONE',  ( 0.000000000000000000, -62.50884508063453637, 41.76106447765467777 ) ) ;
#41082=DIRECTION ( 'NONE',  ( 0.000000000000000000, 0.8526401643540897357, 0.5224985647159527957 ) ) ;
#41083=CARTESIAN_POINT ( 'NONE',  ( 0.000000000000000000, 62.20884554314085335, -46.21855187248562657 ) ) ;
#41094=DIRECTION ( 'NONE',  ( 0.000000000000000000, 0.8090169943749433434, -0.5877852522924786882 ) ) ;
#41106=ORIENTED_EDGE ( 'NONE', *, *, #42762, .T. ) ;
#41114=EDGE_LOOP ( 'NONE', ( #14400, #32278, #37257, #19121 ) ) ;
#41119=DIRECTION ( 'NONE',  ( -1.000000000000000000, -0.000000000000000000, -0.000000000000000000 ) ) ;
#41125=CARTESIAN_POINT ( 'NONE',  ( 15.00000000000000000, 14.60985201121729737, 18.46759930825687235 ) ) ;
#41138=ORIENTED_EDGE ( 'NONE', *, *, #31884, .T. ) ;
#41139=AXIS2_PLACEMENT_3D ( 'NONE', #21194, #10672, #39626 ) ;
#41181=DIRECTION ( 'NONE',  ( -1.000000000000000000, -0.000000000000000000, 0.000000000000000000 ) ) ;
#41182=DIRECTION ( 'NONE',  ( 1.000000000000000000, -0.000000000000000000, 0.000000000000000000 ) ) ;
#41189=ORIENTED_EDGE ( 'NONE', *, *, #68620, .F. ) ;
#41193=DIRECTION ( 'NONE',  ( 0.000000000000000000, 0.000000000000000000, 1.000000000000000000 ) ) ;
#41199=AXIS2_PLACEMENT_3D ( 'NONE', #48404, #71317, #31479 ) ;
#41203=DIRECTION ( 'NONE',  ( -1.000000000000000000, 0.000000000000000000, 0.000000000000000000 ) ) ;
#41204=DIRECTION ( 'NONE',  ( -1.000000000000000000, 0.000000000000000000, 0.000000000000000000 ) ) ;
#41205=FACE_OUTER_BOUND ( 'NONE', #40793, .T. ) ;
#41214=CARTESIAN_POINT ( 'NONE',  ( 0.000000000000000000, 51.02545421589402252, -55.20638768913705263 ) ) ;
#41225=ORIENTED_EDGE ( 'NONE', *, *, #34961, .F. ) ;
#41235=AXIS2_PLACEMENT_3D ( 'NONE', #31575, #1949, #31210 ) ;
#41242=ORIENTED_EDGE ( 'NONE', *, *, #20726, .F. ) ;
#41249=EDGE_CURVE ( 'NONE', #55642, #47807, #60003, .T. ) ;
#41264=DIRECTION ( 'NONE',  ( 0.000000000000000000, 0.000000000000000000, 1.000000000000000000 ) ) ;
#41269=VERTEX_POINT ( 'NONE', #41922 ) ;
#41270=DIRECTION ( 'NONE',  ( -1.000000000000000000, -0.000000000000000000, -0.000000000000000000 ) ) ;
#41273=ORIENTED_EDGE ( 'NONE', *, *, #42346, .T. ) ;
#41275=ADVANCED_FACE ( 'NONE', ( #18609 ), #69378, .T. ) ;
#41278=AXIS2_PLACEMENT_3D ( 'NONE', #70730, #19235, #12849 ) ;
#41280=ORIENTED_EDGE ( 'NONE', *, *, #32237, .F. ) ;
#41283=LINE ( 'NONE', #54408, #69343 ) ;
#41291=DIRECTION ( 'NONE',  ( -1.000000000000000000, 0.000000000000000000, -0.000000000000000000 ) ) ;
#41298=CIRCLE ( 'NONE', #23275, 77.49900000000000944 ) ;
#41299=AXIS2_PLACEMENT_3D ( 'NONE', #25021, #70880, #55450 ) ;
#41303=AXIS2_PLACEMENT_3D ( 'NONE', #54880, #61274, #26305 ) ;
#41304=CARTESIAN_POINT ( 'NONE',  ( 12.00000000000000000, 8.688484142253932063, -21.88630264137371384 ) ) ;
#41306=ORIENTED_EDGE ( 'NONE', *, *, #19104, .T. ) ;
#41307=FACE_OUTER_BOUND ( 'NONE', #26731, .T. ) ;
#41312=CARTESIAN_POINT ( 'NONE',  ( 6.000000000000000000, 80.28980883073758434, 16.65972982744962749 ) ) ;
#41319=VERTEX_POINT ( 'NONE', #18971 ) ;
#41320=CIRCLE ( 'NONE', #18505, 31.99999999999998934 ) ;
#41326=EDGE_CURVE ( 'NONE', #49856, #60856, #64862, .T. ) ;
#41330=ORIENTED_EDGE ( 'NONE', *, *, #22162, .T. ) ;
#41334=EDGE_LOOP ( 'NONE', ( #19524, #50485, #8675, #38595 ) ) ;
#41343=ORIENTED_EDGE ( 'NONE', *, *, #37262, .T. ) ;
#41350=EDGE_LOOP ( 'NONE', ( #45151, #15440, #73170, #45058 ) ) ;
#41352=AXIS2_PLACEMENT_3D ( 'NONE', #34746, #21600, #46036 ) ;
#41355=VERTEX_POINT ( 'NONE', #15567 ) ;
#41359=CIRCLE ( 'NONE', #14947, 82.00000000000000000 ) ;
#41370=EDGE_CURVE ( 'NONE', #20120, #45152, #49183, .T. ) ;
#41378=CARTESIAN_POINT ( 'NONE',  ( 0.000000000000000000, 17.28742895386084655, 75.54627589209950145 ) ) ;
#41384=CARTESIAN_POINT ( 'NONE',  ( 11.99999999999999822, 74.65374052328660071, -8.840884882374309583 ) ) ;
#41403=DIRECTION ( 'NONE',  ( 0.000000000000000000, 0.000000000000000000, -1.000000000000000000 ) ) ;
#41412=AXIS2_PLACEMENT_3D ( 'NONE', #18968, #12599, #58843 ) ;
#41425=EDGE_LOOP ( 'NONE', ( #13267, #5316, #18704, #54443 ) ) ;
#41431=ORIENTED_EDGE ( 'NONE', *, *, #53659, .F. ) ;
#41436=DIRECTION ( 'NONE',  ( -1.000000000000000000, 0.000000000000000000, 0.000000000000000000 ) ) ;
#41438=DIRECTION ( 'NONE',  ( -1.000000000000000000, 0.000000000000000000, 0.000000000000000000 ) ) ;
#41445=ORIENTED_EDGE ( 'NONE', *, *, #70782, .F. ) ;
#41451=AXIS2_PLACEMENT_3D ( 'NONE', #40829, #12968, #68661 ) ;
#41461=DIRECTION ( 'NONE',  ( -1.000000000000000000, 0.000000000000000000, 0.000000000000000000 ) ) ;
#41464=CIRCLE ( 'NONE', #69056, 82.00000000000000000 ) ;
#41466=CYLINDRICAL_SURFACE ( 'NONE', #33133, 31.99999999999998579 ) ;
#41478=VECTOR ( 'NONE', #35184, 1000.000000000000000 ) ;
#41481=DIRECTION ( 'NONE',  ( 0.000000000000000000, 0.9238795325112878487, -0.3826834323650874503 ) ) ;
#41499=CIRCLE ( 'NONE', #69100, 31.99999999999998934 ) ;
#41501=EDGE_CURVE ( 'NONE', #50412, #13574, #21947, .T. ) ;
#41505=CIRCLE ( 'NONE', #69156, 31.99999999999998579 ) ;
#41509=CARTESIAN_POINT ( 'NONE',  ( 0.000000000000000000, -80.28980883073769803, 16.65972982744905551 ) ) ;
#41511=ADVANCED_FACE ( 'NONE', ( #17055 ), #5423, .T. ) ;
#41513=VERTEX_POINT ( 'NONE', #51251 ) ;
#41520=ORIENTED_EDGE ( 'NONE', *, *, #45546, .T. ) ;
#41521=LINE ( 'NONE', #18581, #1079 ) ;
#41522=EDGE_CURVE ( 'NONE', #49623, #10745, #9471, .T. ) ;
#41528=CARTESIAN_POINT ( 'NONE',  ( 0.000000000000000000, 0.000000000000000000, 0.000000000000000000 ) ) ;
#41529=CARTESIAN_POINT ( 'NONE',  ( 15.00000000000000000, -4.261787119644963262, 26.19803753235780164 ) ) ;
#41530=CARTESIAN_POINT ( 'NONE',  ( 6.000000000000000000, -29.01471420065506379, -76.69515212746047439 ) ) ;
#41544=EDGE_CURVE ( 'NONE', #73707, #39502, #52851, .T. ) ;
#41548=DIRECTION ( 'NONE',  ( -1.000000000000000000, -0.000000000000000000, 0.000000000000000000 ) ) ;
#41552=LINE ( 'NONE', #46460, #43878 ) ;
#41564=AXIS2_PLACEMENT_3D ( 'NONE', #71597, #2121, #60347 ) ;
#41565=DIRECTION ( 'NONE',  ( 0.000000000000000000, -0.2079116908177664480, -0.9781476007338041345 ) ) ;
#41575=CARTESIAN_POINT ( 'NONE',  ( 0.000000000000000000, 44.99326035066149387, -68.55367621811095091 ) ) ;
#41596=FACE_OUTER_BOUND ( 'NONE', #28269, .T. ) ;
#41610=AXIS2_PLACEMENT_3D ( 'NONE', #31774, #26136, #49074 ) ;
#41616=CARTESIAN_POINT ( 'NONE',  ( -10.00000000000000000, 0.000000000000000000, 0.000000000000000000 ) ) ;
#41619=VECTOR ( 'NONE', #28901, 1000.000000000000000 ) ;
#41623=ORIENTED_EDGE ( 'NONE', *, *, #6625, .T. ) ;
#41641=ORIENTED_EDGE ( 'NONE', *, *, #27326, .F. ) ;
#41649=CYLINDRICAL_SURFACE ( 'NONE', #14448, 31.99999999999998579 ) ;
#41655=CARTESIAN_POINT ( 'NONE',  ( 11.99999999999999822, -31.47745569255189224, 68.26794271651249346 ) ) ;
#41657=CIRCLE ( 'NONE', #861, 31.99999999999998579 ) ;
#41658=CARTESIAN_POINT ( 'NONE',  ( 6.000000000000000000, -76.69515212746036070, 29.01471420065536932 ) ) ;
#41661=VECTOR ( 'NONE', #47325, 1000.000000000000000 ) ;
#41667=VECTOR ( 'NONE', #16606, 1000.000000000000000 ) ;
#41676=AXIS2_PLACEMENT_3D ( 'NONE', #73573, #39013, #45029 ) ;
#41682=ORIENTED_EDGE ( 'NONE', *, *, #65799, .T. ) ;
#41703=EDGE_LOOP ( 'NONE', ( #13124, #14201, #2002, #23934 ) ) ;
#41706=AXIS2_PLACEMENT_3D ( 'NONE', #67543, #16034, #20567 ) ;
#41708=AXIS2_PLACEMENT_3D ( 'NONE', #57909, #6410, #797 ) ;
#41711=ORIENTED_EDGE ( 'NONE', *, *, #51159, .T. ) ;
#41713=CARTESIAN_POINT ( 'NONE',  ( 6.000000000000000000, -71.87247863392443037, 39.47590169984818687 ) ) ;
#41716=ORIENTED_EDGE ( 'NONE', *, *, #27209, .T. ) ;
#41718=CARTESIAN_POINT ( 'NONE',  ( 11.99999999999999822, -14.66109333815410487, -73.73191006444587003 ) ) ;
#41720=ORIENTED_EDGE ( 'NONE', *, *, #56827, .F. ) ;
#41721=CARTESIAN_POINT ( 'NONE',  ( 11.99999999999999822, 0.000000000000000000, 0.000000000000000000 ) ) ;
#41722=CARTESIAN_POINT ( 'NONE',  ( 0.000000000000000000, -73.72996012237449293, 14.67089635893687571 ) ) ;
#41724=DIRECTION ( 'NONE',  ( -1.000000000000000000, -0.000000000000000000, -0.000000000000000000 ) ) ;
#41732=CARTESIAN_POINT ( 'NONE',  ( 0.000000000000000000, 50.95692526931414790, -58.39081064771693974 ) ) ;
#41737=DIRECTION ( 'NONE',  ( -1.000000000000000000, -0.000000000000000000, 0.000000000000000000 ) ) ;
#41738=DIRECTION ( 'NONE',  ( -1.000000000000000000, -0.000000000000000000, 0.000000000000000000 ) ) ;
#41746=EDGE_CURVE ( 'NONE', #38802, #51749, #74307, .T. ) ;
#41747=DIRECTION ( 'NONE',  ( 0.000000000000000000, 0.000000000000000000, 1.000000000000000000 ) ) ;
#41751=CYLINDRICAL_SURFACE ( 'NONE', #5258, 82.00000000000000000 ) ;
#41757=VECTOR ( 'NONE', #26983, 1000.000000000000000 ) ;
#41759=DIRECTION ( 'NONE',  ( -1.000000000000000000, -0.000000000000000000, -0.000000000000000000 ) ) ;
#41764=VECTOR ( 'NONE', #39438, 1000.000000000000114 ) ;
#41774=ADVANCED_FACE ( 'NONE', ( #46366 ), #47113, .T. ) ;
#41779=VERTEX_POINT ( 'NONE', #35804 ) ;
#41786=VECTOR ( 'NONE', #29105, 1000.000000000000000 ) ;
#41790=AXIS2_PLACEMENT_3D ( 'NONE', #41844, #36202, #59514 ) ;
#41793=EDGE_LOOP ( 'NONE', ( #52055, #52658, #60144, #32712 ) ) ;
#41795=DIRECTION ( 'NONE',  ( -1.000000000000000000, -0.000000000000000000, 0.000000000000000000 ) ) ;
#41798=VERTEX_POINT ( 'NONE', #18884 ) ;
#41805=LINE ( 'NONE', #36904, #34367 ) ;
#41812=ORIENTED_EDGE ( 'NONE', *, *, #53240, .T. ) ;
#41817=DIRECTION ( 'NONE',  ( -1.000000000000000000, -0.000000000000000000, -0.000000000000000000 ) ) ;
#41826=VERTEX_POINT ( 'NONE', #37678 ) ;
#41830=EDGE_CURVE ( 'NONE', #66208, #46926, #65512, .T. ) ;
#41839=ORIENTED_EDGE ( 'NONE', *, *, #20005, .F. ) ;
#41844=CARTESIAN_POINT ( 'NONE',  ( 11.99999999999999822, -72.35160999960801576, -20.41045688087902121 ) ) ;
#41845=AXIS2_PLACEMENT_3D ( 'NONE', #30867, #31248, #29755 ) ;
#41857=ORIENTED_EDGE ( 'NONE', *, *, #68613, .F. ) ;
#41858=DIRECTION ( 'NONE',  ( -1.000000000000000000, -0.000000000000000000, 0.000000000000000000 ) ) ;
#41863=VERTEX_POINT ( 'NONE', #32013 ) ;
#41871=VECTOR ( 'NONE', #2464, 1000.000000000000000 ) ;
#41873=EDGE_LOOP ( 'NONE', ( #11089, #62432, #19560, #9053 ) ) ;
#41874=VECTOR ( 'NONE', #17368, 1000.000000000000000 ) ;
#41876=LINE ( 'NONE', #12184, #41786 ) ;
#41883=ORIENTED_EDGE ( 'NONE', *, *, #33440, .T. ) ;
#41893=DIRECTION ( 'NONE',  ( 1.000000000000000000, 0.000000000000000000, 0.000000000000000000 ) ) ;
#41895=AXIS2_PLACEMENT_3D ( 'NONE', #14517, #8884, #31801 ) ;
#41904=CARTESIAN_POINT ( 'NONE',  ( 0.000000000000000000, -80.55351364060599906, 15.33399622253457295 ) ) ;
#41905=VECTOR ( 'NONE', #21496, 1000.000000000000000 ) ;
#41908=EDGE_CURVE ( 'NONE', #31821, #4105, #34699, .T. ) ;
#41917=EDGE_CURVE ( 'NONE', #15716, #4389, #21483, .T. ) ;
#41922=CARTESIAN_POINT ( 'NONE',  ( 11.99999999999999822, -68.55367621811110723, -44.99326035066126650 ) ) ;
#41924=ADVANCED_FACE ( 'NONE', ( #15095 ), #31646, .F. ) ;
#41929=DIRECTION ( 'NONE',  ( -1.000000000000000000, -0.000000000000000000, -0.000000000000000000 ) ) ;
#41945=FACE_OUTER_BOUND ( 'NONE', #63187, .T. ) ;
#41946=FACE_OUTER_BOUND ( 'NONE', #53799, .T. ) ;
#41947=CARTESIAN_POINT ( 'NONE',  ( 11.99999999999999822, 77.32052557432841411, 5.256550761633121738 ) ) ;
#41948=CARTESIAN_POINT ( 'NONE',  ( 15.00000000000000000, -10.45096189432344502, -21.10159698893425784 ) ) ;
#41950=DIRECTION ( 'NONE',  ( -1.000000000000000000, 0.000000000000000000, -0.000000000000000000 ) ) ;
#41964=AXIS2_PLACEMENT_3D ( 'NONE', #62144, #44860, #27165 ) ;
#41970=ORIENTED_EDGE ( 'NONE', *, *, #62515, .T. ) ;
#41979=CARTESIAN_POINT ( 'NONE',  ( 0.000000000000000000, -50.23322058963393744, 64.81221759200325039 ) ) ;
#41989=VECTOR ( 'NONE', #60604, 1000.000000000000000 ) ;
#41990=ORIENTED_EDGE ( 'NONE', *, *, #38308, .T. ) ;
#42002=DIRECTION ( 'NONE',  ( -1.000000000000000000, -0.000000000000000000, 0.000000000000000000 ) ) ;
#42007=DIRECTION ( 'NONE',  ( -1.000000000000000000, 0.000000000000000000, 0.000000000000000000 ) ) ;
#42008=VECTOR ( 'NONE', #55516, 1000.000000000000000 ) ;
#42011=DIRECTION ( 'NONE',  ( -1.000000000000000000, 0.000000000000000000, 0.000000000000000000 ) ) ;
#42020=DIRECTION ( 'NONE',  ( 0.000000000000000000, 0.000000000000000000, 1.000000000000000000 ) ) ;
#42021=VECTOR ( 'NONE', #21530, 1000.000000000000000 ) ;
#42023=VECTOR ( 'NONE', #70223, 1000.000000000000000 ) ;
#42032=DIRECTION ( 'NONE',  ( 0.000000000000000000, 0.000000000000000000, 1.000000000000000000 ) ) ;
#42035=DIRECTION ( 'NONE',  ( -1.000000000000000000, 0.000000000000000000, 0.000000000000000000 ) ) ;
#42039=EDGE_CURVE ( 'NONE', #28860, #64494, #27106, .T. ) ;
#42042=CARTESIAN_POINT ( 'NONE',  ( 0.000000000000000000, -70.53064760720336324, 26.01480285779810231 ) ) ;
#42050=EDGE_CURVE ( 'NONE', #52399, #3442, #56338, .T. ) ;
#42056=PLANE ( 'NONE',  #5467 ) ;
#42067=VECTOR ( 'NONE', #36590, 999.9999999999998863 ) ;
#42068=DIRECTION ( 'NONE',  ( 0.000000000000000000, 0.000000000000000000, 1.000000000000000000 ) ) ;
#42069=EDGE_LOOP ( 'NONE', ( #21046, #7887, #54625, #36989 ) ) ;
#42070=CARTESIAN_POINT ( 'NONE',  ( 15.00000000000000000, 24.81905959214260804, -9.408202855044828894 ) ) ;
#42081=VERTEX_POINT ( 'NONE', #45171 ) ;
#42086=DIRECTION ( 'NONE',  ( -1.000000000000000000, -0.000000000000000000, -0.000000000000000000 ) ) ;
#42088=ORIENTED_EDGE ( 'NONE', *, *, #65115, .T. ) ;
#42097=LINE ( 'NONE', #37569, #72871 ) ;
#42100=ORIENTED_EDGE ( 'NONE', *, *, #2418, .F. ) ;
#42103=VECTOR ( 'NONE', #31816, 1000.000000000000000 ) ;
#42107=ADVANCED_FACE ( 'NONE', ( #9282 ), #26196, .T. ) ;
#42111=CARTESIAN_POINT ( 'NONE',  ( 6.000000000000000000, -80.55351364060599906, 15.33399622253457295 ) ) ;
#42112=VERTEX_POINT ( 'NONE', #39352 ) ;
#42115=ADVANCED_FACE ( 'NONE', ( #20933 ), #26939, .T. ) ;
#42125=CARTESIAN_POINT ( 'NONE',  ( -10.00000000000000000, 0.000000000000000000, 0.000000000000000000 ) ) ;
#42129=DIRECTION ( 'NONE',  ( 0.000000000000000000, -0.1564344650402170744, -0.9876883405951399908 ) ) ;
#42135=CARTESIAN_POINT ( 'NONE',  ( 15.00000000000000000, -19.89357724624986545, 12.59942793731086219 ) ) ;
#42141=DIRECTION ( 'NONE',  ( 0.000000000000000000, 0.000000000000000000, 1.000000000000000000 ) ) ;
#42147=CARTESIAN_POINT ( 'NONE',  ( 12.00000000000000000, 9.615535125378768200, -24.73947219025917121 ) ) ;
#42151=AXIS2_PLACEMENT_3D ( 'NONE', #52469, #25011, #41565 ) ;
#42152=VECTOR ( 'NONE', #48292, 1000.000000000000000 ) ;
#42164=VERTEX_POINT ( 'NONE', #32580 ) ;
#42169=AXIS2_PLACEMENT_3D ( 'NONE', #59677, #66070, #14542 ) ;
#42173=EDGE_CURVE ( 'NONE', #24493, #43739, #70685, .T. ) ;
#42176=CYLINDRICAL_SURFACE ( 'NONE', #4111, 82.00000000000000000 ) ;
#42178=ORIENTED_EDGE ( 'NONE', *, *, #1935, .F. ) ;
#42183=VERTEX_POINT ( 'NONE', #33311 ) ;
#42191=DIRECTION ( 'NONE',  ( 0.000000000000000000, -0.3090169943749551673, -0.9510565162951510887 ) ) ;
#42192=DIRECTION ( 'NONE',  ( 0.000000000000000000, 0.000000000000000000, 1.000000000000000000 ) ) ;
#42195=CARTESIAN_POINT ( 'NONE',  ( 11.99999999999999822, 55.19960302592066625, 51.03279382321107249 ) ) ;
#42199=ORIENTED_EDGE ( 'NONE', *, *, #12450, .F. ) ;
#42201=ORIENTED_EDGE ( 'NONE', *, *, #40479, .F. ) ;
#42209=CIRCLE ( 'NONE', #69822, 77.49899999999999523 ) ;
#42214=ORIENTED_EDGE ( 'NONE', *, *, #9019, .F. ) ;
#42215=AXIS2_PLACEMENT_3D ( 'NONE', #36932, #7624, #71502 ) ;
#42216=ORIENTED_EDGE ( 'NONE', *, *, #54992, .F. ) ;
#42231=DIRECTION ( 'NONE',  ( 0.000000000000000000, 0.000000000000000000, 1.000000000000000000 ) ) ;
#42234=CARTESIAN_POINT ( 'NONE',  ( 15.00000000000000000, 8.688484142254226938, 21.88630264137359305 ) ) ;
#42251=DIRECTION ( 'NONE',  ( -1.000000000000000000, 0.000000000000000000, -0.000000000000000000 ) ) ;
#42252=DIRECTION ( 'NONE',  ( -1.000000000000000000, 0.000000000000000000, -0.000000000000000000 ) ) ;
#42254=CARTESIAN_POINT ( 'NONE',  ( 0.000000000000000000, -50.95692526931372157, 58.39081064771733054 ) ) ;
#42261=ORIENTED_EDGE ( 'NONE', *, *, #26477, .T. ) ;
#42262=EDGE_CURVE ( 'NONE', #66486, #54478, #23918, .T. ) ;
#42267=ORIENTED_EDGE ( 'NONE', *, *, #4001, .T. ) ;
#42275=ORIENTED_EDGE ( 'NONE', *, *, #52044, .F. ) ;
#42278=CARTESIAN_POINT ( 'NONE',  ( 11.99999999999999822, 73.73191006444551476, 14.66109333815590254 ) ) ;
#42279=AXIS2_PLACEMENT_3D ( 'NONE', #23350, #51160, #46275 ) ;
#42283=CARTESIAN_POINT ( 'NONE',  ( 0.000000000000000000, 0.000000000000000000, 0.000000000000000000 ) ) ;
#42284=CYLINDRICAL_SURFACE ( 'NONE', #56760, 31.99999999999998579 ) ;
#42287=CARTESIAN_POINT ( 'NONE',  ( 0.000000000000000000, -72.35432306680498016, 20.40083707022857951 ) ) ;
#42290=CARTESIAN_POINT ( 'NONE',  ( 11.99999999999999822, 81.50828551894241514, -8.966570791699814080 ) ) ;
#42295=EDGE_CURVE ( 'NONE', #56438, #40273, #28054, .T. ) ;
#42300=CARTESIAN_POINT ( 'NONE',  ( 11.99999999999999822, 50.23322058963348979, 64.81221759200361987 ) ) ;
#42309=LINE ( 'NONE', #60710, #69935 ) ;
#42311=DIRECTION ( 'NONE',  ( -1.000000000000000000, -0.000000000000000000, -0.000000000000000000 ) ) ;
#42320=DIRECTION ( 'NONE',  ( 0.000000000000000000, 0.000000000000000000, 1.000000000000000000 ) ) ;
#42324=CIRCLE ( 'NONE', #20675, 31.99999999999998579 ) ;
#42325=CIRCLE ( 'NONE', #45929, 77.49899999999999523 ) ;
#42333=CIRCLE ( 'NONE', #67487, 31.99999999999998579 ) ;
#42337=VERTEX_POINT ( 'NONE', #48313 ) ;
#42338=ORIENTED_EDGE ( 'NONE', *, *, #49150, .F. ) ;
#42346=EDGE_CURVE ( 'NONE', #19051, #25675, #19833, .T. ) ;
#42358=ORIENTED_EDGE ( 'NONE', *, *, #11953, .T. ) ;
#42360=CIRCLE ( 'NONE', #5140, 77.49899999999999523 ) ;
#42367=ORIENTED_EDGE ( 'NONE', *, *, #31381, .T. ) ;
#42369=EDGE_CURVE ( 'NONE', #29284, #61762, #70121, .T. ) ;
#42394=ORIENTED_EDGE ( 'NONE', *, *, #42262, .T. ) ;
#42395=CARTESIAN_POINT ( 'NONE',  ( 11.99999999999999822, 75.11725578898472122, -2.956366410619845730 ) ) ;
#42400=LINE ( 'NONE', #19820, #36184 ) ;
#42412=CARTESIAN_POINT ( 'NONE',  ( 0.000000000000000000, -34.94270380257585629, -74.18225833017926618 ) ) ;
#42419=CIRCLE ( 'NONE', #20843, 31.99999999999997868 ) ;
#42427=EDGE_CURVE ( 'NONE', #13981, #58816, #7722, .T. ) ;
#42429=VERTEX_POINT ( 'NONE', #13356 ) ;
#42432=CARTESIAN_POINT ( 'NONE',  ( 0.000000000000000000, 0.000000000000000000, 0.000000000000000000 ) ) ;
#42450=VERTEX_POINT ( 'NONE', #48682 ) ;
#42452=DIRECTION ( 'NONE',  ( 0.000000000000000000, 0.000000000000000000, 1.000000000000000000 ) ) ;
#42468=AXIS2_PLACEMENT_3D ( 'NONE', #54365, #37458, #43099 ) ;
#42475=EDGE_CURVE ( 'NONE', #13138, #15732, #10312, .T. ) ;
#42480=DIRECTION ( 'NONE',  ( -1.000000000000000000, -0.000000000000000000, -0.000000000000000000 ) ) ;
#42489=AXIS2_PLACEMENT_3D ( 'NONE', #55253, #73278, #20670 ) ;
#42496=CARTESIAN_POINT ( 'NONE',  ( -10.00000000000000000, 0.000000000000000000, 0.000000000000000000 ) ) ;
#42501=FACE_OUTER_BOUND ( 'NONE', #21010, .T. ) ;
#42507=DIRECTION ( 'NONE',  ( -1.000000000000000000, -0.000000000000000000, -0.000000000000000000 ) ) ;
#42509=CARTESIAN_POINT ( 'NONE',  ( 0.000000000000000000, 0.000000000000000000, 0.000000000000000000 ) ) ;
#42518=ORIENTED_EDGE ( 'NONE', *, *, #64087, .F. ) ;
#42519=AXIS2_PLACEMENT_3D ( 'NONE', #18756, #58615, #19497 ) ;
#42527=ORIENTED_EDGE ( 'NONE', *, *, #70833, .T. ) ;
#42530=ORIENTED_EDGE ( 'NONE', *, *, #44507, .F. ) ;
#42551=ORIENTED_EDGE ( 'NONE', *, *, #16579, .F. ) ;
#42556=CARTESIAN_POINT ( 'NONE',  ( 11.99999999999999822, 68.55367621811141987, 44.99326035066078333 ) ) ;
#42560=ORIENTED_EDGE ( 'NONE', *, *, #37379, .F. ) ;
#42561=VECTOR ( 'NONE', #58856, 1000.000000000000000 ) ;
#42568=CARTESIAN_POINT ( 'NONE',  ( 6.000000000000000000, -81.50828551894220197, -8.966570791701593990 ) ) ;
#42574=AXIS2_PLACEMENT_3D ( 'NONE', #65745, #70996, #66493 ) ;
#42590=CARTESIAN_POINT ( 'NONE',  ( 0.000000000000000000, 0.000000000000000000, 0.000000000000000000 ) ) ;
#42597=CIRCLE ( 'NONE', #31781, 77.49899999999999523 ) ;
#42602=FACE_OUTER_BOUND ( 'NONE', #56862, .T. ) ;
#42607=CYLINDRICAL_SURFACE ( 'NONE', #67812, 77.49899999999999523 ) ;
#42609=CARTESIAN_POINT ( 'NONE',  ( 11.99999999999999822, 0.000000000000000000, 0.000000000000000000 ) ) ;
#42615=ORIENTED_EDGE ( 'NONE', *, *, #14495, .F. ) ;
#42617=CARTESIAN_POINT ( 'NONE',  ( 11.99999999999999822, 8.830959090343430518, -74.65491531819107252 ) ) ;
#42625=EDGE_CURVE ( 'NONE', #55755, #33844, #38517, .T. ) ;
#42627=ORIENTED_EDGE ( 'NONE', *, *, #11630, .T. ) ;
#42632=AXIS2_PLACEMENT_3D ( 'NONE', #62452, #63191, #40613 ) ;
#42634=EDGE_LOOP ( 'NONE', ( #56410, #3741, #16749, #38184 ) ) ;
#42638=ORIENTED_EDGE ( 'NONE', *, *, #66650, .F. ) ;
#42639=CIRCLE ( 'NONE', #31837, 31.99999999999999289 ) ;
#42655=DIRECTION ( 'NONE',  ( -1.000000000000000000, -0.000000000000000000, -0.000000000000000000 ) ) ;
#42662=CARTESIAN_POINT ( 'NONE',  ( 6.000000000000000000, 29.01471420065673712, -76.69515212745984911 ) ) ;
#42672=VERTEX_POINT ( 'NONE', #11418 ) ;
#42674=DIRECTION ( 'NONE',  ( 1.000000000000000000, 0.000000000000000000, 0.000000000000000000 ) ) ;
#42675=VECTOR ( 'NONE', #47543, 1000.000000000000000 ) ;
#42691=CARTESIAN_POINT ( 'NONE',  ( 0.000000000000000000, 63.97538442413498672, -51.29473840253155004 ) ) ;
#42696=CIRCLE ( 'NONE', #65556, 77.49899999999999523 ) ;
#42700=CARTESIAN_POINT ( 'NONE',  ( 11.99999999999999822, -34.44570377933549565, -69.42325613327476219 ) ) ;
#42705=VERTEX_POINT ( 'NONE', #62964 ) ;
#42706=CARTESIAN_POINT ( 'NONE',  ( 6.000000000000000000, -81.90746397400391743, 3.894527615417579636 ) ) ;
#42708=VERTEX_POINT ( 'NONE', #16326 ) ;
#42713=EDGE_CURVE ( 'NONE', #18663, #34276, #5440, .T. ) ;
#42715=LINE ( 'NONE', #59266, #55654 ) ;
#42717=EDGE_CURVE ( 'NONE', #13516, #44140, #5437, .T. ) ;
#42720=VERTEX_POINT ( 'NONE', #5804 ) ;
#42739=CIRCLE ( 'NONE', #51154, 31.99999999999999289 ) ;
#42743=CARTESIAN_POINT ( 'NONE',  ( 6.000000000000000000, -15.33399622253541317, 80.55351364060584274 ) ) ;
#42746=AXIS2_PLACEMENT_3D ( 'NONE', #49003, #55021, #2820 ) ;
#42751=VECTOR ( 'NONE', #37601, 1000.000000000000000 ) ;
#42756=VECTOR ( 'NONE', #17698, 1000.000000000000000 ) ;
#42762=EDGE_CURVE ( 'NONE', #25706, #55085, #36642, .T. ) ;
#42763=ORIENTED_EDGE ( 'NONE', *, *, #39240, .T. ) ;
#42766=CIRCLE ( 'NONE', #60803, 31.99999999999998579 ) ;
#42769=CARTESIAN_POINT ( 'NONE',  ( 11.99999999999999822, 31.46837873495072913, -68.27212725128242710 ) ) ;
#42770=CARTESIAN_POINT ( 'NONE',  ( 11.99999999999999822, 0.000000000000000000, 0.000000000000000000 ) ) ;
#42772=DIRECTION ( 'NONE',  ( 0.000000000000000000, -0.9723699203976789995, 0.2334453638558957322 ) ) ;
#42784=CARTESIAN_POINT ( 'NONE',  ( 0.000000000000000000, -63.97538442413390669, -51.29473840253292138 ) ) ;
#42785=EDGE_LOOP ( 'NONE', ( #17172, #57454, #49407, #28958 ) ) ;
#42793=VERTEX_POINT ( 'NONE', #52379 ) ;
#42800=CIRCLE ( 'NONE', #10390, 31.99999999999998224 ) ;
#42807=ORIENTED_EDGE ( 'NONE', *, *, #55692, .T. ) ;
#42816=CARTESIAN_POINT ( 'NONE',  ( 0.000000000000000000, 11.30684508768450591, -76.66974797899824523 ) ) ;
#42819=EDGE_LOOP ( 'NONE', ( #46004, #12461, #40913, #6112 ) ) ;
#42823=ORIENTED_EDGE ( 'NONE', *, *, #34732, .F. ) ;
#42829=VERTEX_POINT ( 'NONE', #7272 ) ;
#42835=LINE ( 'NONE', #2656, #24095 ) ;
#42839=DIRECTION ( 'NONE',  ( -1.000000000000000000, 0.000000000000000000, 0.000000000000000000 ) ) ;
#42842=ORIENTED_EDGE ( 'NONE', *, *, #39464, .F. ) ;
#42847=CIRCLE ( 'NONE', #3258, 31.99999999999998579 ) ;
#42851=ADVANCED_FACE ( 'NONE', ( #53129 ), #1305, .T. ) ;
#42861=CARTESIAN_POINT ( 'NONE',  ( 11.99999999999999822, 62.50884508063487033, -41.76106447765422303 ) ) ;
#42870=LINE ( 'NONE', #15392, #22037 ) ;
#42872=EDGE_CURVE ( 'NONE', #34012, #61374, #30552, .T. ) ;
#42878=VECTOR ( 'NONE', #51029, 1000.000000000000000 ) ;
#42886=EDGE_CURVE ( 'NONE', #1170, #1681, #68213, .T. ) ;
#42910=AXIS2_PLACEMENT_3D ( 'NONE', #28714, #33987, #51654 ) ;
#42911=VERTEX_POINT ( 'NONE', #71138 ) ;
#42915=CARTESIAN_POINT ( 'NONE',  ( 11.99999999999999822, -68.27212725128298132, 31.46837873494953541 ) ) ;
#42919=ORIENTED_EDGE ( 'NONE', *, *, #28004, .F. ) ;
#42929=CARTESIAN_POINT ( 'NONE',  ( 15.00000000000000000, 8.688484142253932063, -21.88630264137371029 ) ) ;
#42951=ORIENTED_EDGE ( 'NONE', *, *, #70342, .T. ) ;
#42953=EDGE_CURVE ( 'NONE', #63042, #14951, #70775, .T. ) ;
#42954=EDGE_CURVE ( 'NONE', #55121, #41779, #53762, .T. ) ;
#42956=DIRECTION ( 'NONE',  ( 0.000000000000000000, -0.6494480483301739993, -0.7604059656000390355 ) ) ;
#42963=DIRECTION ( 'NONE',  ( 0.000000000000000000, 0.000000000000000000, 1.000000000000000000 ) ) ;
#42976=DIRECTION ( 'NONE',  ( -1.000000000000000000, -0.000000000000000000, -0.000000000000000000 ) ) ;
#42991=CARTESIAN_POINT ( 'NONE',  ( 15.00000000000000000, -22.67460108101782978, -6.353146135317906840 ) ) ;
#42993=DIRECTION ( 'NONE',  ( 0.000000000000000000, 0.000000000000000000, 1.000000000000000000 ) ) ;
#42998=ORIENTED_EDGE ( 'NONE', *, *, #18076, .T. ) ;
#43001=ORIENTED_EDGE ( 'NONE', *, *, #61234, .F. ) ;
#43011=ORIENTED_EDGE ( 'NONE', *, *, #65355, .T. ) ;
#43012=DIRECTION ( 'NONE',  ( 0.000000000000000000, 0.000000000000000000, -1.000000000000000000 ) ) ;
#43015=DIRECTION ( 'NONE',  ( 0.000000000000000000, -0.5000000000000028866, -0.8660254037844369313 ) ) ;
#43016=AXIS2_PLACEMENT_3D ( 'NONE', #17787, #24187, #11764 ) ;
#43017=CARTESIAN_POINT ( 'NONE',  ( 12.00000000000000000, -14.54903810567644484, 22.19967320028775504 ) ) ;
#43030=CYLINDRICAL_SURFACE ( 'NONE', #50555, 77.49899999999999523 ) ;
#43035=VECTOR ( 'NONE', #33614, 1000.000000000000000 ) ;
#43037=EDGE_CURVE ( 'NONE', #18122, #11167, #9377, .T. ) ;
#43040=ORIENTED_EDGE ( 'NONE', *, *, #73686, .F. ) ;
#43042=ADVANCED_FACE ( 'NONE', ( #48597 ), #66632, .T. ) ;
#43044=VECTOR ( 'NONE', #31447, 1000.000000000000000 ) ;
#43048=DIRECTION ( 'NONE',  ( -1.000000000000000000, -0.000000000000000000, -0.000000000000000000 ) ) ;
#43052=CARTESIAN_POINT ( 'NONE',  ( 11.99999999999999822, 68.26794271651307611, -31.47745569255064169 ) ) ;
#43055=EDGE_CURVE ( 'NONE', #34723, #56976, #43708, .T. ) ;
#43060=CYLINDRICAL_SURFACE ( 'NONE', #34528, 77.49899999999999523 ) ;
#43061=DIRECTION ( 'NONE',  ( 0.000000000000000000, 0.000000000000000000, 1.000000000000000000 ) ) ;
#43074=CARTESIAN_POINT ( 'NONE',  ( 0.000000000000000000, 11.30684508768339569, 76.66974797899841576 ) ) ;
#43076=DIRECTION ( 'NONE',  ( -1.000000000000000000, 0.000000000000000000, 0.000000000000000000 ) ) ;
#43080=ADVANCED_FACE ( 'NONE', ( #20006 ), #32398, .F. ) ;
#43081=AXIS2_PLACEMENT_3D ( 'NONE', #54510, #47752, #35723 ) ;
#43084=ORIENTED_EDGE ( 'NONE', *, *, #15952, .F. ) ;
#43090=VECTOR ( 'NONE', #49558, 1000.000000000000000 ) ;
#43092=CIRCLE ( 'NONE', #74256, 77.49900000000000944 ) ;
#43099=DIRECTION ( 'NONE',  ( 0.000000000000000000, 0.000000000000000000, 1.000000000000000000 ) ) ;
#43101=CARTESIAN_POINT ( 'NONE',  ( 11.99999999999999822, -51.29473840253177741, -63.97538442413483750 ) ) ;
#43109=DIRECTION ( 'NONE',  ( 0.000000000000000000, -0.9969173337331287410, 0.07845909572783495156 ) ) ;
#43110=EDGE_CURVE ( 'NONE', #69197, #39310, #72982, .T. ) ;
#43115=CIRCLE ( 'NONE', #74328, 77.49900000000000944 ) ;
#43122=VECTOR ( 'NONE', #68922, 999.9999999999998863 ) ;
#43123=EDGE_LOOP ( 'NONE', ( #41189, #61754, #69248, #65485 ) ) ;
#43131=ORIENTED_EDGE ( 'NONE', *, *, #18913, .T. ) ;
#43141=CARTESIAN_POINT ( 'NONE',  ( 11.99999999999999822, -34.44570377933647620, 69.42325613327427902 ) ) ;
#43143=ORIENTED_EDGE ( 'NONE', *, *, #67831, .F. ) ;
#43148=AXIS2_PLACEMENT_3D ( 'NONE', #72269, #43724, #20769 ) ;
#43151=VECTOR ( 'NONE', #4847, 1000.000000000000000 ) ;
#43156=FACE_OUTER_BOUND ( 'NONE', #50087, .T. ) ;
#43168=DIRECTION ( 'NONE',  ( -1.000000000000000000, -0.000000000000000000, 0.000000000000000000 ) ) ;
#43172=DIRECTION ( 'NONE',  ( -1.000000000000000000, -0.000000000000000000, -0.000000000000000000 ) ) ;
#43175=AXIS2_PLACEMENT_3D ( 'NONE', #32373, #50409, #62080 ) ;
#43178=CARTESIAN_POINT ( 'NONE',  ( 11.99999999999999822, -65.58780272294048075, -36.73666225445966660 ) ) ;
#43179=AXIS2_PLACEMENT_3D ( 'NONE', #61772, #27914, #38834 ) ;
#43185=ORIENTED_EDGE ( 'NONE', *, *, #29943, .F. ) ;
#43203=CIRCLE ( 'NONE', #10782, 77.49899999999999523 ) ;
#43221=ORIENTED_EDGE ( 'NONE', *, *, #42039, .F. ) ;
#43230=LINE ( 'NONE', #49945, #27551 ) ;
#43231=DIRECTION ( 'NONE',  ( -1.000000000000000000, 0.000000000000000000, 0.000000000000000000 ) ) ;
#43253=DIRECTION ( 'NONE',  ( -1.000000000000000000, 0.000000000000000000, -0.000000000000000000 ) ) ;
#43257=LINE ( 'NONE', #43621, #64070 ) ;
#43261=FACE_OUTER_BOUND ( 'NONE', #36220, .T. ) ;
#43274=EDGE_LOOP ( 'NONE', ( #27587, #72857, #37201, #16441 ) ) ;
#43291=VERTEX_POINT ( 'NONE', #74110 ) ;
#43293=CARTESIAN_POINT ( 'NONE',  ( 0.000000000000000000, -65.59268652807183742, -36.72794159290312166 ) ) ;
#43295=ORIENTED_EDGE ( 'NONE', *, *, #29714, .T. ) ;
#43296=DIRECTION ( 'NONE',  ( -0.000000000000000000, 0.5000000000000038858, 0.8660254037844363761 ) ) ;
#43306=ORIENTED_EDGE ( 'NONE', *, *, #59661, .F. ) ;
#43314=ORIENTED_EDGE ( 'NONE', *, *, #45709, .T. ) ;
#43327=EDGE_CURVE ( 'NONE', #30858, #71384, #23823, .T. ) ;
#43333=EDGE_CURVE ( 'NONE', #59348, #40890, #40650, .T. ) ;
#43344=CARTESIAN_POINT ( 'NONE',  ( 15.00000000000000000, 26.49999999999999645, 1.499999999999995781 ) ) ;
#43348=CIRCLE ( 'NONE', #22946, 77.49899999999999523 ) ;
#43349=DIRECTION ( 'NONE',  ( -1.000000000000000000, 0.000000000000000000, -0.000000000000000000 ) ) ;
#43353=CARTESIAN_POINT ( 'NONE',  ( 6.000000000000000000, -81.90746397400386059, -3.894527615418766242 ) ) ;
#43354=CARTESIAN_POINT ( 'NONE',  ( 0.000000000000000000, 0.000000000000000000, 0.000000000000000000 ) ) ;
#43358=DIRECTION ( 'NONE',  ( -1.000000000000000000, 0.000000000000000000, 0.000000000000000000 ) ) ;
#43363=CARTESIAN_POINT ( 'NONE',  ( 0.000000000000000000, 68.27212725128275395, 31.46837873495001503 ) ) ;
#43364=CARTESIAN_POINT ( 'NONE',  ( 0.000000000000000000, 46.11716303203186840, 67.80270845531904911 ) ) ;
#43366=VECTOR ( 'NONE', #38396, 1000.000000000000000 ) ;
#43367=AXIS2_PLACEMENT_3D ( 'NONE', #59894, #33421, #27795 ) ;
#43370=CARTESIAN_POINT ( 'NONE',  ( 11.99999999999999822, -26.02418014898260878, -70.52718814184285634 ) ) ;
#43373=DIRECTION ( 'NONE',  ( -1.000000000000000000, 0.000000000000000000, 0.000000000000000000 ) ) ;
#43391=DIRECTION ( 'NONE',  ( 0.000000000000000000, -0.8090169943749530024, 0.5877852522924653655 ) ) ;
#43395=AXIS2_PLACEMENT_3D ( 'NONE', #48320, #71232, #19735 ) ;
#43400=ORIENTED_EDGE ( 'NONE', *, *, #6547, .F. ) ;
#43425=EDGE_CURVE ( 'NONE', #68450, #30858, #7909, .T. ) ;
#43430=EDGE_LOOP ( 'NONE', ( #72178, #54721, #35343, #48260 ) ) ;
#43431=CIRCLE ( 'NONE', #3809, 77.49900000000000944 ) ;
#43432=CARTESIAN_POINT ( 'NONE',  ( 11.99999999999999822, 0.000000000000000000, 0.000000000000000000 ) ) ;
#43443=CARTESIAN_POINT ( 'NONE',  ( 0.000000000000000000, 74.65491531819118620, 23.16904090965732621 ) ) ;
#43444=CARTESIAN_POINT ( 'NONE',  ( 11.99999999999999822, 71.91182617369190666, 28.89263327155770966 ) ) ;
#43454=DIRECTION ( 'NONE',  ( 0.000000000000000000, 0.000000000000000000, 1.000000000000000000 ) ) ;
#43464=ORIENTED_EDGE ( 'NONE', *, *, #6862, .F. ) ;
#43473=ORIENTED_EDGE ( 'NONE', *, *, #29551, .T. ) ;
#43480=EDGE_CURVE ( 'NONE', #64655, #6829, #35378, .T. ) ;
#43499=ORIENTED_EDGE ( 'NONE', *, *, #64536, .T. ) ;
#43506=CARTESIAN_POINT ( 'NONE',  ( 12.00000000000000000, -4.261787119644963262, 26.19803753235780164 ) ) ;
#43509=DIRECTION ( 'NONE',  ( 0.000000000000000000, -0.4067366430758009854, -0.9135454576426004225 ) ) ;
#43510=ORIENTED_EDGE ( 'NONE', *, *, #20894, .F. ) ;
#43511=DIRECTION ( 'NONE',  ( -1.000000000000000000, 0.000000000000000000, 0.000000000000000000 ) ) ;
#43514=DIRECTION ( 'NONE',  ( 0.000000000000000000, 0.000000000000000000, 1.000000000000000000 ) ) ;
#43518=CARTESIAN_POINT ( 'NONE',  ( 11.99999999999999822, 0.000000000000000000, 0.000000000000000000 ) ) ;
#43532=CARTESIAN_POINT ( 'NONE',  ( 0.000000000000000000, 0.000000000000000000, 0.000000000000000000 ) ) ;
#43536=CARTESIAN_POINT ( 'NONE',  ( 0.000000000000000000, 80.55351364060589958, 15.33399622253512540 ) ) ;
#43542=CARTESIAN_POINT ( 'NONE',  ( 5.999999999999999112, 74.74816331893430288, 33.71516098798768724 ) ) ;
#43555=EDGE_CURVE ( 'NONE', #39400, #15161, #16051, .T. ) ;
#43557=EDGE_LOOP ( 'NONE', ( #48693, #48393, #13839, #36450 ) ) ;
#43559=VECTOR ( 'NONE', #19722, 1000.000000000000000 ) ;
#43564=EDGE_CURVE ( 'NONE', #13681, #67162, #71416, .T. ) ;
#43571=DIRECTION ( 'NONE',  ( -1.000000000000000000, 0.000000000000000000, -0.000000000000000000 ) ) ;
#43578=EDGE_CURVE ( 'NONE', #3442, #24796, #47857, .T. ) ;
#43590=CARTESIAN_POINT ( 'NONE',  ( 11.99999999999999822, 0.000000000000000000, 0.000000000000000000 ) ) ;
#43602=ORIENTED_EDGE ( 'NONE', *, *, #14750, .F. ) ;
#43606=CARTESIAN_POINT ( 'NONE',  ( 15.00000000000000000, 14.60985201121729737, 18.46759930825687235 ) ) ;
#43619=DIRECTION ( 'NONE',  ( 0.000000000000000000, -0.8526401643540970632, 0.5224985647159409163 ) ) ;
#43621=CARTESIAN_POINT ( 'NONE',  ( 15.00000000000000000, -26.23277895567245466, 4.042438405570107918 ) ) ;
#43629=ADVANCED_FACE ( 'NONE', ( #43261 ), #54881, .T. ) ;
#43630=CARTESIAN_POINT ( 'NONE',  ( 11.99999999999999822, 63.18004540533092239, -44.88180994100307686 ) ) ;
#43638=ORIENTED_EDGE ( 'NONE', *, *, #65170, .T. ) ;
#43639=DIRECTION ( 'NONE',  ( -1.000000000000000000, 0.000000000000000000, 0.000000000000000000 ) ) ;
#43641=ORIENTED_EDGE ( 'NONE', *, *, #21364, .T. ) ;
#43642=AXIS2_PLACEMENT_3D ( 'NONE', #51744, #289, #23185 ) ;
#43657=DIRECTION ( 'NONE',  ( 0.000000000000000000, 0.000000000000000000, 1.000000000000000000 ) ) ;
#43658=CARTESIAN_POINT ( 'NONE',  ( 11.99999999999999822, 62.50329211542494789, -41.76937507738723099 ) ) ;
#43662=ADVANCED_FACE ( 'NONE', ( #18909 ), #7279, .T. ) ;
#43666=EDGE_CURVE ( 'NONE', #73391, #16056, #70783, .T. ) ;
#43671=ORIENTED_EDGE ( 'NONE', *, *, #38136, .F. ) ;
#43677=VERTEX_POINT ( 'NONE', #25311 ) ;
#43678=CARTESIAN_POINT ( 'NONE',  ( 0.000000000000000000, 0.000000000000000000, 0.000000000000000000 ) ) ;
#43683=VERTEX_POINT ( 'NONE', #36576 ) ;
#43688=LINE ( 'NONE', #66608, #35694 ) ;
#43694=ORIENTED_EDGE ( 'NONE', *, *, #49460, .T. ) ;
#43706=EDGE_CURVE ( 'NONE', #39794, #11001, #8011, .T. ) ;
#43708=LINE ( 'NONE', #66269, #64605 ) ;
#43714=EDGE_CURVE ( 'NONE', #9521, #7284, #58782, .T. ) ;
#43718=DIRECTION ( 'NONE',  ( -1.000000000000000000, -0.000000000000000000, -0.000000000000000000 ) ) ;
#43724=DIRECTION ( 'NONE',  ( -1.000000000000000000, 0.000000000000000000, 0.000000000000000000 ) ) ;
#43733=ORIENTED_EDGE ( 'NONE', *, *, #45406, .F. ) ;
#43739=VERTEX_POINT ( 'NONE', #64425 ) ;
#43740=DIRECTION ( 'NONE',  ( -1.000000000000000000, 0.000000000000000000, -0.000000000000000000 ) ) ;
#43741=ORIENTED_EDGE ( 'NONE', *, *, #27863, .F. ) ;
#43743=ORIENTED_EDGE ( 'NONE', *, *, #47945, .T. ) ;
#43745=CARTESIAN_POINT ( 'NONE',  ( 11.99999999999999822, -75.11764819372149304, 2.946379043146075905 ) ) ;
#43753=DIRECTION ( 'NONE',  ( -1.000000000000000000, 0.000000000000000000, -0.000000000000000000 ) ) ;
#43757=EDGE_LOOP ( 'NONE', ( #57014, #4440, #57348, #18750 ) ) ;
#43763=CARTESIAN_POINT ( 'NONE',  ( 0.000000000000000000, -16.65972982744876774, -80.28980883073775487 ) ) ;
#43767=DIRECTION ( 'NONE',  ( -1.000000000000000000, 0.000000000000000000, 0.000000000000000000 ) ) ;
#43776=CARTESIAN_POINT ( 'NONE',  ( 15.00000000000000000, -18.13022148937242761, 15.02647892043569122 ) ) ;
#43800=CIRCLE ( 'NONE', #72573, 31.99999999999998579 ) ;
#43809=CARTESIAN_POINT ( 'NONE',  ( 11.99999999999999822, -27.74655509720618696, -77.16300072079690153 ) ) ;
#43816=ADVANCED_FACE ( 'NONE', ( #14753 ), #66994, .T. ) ;
#43826=VERTEX_POINT ( 'NONE', #21878 ) ;
#43830=ORIENTED_EDGE ( 'NONE', *, *, #7118, .F. ) ;
#43833=EDGE_CURVE ( 'NONE', #28422, #10181, #56095, .T. ) ;
#43836=ADVANCED_FACE ( 'NONE', ( #44453 ), #49694, .T. ) ;
#43838=DIRECTION ( 'NONE',  ( -1.000000000000000000, -0.000000000000000000, -0.000000000000000000 ) ) ;
#43843=EDGE_CURVE ( 'NONE', #25675, #67853, #51505, .T. ) ;
#43845=EDGE_LOOP ( 'NONE', ( #10175, #42275, #63643, #9313 ) ) ;
#43852=CARTESIAN_POINT ( 'NONE',  ( 11.99999999999999822, -51.02545421589363883, 55.20638768913742922 ) ) ;
#43856=VERTEX_POINT ( 'NONE', #10224 ) ;
#43863=CARTESIAN_POINT ( 'NONE',  ( 15.00000000000000000, -11.95096189432345746, -23.69967320028757030 ) ) ;
#43865=DIRECTION ( 'NONE',  ( -1.000000000000000000, 0.000000000000000000, -0.000000000000000000 ) ) ;
#43875=LINE ( 'NONE', #14167, #16097 ) ;
#43878=VECTOR ( 'NONE', #46096, 1000.000000000000000 ) ;
#43880=AXIS2_PLACEMENT_3D ( 'NONE', #27459, #15072, #38011 ) ;
#43881=ORIENTED_EDGE ( 'NONE', *, *, #34360, .T. ) ;
#43887=DIRECTION ( 'NONE',  ( -1.000000000000000000, -0.000000000000000000, 0.000000000000000000 ) ) ;
#43890=DIRECTION ( 'NONE',  ( -1.000000000000000000, -0.000000000000000000, 0.000000000000000000 ) ) ;
#43905=ADVANCED_FACE ( 'NONE', ( #44824 ), #67749, .T. ) ;
#43913=ADVANCED_FACE ( 'NONE', ( #48960 ), #9858, .T. ) ;
#43918=CARTESIAN_POINT ( 'NONE',  ( 11.99999999999999822, 0.000000000000000000, 0.000000000000000000 ) ) ;
#43921=CARTESIAN_POINT ( 'NONE',  ( 5.999999999999999112, -50.23322058963299241, -64.81221759200397514 ) ) ;
#43925=ORIENTED_EDGE ( 'NONE', *, *, #6117, .F. ) ;
#43928=CIRCLE ( 'NONE', #37910, 82.00000000000000000 ) ;
#43931=AXIS2_PLACEMENT_3D ( 'NONE', #68508, #35025, #6816 ) ;
#43940=DIRECTION ( 'NONE',  ( 1.000000000000000000, -0.000000000000000000, 0.000000000000000000 ) ) ;
#43942=ORIENTED_EDGE ( 'NONE', *, *, #34961, .T. ) ;
#43943=VECTOR ( 'NONE', #66611, 1000.000000000000000 ) ;
#43957=CARTESIAN_POINT ( 'NONE',  ( 11.99999999999999822, 68.27212725128275395, 31.46837873495001503 ) ) ;
#43962=CARTESIAN_POINT ( 'NONE',  ( 12.00000000000000000, 20.85821328998756385, 10.92862929874494249 ) ) ;
#43964=LINE ( 'NONE', #3028, #16545 ) ;
#43968=EDGE_CURVE ( 'NONE', #68824, #13504, #28698, .T. ) ;
#43969=DIRECTION ( 'NONE',  ( -1.000000000000000000, -0.000000000000000000, -0.000000000000000000 ) ) ;
#43976=DIRECTION ( 'NONE',  ( -1.000000000000000000, -0.000000000000000000, 0.000000000000000000 ) ) ;
#43977=DIRECTION ( 'NONE',  ( -1.000000000000000000, 0.000000000000000000, 0.000000000000000000 ) ) ;
#43978=DIRECTION ( 'NONE',  ( -1.000000000000000000, 0.000000000000000000, 0.000000000000000000 ) ) ;
#43980=CIRCLE ( 'NONE', #18731, 31.99999999999998934 ) ;
#43984=CIRCLE ( 'NONE', #17569, 82.00000000000000000 ) ;
#43986=AXIS2_PLACEMENT_3D ( 'NONE', #54746, #60768, #26906 ) ;
#43989=EDGE_CURVE ( 'NONE', #60745, #55710, #56293, .T. ) ;
#44001=CARTESIAN_POINT ( 'NONE',  ( 11.99999999999999822, 8.830959090343430518, -74.65491531819107252 ) ) ;
#44006=ORIENTED_EDGE ( 'NONE', *, *, #62038, .F. ) ;
#44010=ORIENTED_EDGE ( 'NONE', *, *, #11805, .F. ) ;
#44013=VERTEX_POINT ( 'NONE', #477 ) ;
#44027=ORIENTED_EDGE ( 'NONE', *, *, #18747, .T. ) ;
#44030=CARTESIAN_POINT ( 'NONE',  ( 0.000000000000000000, 0.000000000000000000, 0.000000000000000000 ) ) ;
#44042=AXIS2_PLACEMENT_3D ( 'NONE', #10491, #10876, #44342 ) ;
#44051=EDGE_CURVE ( 'NONE', #63122, #45831, #21431, .T. ) ;
#44058=CARTESIAN_POINT ( 'NONE',  ( 0.000000000000000000, 0.000000000000000000, 0.000000000000000000 ) ) ;
#44079=LINE ( 'NONE', #55351, #1011 ) ;
#44081=EDGE_LOOP ( 'NONE', ( #26629, #26952, #2772, #44623 ) ) ;
#44089=ORIENTED_EDGE ( 'NONE', *, *, #6284, .T. ) ;
#44095=CARTESIAN_POINT ( 'NONE',  ( 12.00000000000000000, -13.04903810567646971, 19.60159698893442481 ) ) ;
#44102=EDGE_CURVE ( 'NONE', #24794, #13281, #69955, .T. ) ;
#44106=CARTESIAN_POINT ( 'NONE',  ( 11.99999999999999822, 0.000000000000000000, 0.000000000000000000 ) ) ;
#44117=DIRECTION ( 'NONE',  ( 0.000000000000000000, 0.000000000000000000, 1.000000000000000000 ) ) ;
#44131=DIRECTION ( 'NONE',  ( 0.000000000000000000, 0.000000000000000000, 1.000000000000000000 ) ) ;
#44140=VERTEX_POINT ( 'NONE', #18818 ) ;
#44145=DIRECTION ( 'NONE',  ( -1.000000000000000000, 0.000000000000000000, 0.000000000000000000 ) ) ;
#44147=DIRECTION ( 'NONE',  ( 0.000000000000000000, 0.07845909572784530439, -0.9969173337331279638 ) ) ;
#44148=DIRECTION ( 'NONE',  ( -1.000000000000000000, 0.000000000000000000, -0.000000000000000000 ) ) ;
#44159=PLANE ( 'NONE',  #47317 ) ;
#44163=AXIS2_PLACEMENT_3D ( 'NONE', #32766, #32028, #49328 ) ;
#44165=EDGE_CURVE ( 'NONE', #46404, #12556, #64777, .T. ) ;
#44168=EDGE_CURVE ( 'NONE', #72371, #53358, #52750, .T. ) ;
#44172=ORIENTED_EDGE ( 'NONE', *, *, #40014, .T. ) ;
#44184=AXIS2_PLACEMENT_3D ( 'NONE', #14470, #61078, #54332 ) ;
#44191=DIRECTION ( 'NONE',  ( -1.000000000000000000, 0.000000000000000000, 0.000000000000000000 ) ) ;
#44200=VERTEX_POINT ( 'NONE', #42147 ) ;
#44201=ORIENTED_EDGE ( 'NONE', *, *, #72875, .F. ) ;
#44204=CARTESIAN_POINT ( 'NONE',  ( 0.000000000000000000, 6.903761155838878061, -77.19088730480517313 ) ) ;
#44212=DIRECTION ( 'NONE',  ( -1.000000000000000000, -0.000000000000000000, 0.000000000000000000 ) ) ;
#44223=VERTEX_POINT ( 'NONE', #8669 ) ;
#44225=CARTESIAN_POINT ( 'NONE',  ( 11.99999999999999822, 24.73286445877705475, 73.44644590900068692 ) ) ;
#44226=LINE ( 'NONE', #5131, #73852 ) ;
#44227=DIRECTION ( 'NONE',  ( 0.000000000000000000, 0.000000000000000000, 1.000000000000000000 ) ) ;
#44230=CARTESIAN_POINT ( 'NONE',  ( 0.000000000000000000, 0.000000000000000000, 0.000000000000000000 ) ) ;
#44232=CARTESIAN_POINT ( 'NONE',  ( 11.99999999999999822, 44.99326035066052754, 68.55367621811160461 ) ) ;
#44233=CYLINDRICAL_SURFACE ( 'NONE', #50312, 77.49899999999999523 ) ;
#44236=CARTESIAN_POINT ( 'NONE',  ( 0.000000000000000000, 71.21200624218795383, 40.65526001592638039 ) ) ;
#44241=ORIENTED_EDGE ( 'NONE', *, *, #72875, .T. ) ;
#44242=CIRCLE ( 'NONE', #23841, 77.49899999999999523 ) ;
#44243=EDGE_CURVE ( 'NONE', #5010, #20558, #61284, .T. ) ;
#44250=CIRCLE ( 'NONE', #52605, 31.99999999999998224 ) ;
#44251=CARTESIAN_POINT ( 'NONE',  ( 0.000000000000000000, 74.65374052328648702, 8.840884882375350529 ) ) ;
#44252=DIRECTION ( 'NONE',  ( 0.000000000000000000, 0.000000000000000000, 1.000000000000000000 ) ) ;
#44255=LINE ( 'NONE', #61553, #12555 ) ;
#44258=DIRECTION ( 'NONE',  ( -1.000000000000000000, 0.000000000000000000, 0.000000000000000000 ) ) ;
#44259=EDGE_CURVE ( 'NONE', #11277, #35768, #56352, .T. ) ;
#44261=CYLINDRICAL_SURFACE ( 'NONE', #12104, 31.99999999999998579 ) ;
#44265=FACE_OUTER_BOUND ( 'NONE', #19884, .T. ) ;
#44274=DIRECTION ( 'NONE',  ( -1.000000000000000000, 0.000000000000000000, 0.000000000000000000 ) ) ;
#44277=ORIENTED_EDGE ( 'NONE', *, *, #53789, .T. ) ;
#44282=DIRECTION ( 'NONE',  ( -1.000000000000000000, 0.000000000000000000, 0.000000000000000000 ) ) ;
#44288=EDGE_CURVE ( 'NONE', #33478, #58617, #37616, .T. ) ;
#44292=EDGE_CURVE ( 'NONE', #33472, #18767, #67287, .T. ) ;
#44298=ADVANCED_FACE ( 'NONE', ( #27044 ), #32686, .T. ) ;
#44310=DIRECTION ( 'NONE',  ( -1.000000000000000000, -0.000000000000000000, -0.000000000000000000 ) ) ;
#44312=LINE ( 'NONE', #21744, #3693 ) ;
#44313=ORIENTED_EDGE ( 'NONE', *, *, #44770, .T. ) ;
#44314=CARTESIAN_POINT ( 'NONE',  ( 0.000000000000000000, -31.46837873495025306, 68.27212725128265447 ) ) ;
#44320=DIRECTION ( 'NONE',  ( 0.000000000000000000, -1.000000000000000000, -1.040834085586084730E-14 ) ) ;
#44322=VECTOR ( 'NONE', #3414, 1000.000000000000000 ) ;
#44335=ADVANCED_FACE ( 'NONE', ( #26315 ), #15032, .F. ) ;
#44342=DIRECTION ( 'NONE',  ( 0.000000000000000000, 0.000000000000000000, 1.000000000000000000 ) ) ;
#44347=DIRECTION ( 'NONE',  ( 0.000000000000000000, 0.000000000000000000, 1.000000000000000000 ) ) ;
#44355=AXIS2_PLACEMENT_3D ( 'NONE', #40099, #62298, #46111 ) ;
#44357=AXIS2_PLACEMENT_3D ( 'NONE', #15785, #10507, #74034 ) ;
#44360=DIRECTION ( 'NONE',  ( -1.000000000000000000, -0.000000000000000000, -0.000000000000000000 ) ) ;
#44362=DIRECTION ( 'NONE',  ( 0.000000000000000000, 0.000000000000000000, 1.000000000000000000 ) ) ;
#44373=VERTEX_POINT ( 'NONE', #55263 ) ;
#44383=EDGE_CURVE ( 'NONE', #2104, #2804, #5976, .T. ) ;
#44385=CARTESIAN_POINT ( 'NONE',  ( 0.000000000000000000, 0.000000000000000000, 0.000000000000000000 ) ) ;
#44391=DIRECTION ( 'NONE',  ( 0.000000000000000000, 0.000000000000000000, 1.000000000000000000 ) ) ;
#44396=VECTOR ( 'NONE', #36451, 1000.000000000000000 ) ;
#44400=ADVANCED_FACE ( 'NONE', ( #56390 ), #4905, .F. ) ;
#44405=DIRECTION ( 'NONE',  ( -1.000000000000000000, 0.000000000000000000, 0.000000000000000000 ) ) ;
#44408=CIRCLE ( 'NONE', #48002, 31.99999999999998934 ) ;
#44414=EDGE_CURVE ( 'NONE', #5889, #42911, #27801, .T. ) ;
#44425=AXIS2_PLACEMENT_3D ( 'NONE', #69472, #64216, #58556 ) ;
#44430=ORIENTED_EDGE ( 'NONE', *, *, #62246, .F. ) ;
#44431=AXIS2_PLACEMENT_3D ( 'NONE', #9903, #9540, #5031 ) ;
#44434=AXIS2_PLACEMENT_3D ( 'NONE', #25735, #49765, #38123 ) ;
#44435=ORIENTED_EDGE ( 'NONE', *, *, #13917, .F. ) ;
#44438=VECTOR ( 'NONE', #21137, 1000.000000000000000 ) ;
#44449=DIRECTION ( 'NONE',  ( 0.000000000000000000, 0.000000000000000000, 1.000000000000000000 ) ) ;
#44453=FACE_OUTER_BOUND ( 'NONE', #66196, .T. ) ;
#44459=DIRECTION ( 'NONE',  ( -1.000000000000000000, 0.000000000000000000, -0.000000000000000000 ) ) ;
#44463=ADVANCED_FACE ( 'NONE', ( #56765 ), #62793, .T. ) ;
#44468=ORIENTED_EDGE ( 'NONE', *, *, #18984, .T. ) ;
#44473=ADVANCED_FACE ( 'NONE', ( #51847 ), #22926, .T. ) ;
#44479=CIRCLE ( 'NONE', #36097, 31.99999999999998579 ) ;
#44487=DIRECTION ( 'NONE',  ( 0.000000000000000000, 0.000000000000000000, 1.000000000000000000 ) ) ;
#44495=ORIENTED_EDGE ( 'NONE', *, *, #24459, .T. ) ;
#44502=DIRECTION ( 'NONE',  ( 0.000000000000000000, -0.9135454576426050854, -0.4067366430757908824 ) ) ;
#44505=CARTESIAN_POINT ( 'NONE',  ( 11.99999999999999822, -62.50329211542407393, -41.76937507738853839 ) ) ;
#44507=EDGE_CURVE ( 'NONE', #23563, #25482, #51614, .T. ) ;
#44517=DIRECTION ( 'NONE',  ( -1.000000000000000000, 0.000000000000000000, 0.000000000000000000 ) ) ;
#44521=CARTESIAN_POINT ( 'NONE',  ( 11.99999999999999822, 0.8261519478441983200, -77.49459641780885022 ) ) ;
#44526=CARTESIAN_POINT ( 'NONE',  ( 12.00000000000000000, -19.89357724624986901, 12.59942793731086219 ) ) ;
#44529=DIRECTION ( 'NONE',  ( -1.000000000000000000, 0.000000000000000000, -0.000000000000000000 ) ) ;
#44531=FACE_OUTER_BOUND ( 'NONE', #19638, .T. ) ;
#44540=CARTESIAN_POINT ( 'NONE',  ( 11.99999999999999822, 0.000000000000000000, 0.000000000000000000 ) ) ;
#44550=DIRECTION ( 'NONE',  ( -1.000000000000000000, 0.000000000000000000, -0.000000000000000000 ) ) ;
#44554=DIRECTION ( 'NONE',  ( -1.000000000000000000, -0.000000000000000000, 0.000000000000000000 ) ) ;
#44560=ORIENTED_EDGE ( 'NONE', *, *, #11899, .T. ) ;
#44563=EDGE_CURVE ( 'NONE', #9702, #46802, #2235, .T. ) ;
#44565=VECTOR ( 'NONE', #67181, 1000.000000000000000 ) ;
#44571=ORIENTED_EDGE ( 'NONE', *, *, #33105, .F. ) ;
#44583=ORIENTED_EDGE ( 'NONE', *, *, #74106, .F. ) ;
#44586=VECTOR ( 'NONE', #31644, 1000.000000000000114 ) ;
#44598=ORIENTED_EDGE ( 'NONE', *, *, #45607, .T. ) ;
#44603=AXIS2_PLACEMENT_3D ( 'NONE', #38341, #20676, #15780 ) ;
#44609=CYLINDRICAL_SURFACE ( 'NONE', #26584, 31.99999999999998579 ) ;
#44623=ORIENTED_EDGE ( 'NONE', *, *, #30134, .T. ) ;
#44641=DIRECTION ( 'NONE',  ( -0.000000000000000000, -0.9135454576426058626, -0.4067366430757889395 ) ) ;
#44648=AXIS2_PLACEMENT_3D ( 'NONE', #28597, #55189, #50277 ) ;
#44649=CARTESIAN_POINT ( 'NONE',  ( 5.999999999999999112, 46.11716303203186840, 67.80270845531904911 ) ) ;
#44652=EDGE_CURVE ( 'NONE', #10620, #37614, #38417, .T. ) ;
#44656=DIRECTION ( 'NONE',  ( -1.000000000000000000, -0.000000000000000000, -0.000000000000000000 ) ) ;
#44660=LINE ( 'NONE', #22084, #59960 ) ;
#44662=EDGE_LOOP ( 'NONE', ( #47595, #37464, #2912, #33254 ) ) ;
#44672=AXIS2_PLACEMENT_3D ( 'NONE', #34902, #74000, #46549 ) ;
#44675=EDGE_LOOP ( 'NONE', ( #47900, #45268, #35265, #6810 ) ) ;
#44684=ORIENTED_EDGE ( 'NONE', *, *, #15374, .T. ) ;
#44690=FACE_OUTER_BOUND ( 'NONE', #21428, .T. ) ;
#44700=FACE_OUTER_BOUND ( 'NONE', #70921, .T. ) ;
#44708=DIRECTION ( 'NONE',  ( -1.000000000000000000, -0.000000000000000000, -0.000000000000000000 ) ) ;
#44710=ORIENTED_EDGE ( 'NONE', *, *, #38369, .F. ) ;
#44713=LINE ( 'NONE', #43962, #6258 ) ;
#44716=DIRECTION ( 'NONE',  ( 0.000000000000000000, 0.000000000000000000, 1.000000000000000000 ) ) ;
#44736=EDGE_CURVE ( 'NONE', #24497, #7244, #60822, .T. ) ;
#44741=DIRECTION ( 'NONE',  ( 0.000000000000000000, 0.000000000000000000, 1.000000000000000000 ) ) ;
#44743=CARTESIAN_POINT ( 'NONE',  ( 0.000000000000000000, 0.000000000000000000, 0.000000000000000000 ) ) ;
#44745=AXIS2_PLACEMENT_3D ( 'NONE', #24453, #17066, #39997 ) ;
#44762=CARTESIAN_POINT ( 'NONE',  ( 0.000000000000000000, 81.96053171279902472, -2.543863470248677316 ) ) ;
#44770=EDGE_CURVE ( 'NONE', #35604, #2536, #46793, .T. ) ;
#44772=DIRECTION ( 'NONE',  ( 0.000000000000000000, 0.000000000000000000, 1.000000000000000000 ) ) ;
#44775=VERTEX_POINT ( 'NONE', #4064 ) ;
#44782=ORIENTED_EDGE ( 'NONE', *, *, #31230, .T. ) ;
#44783=EDGE_LOOP ( 'NONE', ( #32078, #2183, #45870, #33063 ) ) ;
#44793=ORIENTED_EDGE ( 'NONE', *, *, #41022, .T. ) ;
#44794=CARTESIAN_POINT ( 'NONE',  ( 15.00000000000000000, -20.55727247249748402, -16.78983467731284307 ) ) ;
#44795=CARTESIAN_POINT ( 'NONE',  ( 11.99999999999999822, 78.73519480814985627, -22.90783923731548199 ) ) ;
#44799=CARTESIAN_POINT ( 'NONE',  ( 15.00000000000000000, -26.23277895567245466, 4.042438405570107918 ) ) ;
#44808=CARTESIAN_POINT ( 'NONE',  ( 0.000000000000000000, 50.95692526931329525, 58.39081064771768581 ) ) ;
#44816=CYLINDRICAL_SURFACE ( 'NONE', #70569, 82.00000000000000000 ) ;
#44821=DIRECTION ( 'NONE',  ( -1.000000000000000000, -0.000000000000000000, -0.000000000000000000 ) ) ;
#44824=FACE_OUTER_BOUND ( 'NONE', #27455, .T. ) ;
#44826=CARTESIAN_POINT ( 'NONE',  ( 11.99999999999999822, 0.000000000000000000, 0.000000000000000000 ) ) ;
#44834=ORIENTED_EDGE ( 'NONE', *, *, #47359, .F. ) ;
#44835=CARTESIAN_POINT ( 'NONE',  ( 11.99999999999999822, 0.000000000000000000, 0.000000000000000000 ) ) ;
#44836=CYLINDRICAL_SURFACE ( 'NONE', #66749, 82.00000000000000000 ) ;
#44845=AXIS2_PLACEMENT_3D ( 'NONE', #3680, #20579, #66445 ) ;
#44847=EDGE_LOOP ( 'NONE', ( #21086, #30853, #10094, #19493 ) ) ;
#44860=DIRECTION ( 'NONE',  ( -1.000000000000000000, -0.000000000000000000, -0.000000000000000000 ) ) ;
#44864=ORIENTED_EDGE ( 'NONE', *, *, #6167, .F. ) ;
#44871=DIRECTION ( 'NONE',  ( 0.000000000000000000, 0.4067366430757908824, -0.9135454576426050854 ) ) ;
#44873=CYLINDRICAL_SURFACE ( 'NONE', #44431, 82.00000000000000000 ) ;
#44878=VECTOR ( 'NONE', #49429, 1000.000000000000000 ) ;
#44887=VECTOR ( 'NONE', #26762, 1000.000000000000000 ) ;
#44892=DIRECTION ( 'NONE',  ( 0.000000000000000000, 0.000000000000000000, 1.000000000000000000 ) ) ;
#44894=AXIS2_PLACEMENT_3D ( 'NONE', #62619, #33262, #55845 ) ;
#44904=AXIS2_PLACEMENT_3D ( 'NONE', #69691, #58787, #18188 ) ;
#44914=DIRECTION ( 'NONE',  ( -1.000000000000000000, -0.000000000000000000, 0.000000000000000000 ) ) ;
#44919=ADVANCED_FACE ( 'NONE', ( #73565 ), #34097, .F. ) ;
#44932=CIRCLE ( 'NONE', #22112, 82.00000000000000000 ) ;
#44933=DIRECTION ( 'NONE',  ( -1.000000000000000000, 0.000000000000000000, 0.000000000000000000 ) ) ;
#44934=ORIENTED_EDGE ( 'NONE', *, *, #36435, .F. ) ;
#44948=VECTOR ( 'NONE', #57598, 1000.000000000000000 ) ;
#44955=FACE_OUTER_BOUND ( 'NONE', #36157, .T. ) ;
#44956=CYLINDRICAL_SURFACE ( 'NONE', #34307, 31.99999999999997868 ) ;
#44957=CARTESIAN_POINT ( 'NONE',  ( 11.99999999999999822, 0.000000000000000000, 0.000000000000000000 ) ) ;
#44971=DIRECTION ( 'NONE',  ( -1.000000000000000000, -0.000000000000000000, 0.000000000000000000 ) ) ;
#44975=CARTESIAN_POINT ( 'NONE',  ( 11.99999999999999822, -74.18225833017864090, -34.94270380257717790 ) ) ;
#44990=ORIENTED_EDGE ( 'NONE', *, *, #44288, .T. ) ;
#44992=VERTEX_POINT ( 'NONE', #27716 ) ;
#44994=EDGE_CURVE ( 'NONE', #48071, #42429, #60286, .T. ) ;
#44995=FACE_OUTER_BOUND ( 'NONE', #54197, .T. ) ;
#44998=CARTESIAN_POINT ( 'NONE',  ( 11.99999999999999822, 74.65491531819118620, -8.830959090342659579 ) ) ;
#45000=DIRECTION ( 'NONE',  ( -1.000000000000000000, 0.000000000000000000, 0.000000000000000000 ) ) ;
#45001=CARTESIAN_POINT ( 'NONE',  ( 11.99999999999999822, -18.89407956138204980, -75.16055320797050854 ) ) ;
#45003=CARTESIAN_POINT ( 'NONE',  ( 12.00000000000000000, 26.50000000000000355, -1.500000000000000000 ) ) ;
#45005=DIRECTION ( 'NONE',  ( 0.000000000000000000, 0.000000000000000000, 1.000000000000000000 ) ) ;
#45016=AXIS2_PLACEMENT_3D ( 'NONE', #53882, #19657, #60645 ) ;
#45018=EDGE_CURVE ( 'NONE', #21751, #40611, #29549, .T. ) ;
#45023=EDGE_CURVE ( 'NONE', #7584, #8374, #48618, .T. ) ;
#45024=CARTESIAN_POINT ( 'NONE',  ( 5.999999999999999112, -51.29473840253177030, -63.97538442413482329 ) ) ;
#45028=VERTEX_POINT ( 'NONE', #36967 ) ;
#45029=DIRECTION ( 'NONE',  ( 0.000000000000000000, 0.000000000000000000, 1.000000000000000000 ) ) ;
#45032=CARTESIAN_POINT ( 'NONE',  ( 11.99999999999999822, -74.65374052328654386, 8.840884882374837161 ) ) ;
#45036=ORIENTED_EDGE ( 'NONE', *, *, #17229, .F. ) ;
#45048=ORIENTED_EDGE ( 'NONE', *, *, #62579, .T. ) ;
#45053=FACE_OUTER_BOUND ( 'NONE', #37365, .T. ) ;
#45058=ORIENTED_EDGE ( 'NONE', *, *, #22615, .T. ) ;
#45060=DIRECTION ( 'NONE',  ( 0.000000000000000000, 0.000000000000000000, 1.000000000000000000 ) ) ;
#45066=AXIS2_PLACEMENT_3D ( 'NONE', #55485, #67508, #9983 ) ;
#45068=ORIENTED_EDGE ( 'NONE', *, *, #72531, .T. ) ;
#45070=EDGE_CURVE ( 'NONE', #51530, #19604, #54269, .T. ) ;
#45072=DIRECTION ( 'NONE',  ( -1.000000000000000000, -0.000000000000000000, 0.000000000000000000 ) ) ;
#45085=CIRCLE ( 'NONE', #65465, 77.49900000000000944 ) ;
#45087=CARTESIAN_POINT ( 'NONE',  ( 0.000000000000000000, 0.000000000000000000, 0.000000000000000000 ) ) ;
#45088=VECTOR ( 'NONE', #53582, 1000.000000000000000 ) ;
#45097=CARTESIAN_POINT ( 'NONE',  ( 11.99999999999999822, -55.20638768913724448, -51.02545421589383068 ) ) ;
#45098=CARTESIAN_POINT ( 'NONE',  ( 11.99999999999999822, 0.000000000000000000, 0.000000000000000000 ) ) ;
#45106=DIRECTION ( 'NONE',  ( -1.000000000000000000, 0.000000000000000000, 0.000000000000000000 ) ) ;
#45109=CARTESIAN_POINT ( 'NONE',  ( 5.999999999999999112, 55.16347631943131802, -60.67117009219074930 ) ) ;
#45124=CIRCLE ( 'NONE', #12690, 77.49900000000000944 ) ;
#45128=ORIENTED_EDGE ( 'NONE', *, *, #73829, .T. ) ;
#45130=VERTEX_POINT ( 'NONE', #12270 ) ;
#45133=DIRECTION ( 'NONE',  ( 0.000000000000000000, 1.000000000000000000, 1.301042606982602757E-15 ) ) ;
#45136=DIRECTION ( 'NONE',  ( 0.000000000000000000, -0.3826834323650969427, 0.9238795325112837409 ) ) ;
#45137=EDGE_LOOP ( 'NONE', ( #42763, #67875, #25975, #18886 ) ) ;
#45138=CYLINDRICAL_SURFACE ( 'NONE', #27443, 77.49899999999999523 ) ;
#45149=ORIENTED_EDGE ( 'NONE', *, *, #20726, .T. ) ;
#45151=ORIENTED_EDGE ( 'NONE', *, *, #45708, .T. ) ;
#45152=VERTEX_POINT ( 'NONE', #73382 ) ;
#45155=LINE ( 'NONE', #16198, #43366 ) ;
#45168=EDGE_CURVE ( 'NONE', #47715, #24191, #26776, .T. ) ;
#45171=CARTESIAN_POINT ( 'NONE',  ( 0.000000000000000000, -46.21855187248673502, 62.20884554314003623 ) ) ;
#45172=AXIS2_PLACEMENT_3D ( 'NONE', #50457, #21886, #23736 ) ;
#45182=EDGE_CURVE ( 'NONE', #62894, #60745, #20432, .T. ) ;
#45183=AXIS2_PLACEMENT_3D ( 'NONE', #16212, #62090, #11314 ) ;
#45187=EDGE_CURVE ( 'NONE', #34606, #9528, #37719, .T. ) ;
#45191=CARTESIAN_POINT ( 'NONE',  ( 11.99999999999999822, 0.000000000000000000, 0.000000000000000000 ) ) ;
#45201=EDGE_CURVE ( 'NONE', #588, #19443, #63655, .T. ) ;
#45204=CLOSED_SHELL ( 'NONE', ( #25488, #2987, #12876, #8423, #43905, #56634, #65696, #52098, #8648, #71695, #16491, #63160, #52772, #14585, #43816, #71467, #65896, #32144, #40318, #63618, #71983, #30861, #151, #30355, #56611, #43042, #6788, #30872, #64607, #38701, #62845, #57886, #61700, #51410, #63902, #25738, #63238, #48407, #49387, #67462, #65396, #49605, #53984, #22652, #16489, #37723, #22602, #25360, #27081, #63953, #46837, #67662, #51500, #40743, #45849, #24629, #3781, #54101, #43662, #23122, #40745, #59666, #69706, #53553, #15470, #49622, #42115, #24756, #55699, #10706, #34832, #12112, #48638, #8231, #20896, #53463, #46507, #24414, #43913, #70323, #9306, #21125, #57312, #37694, #23708, #59700, #71435, #5443, #17079, #10240, #32340, #24988, #23746, #31415, #54983, #14874, #50156, #73752, #70032, #18088, #35546, #53744, #30571, #61015, #24278, #9010, #14226, #65626, #37938, #41511, #12351, #56184, #50440, #57372, #70330, #12817, #21191, #2697, #37451, #57124, #40859, #27203, #11042, #13655, #58048, #67581, #22884, #69282, #5313, #12809, #24293, #60184, #11646, #3854, #42851, #9340, #43629, #18079, #58416, #73173, #49886, #3070, #35969, #21830, #65269, #72564, #2515, #57983, #20352, #47251, #4236, #18525, #29679, #2106, #37281, #16902, #47059, #52632, #28971, #41275, #44473, #60222, #51116, #35402, #22756, #36048, #13807, #9933, #34192, #26, #65809, #40947, #18005, #8087, #57904, #44298, #30948, #21801, #36259, #10975, #39031, #5110, #14420, #34547, #64682, #66119, #26881, #31495, #69243, #3916, #72932, #3876, #3840, #64247, #43836, #38479, #29544, #64495, #122, #23261, #23528, #18192, #18690, #1762, #44463, #6902, #53980, #61903, #37808, #46113, #36006, #12576, #9012, #65796, #48282, #19784, #71535, #27598, #58576, #7555, #25777, #63074, #62205, #42107, #65277, #28835, #62906, #68336, #2909, #9945, #19738, #34477, #52033, #11777, #40136, #46262, #40139, #46796, #37682, #23937, #13303, #21981, #29597, #20712, #56531, #53699, #16128, #58989, #24194, #14538, #1098, #47677, #59079, #1482, #37804, #56387, #71257, #15361, #5243, #20761, #14265, #20396, #33053, #19834, #69207, #50399, #7111, #38434, #39892, #35241, #62858, #11621, #66468, #5183, #61465, #16237, #22758, #12325, #14669, #60014, #52554, #46712, #39916, #1472, #2923, #50352, #12789, #34385, #64740, #1075, #50642, #67383, #10337, #66161, #59655, #23579, #49799, #4033, #24519, #71352, #25896, #17907, #13732, #68956, #59263, #2594, #15389, #12498, #7999, #244, #2939, #71212, #7720, #37022, #21283, #55420, #38204, #32717, #24227, #41774, #13353, #24689, #67557, #6568, #69701, #74123, #61307, #51842, #58468, #32405, #67985, #47220, #26273, #67917, #50696, #3742, #57291, #37693, #61124, #69531, #17687, #1733, #58252, #54683, #45921, #10973, #21359, #1656, #29015, #27128, #20121, #48469, #50320, #10295, #2694, #52954, #56200, #9767, #68019, #18800, #73562, #57301, #39651, #33687, #63322, #57370, #64423, #44400, #44335, #36667, #30895, #21184, #74155, #14948, #63038, #9062, #17758, #63522, #14352, #3651, #57207, #58554, #14854, #53783, #72732, #61370, #21909, #47712, #29421, #72697, #29828, #23969, #41924, #20290, #28023, #58507, #66903, #43080, #63321, #44919, #22711, #26404, #61994, #48621 ) ) ;
#45212=AXIS2_PLACEMENT_3D ( 'NONE', #68839, #17326, #12049 ) ;
#45222=CIRCLE ( 'NONE', #35595, 31.99999999999998934 ) ;
#45223=ORIENTED_EDGE ( 'NONE', *, *, #65529, .F. ) ;
#45231=DIRECTION ( 'NONE',  ( 0.000000000000000000, 0.9945218953682742891, 0.1045284632676436315 ) ) ;
#45240=FACE_OUTER_BOUND ( 'NONE', #21149, .T. ) ;
#45242=CIRCLE ( 'NONE', #47647, 82.00000000000000000 ) ;
#45257=DIRECTION ( 'NONE',  ( 0.000000000000000000, 0.000000000000000000, 1.000000000000000000 ) ) ;
#45259=CARTESIAN_POINT ( 'NONE',  ( 0.000000000000000000, 0.000000000000000000, 0.000000000000000000 ) ) ;
#45263=CARTESIAN_POINT ( 'NONE',  ( 12.00000000000000000, 23.49999999999999645, -1.500000000000003997 ) ) ;
#45268=ORIENTED_EDGE ( 'NONE', *, *, #20356, .T. ) ;
#45278=CIRCLE ( 'NONE', #62060, 31.99999999999998224 ) ;
#45281=CIRCLE ( 'NONE', #4495, 31.99999999999998224 ) ;
#45282=FACE_OUTER_BOUND ( 'NONE', #59332, .T. ) ;
#45294=VECTOR ( 'NONE', #63231, 1000.000000000000000 ) ;
#45298=LINE ( 'NONE', #68217, #63867 ) ;
#45315=VERTEX_POINT ( 'NONE', #58325 ) ;
#45317=ORIENTED_EDGE ( 'NONE', *, *, #34531, .F. ) ;
#45325=ORIENTED_EDGE ( 'NONE', *, *, #13178, .T. ) ;
#45327=VERTEX_POINT ( 'NONE', #22267 ) ;
#45329=DIRECTION ( 'NONE',  ( -1.000000000000000000, -0.000000000000000000, -0.000000000000000000 ) ) ;
#45330=DIRECTION ( 'NONE',  ( 0.000000000000000000, 0.000000000000000000, 1.000000000000000000 ) ) ;
#45333=DIRECTION ( 'NONE',  ( -1.000000000000000000, -0.000000000000000000, -0.000000000000000000 ) ) ;
#45334=CIRCLE ( 'NONE', #57342, 77.49900000000000944 ) ;
#45341=VERTEX_POINT ( 'NONE', #853 ) ;
#45342=DIRECTION ( 'NONE',  ( -1.000000000000000000, -0.000000000000000000, -0.000000000000000000 ) ) ;
#45349=CARTESIAN_POINT ( 'NONE',  ( 11.99999999999999822, 51.03279382321166224, -55.19960302592011914 ) ) ;
#45357=DIRECTION ( 'NONE',  ( -1.000000000000000000, -0.000000000000000000, -0.000000000000000000 ) ) ;
#45359=VECTOR ( 'NONE', #32985, 1000.000000000000000 ) ;
#45360=ORIENTED_EDGE ( 'NONE', *, *, #12247, .F. ) ;
#45365=CARTESIAN_POINT ( 'NONE',  ( 11.99999999999999822, 46.54456581323888997, -59.03342792756214408 ) ) ;
#45376=CARTESIAN_POINT ( 'NONE',  ( 11.99999999999999822, 55.19960302592141232, -51.03279382321027668 ) ) ;
#45378=DIRECTION ( 'NONE',  ( 0.000000000000000000, 0.5224985647159500202, -0.8526401643540915121 ) ) ;
#45379=CARTESIAN_POINT ( 'NONE',  ( 11.99999999999999822, -55.19960302592029677, -51.03279382321147750 ) ) ;
#45381=DIRECTION ( 'NONE',  ( 0.000000000000000000, 0.8910065241883655673, 0.4539904997395510233 ) ) ;
#45382=DIRECTION ( 'NONE',  ( -1.000000000000000000, 0.000000000000000000, 0.000000000000000000 ) ) ;
#45383=CARTESIAN_POINT ( 'NONE',  ( 0.000000000000000000, -78.73519480814971416, 22.90783923731599359 ) ) ;
#45390=DIRECTION ( 'NONE',  ( 0.000000000000000000, 0.1564344650402244852, 0.9876883405951387696 ) ) ;
#45393=VERTEX_POINT ( 'NONE', #41048 ) ;
#45401=ORIENTED_EDGE ( 'NONE', *, *, #3954, .F. ) ;
#45403=ORIENTED_EDGE ( 'NONE', *, *, #57887, .F. ) ;
#45406=EDGE_CURVE ( 'NONE', #48817, #15890, #25270, .T. ) ;
#45411=DIRECTION ( 'NONE',  ( 0.000000000000000000, 0.000000000000000000, 1.000000000000000000 ) ) ;
#45445=ORIENTED_EDGE ( 'NONE', *, *, #48775, .T. ) ;
#45450=EDGE_CURVE ( 'NONE', #60769, #6114, #3667, .T. ) ;
#45451=EDGE_LOOP ( 'NONE', ( #4872, #29315, #23009, #45896 ) ) ;
#45461=DIRECTION ( 'NONE',  ( 0.000000000000000000, 0.000000000000000000, -1.000000000000000000 ) ) ;
#45471=AXIS2_PLACEMENT_3D ( 'NONE', #12558, #29836, #5832 ) ;
#45479=CARTESIAN_POINT ( 'NONE',  ( 12.00000000000000000, -10.45096189432344502, -21.10159698893425784 ) ) ;
#45481=DIRECTION ( 'NONE',  ( -1.000000000000000000, -0.000000000000000000, -0.000000000000000000 ) ) ;
#45508=VERTEX_POINT ( 'NONE', #13923 ) ;
#45521=AXIS2_PLACEMENT_3D ( 'NONE', #61103, #26874, #37445 ) ;
#45533=EDGE_LOOP ( 'NONE', ( #42367, #7485, #12411, #41106 ) ) ;
#45534=CARTESIAN_POINT ( 'NONE',  ( 0.000000000000000000, 41.76106447765489094, 62.50884508063442269 ) ) ;
#45546=EDGE_CURVE ( 'NONE', #25482, #29219, #47778, .T. ) ;
#45555=CARTESIAN_POINT ( 'NONE',  ( 0.000000000000000000, 51.29473840253223216, 63.97538442413444670 ) ) ;
#45557=CIRCLE ( 'NONE', #13101, 77.49899999999998101 ) ;
#45558=CARTESIAN_POINT ( 'NONE',  ( 11.99999999999999822, 74.65491531819118620, 23.16904090965732621 ) ) ;
#45580=LINE ( 'NONE', #33905, #4575 ) ;
#45582=DIRECTION ( 'NONE',  ( 0.000000000000000000, 0.000000000000000000, 1.000000000000000000 ) ) ;
#45586=ORIENTED_EDGE ( 'NONE', *, *, #60553, .T. ) ;
#45588=DIRECTION ( 'NONE',  ( -1.000000000000000000, -0.000000000000000000, -0.000000000000000000 ) ) ;
#45591=CARTESIAN_POINT ( 'NONE',  ( 11.99999999999999822, -71.91182617369207719, 28.89263327155721228 ) ) ;
#45598=ORIENTED_EDGE ( 'NONE', *, *, #35040, .T. ) ;
#45599=DIRECTION ( 'NONE',  ( 0.000000000000000000, 0.000000000000000000, 1.000000000000000000 ) ) ;
#45600=VERTEX_POINT ( 'NONE', #24482 ) ;
#45605=DIRECTION ( 'NONE',  ( -1.000000000000000000, 0.000000000000000000, 0.000000000000000000 ) ) ;
#45607=EDGE_CURVE ( 'NONE', #19859, #55964, #70696, .T. ) ;
#45611=EDGE_CURVE ( 'NONE', #56976, #24230, #68373, .T. ) ;
#45626=CARTESIAN_POINT ( 'NONE',  ( 0.000000000000000000, 0.000000000000000000, 0.000000000000000000 ) ) ;
#45646=CARTESIAN_POINT ( 'NONE',  ( 11.99999999999999822, 0.000000000000000000, 0.000000000000000000 ) ) ;
#45649=ORIENTED_EDGE ( 'NONE', *, *, #29269, .T. ) ;
#45651=DIRECTION ( 'NONE',  ( 0.000000000000000000, -0.6494480483301903195, 0.7604059656000251577 ) ) ;
#45656=DIRECTION ( 'NONE',  ( -1.000000000000000000, 0.000000000000000000, -0.000000000000000000 ) ) ;
#45659=AXIS2_PLACEMENT_3D ( 'NONE', #56927, #45656, #61451 ) ;
#45669=EDGE_CURVE ( 'NONE', #65482, #32129, #23927, .T. ) ;
#45673=EDGE_LOOP ( 'NONE', ( #42627, #29246, #19119, #884 ) ) ;
#45675=CARTESIAN_POINT ( 'NONE',  ( 0.000000000000000000, 68.55367621811141987, 44.99326035066079044 ) ) ;
#45678=EDGE_CURVE ( 'NONE', #44013, #33546, #50311, .T. ) ;
#45680=EDGE_CURVE ( 'NONE', #8327, #20786, #63538, .T. ) ;
#45681=AXIS2_PLACEMENT_3D ( 'NONE', #19937, #54176, #1233 ) ;
#45689=ORIENTED_EDGE ( 'NONE', *, *, #71088, .F. ) ;
#45696=CARTESIAN_POINT ( 'NONE',  ( 11.99999999999999822, 74.18225833017889670, 34.94270380257665209 ) ) ;
#45702=ORIENTED_EDGE ( 'NONE', *, *, #51676, .F. ) ;
#45705=VERTEX_POINT ( 'NONE', #31958 ) ;
#45707=AXIS2_PLACEMENT_3D ( 'NONE', #10029, #55899, #37874 ) ;
#45708=EDGE_CURVE ( 'NONE', #25161, #48419, #3422, .T. ) ;
#45709=EDGE_CURVE ( 'NONE', #7579, #4754, #37622, .T. ) ;
#45713=DIRECTION ( 'NONE',  ( -1.000000000000000000, -0.000000000000000000, -0.000000000000000000 ) ) ;
#45714=AXIS2_PLACEMENT_3D ( 'NONE', #27760, #28873, #29245 ) ;
#45716=LINE ( 'NONE', #68639, #26382 ) ;
#45734=CARTESIAN_POINT ( 'NONE',  ( 11.99999999999999822, -77.16300072079641836, -27.74655509720752633 ) ) ;
#45736=CIRCLE ( 'NONE', #55303, 31.99999999999999289 ) ;
#45738=ORIENTED_EDGE ( 'NONE', *, *, #71639, .F. ) ;
#45744=DIRECTION ( 'NONE',  ( -1.000000000000000000, 0.000000000000000000, 0.000000000000000000 ) ) ;
#45753=LINE ( 'NONE', #62679, #62898 ) ;
#45762=VERTEX_POINT ( 'NONE', #49988 ) ;
#45773=DIRECTION ( 'NONE',  ( 0.000000000000000000, 0.07845909572784530439, -0.9969173337331279638 ) ) ;
#45792=ORIENTED_EDGE ( 'NONE', *, *, #45023, .T. ) ;
#45796=DIRECTION ( 'NONE',  ( -1.000000000000000000, -0.000000000000000000, 0.000000000000000000 ) ) ;
#45799=DIRECTION ( 'NONE',  ( 0.000000000000000000, 0.000000000000000000, 1.000000000000000000 ) ) ;
#45800=DIRECTION ( 'NONE',  ( 0.000000000000000000, 0.000000000000000000, 1.000000000000000000 ) ) ;
#45806=CARTESIAN_POINT ( 'NONE',  ( 0.000000000000000000, 0.000000000000000000, 0.000000000000000000 ) ) ;
#45812=DIRECTION ( 'NONE',  ( 0.000000000000000000, 0.000000000000000000, 1.000000000000000000 ) ) ;
#45813=DIRECTION ( 'NONE',  ( 0.000000000000000000, -0.9969173337331271867, -0.07845909572785571273 ) ) ;
#45815=MECHANICAL_DESIGN_GEOMETRIC_PRESENTATION_REPRESENTATION('',(#24175),#54227);
#45817=DIRECTION ( 'NONE',  ( 0.000000000000000000, -0.8090169943749497827, -0.5877852522924698064 ) ) ;
#45818=ORIENTED_EDGE ( 'NONE', *, *, #23202, .F. ) ;
#45823=AXIS2_PLACEMENT_3D ( 'NONE', #73069, #44529, #62573 ) ;
#45825=FACE_BOUND ( 'NONE', #59682, .T. ) ;
#45827=ORIENTED_EDGE ( 'NONE', *, *, #21620, .F. ) ;
#45831=VERTEX_POINT ( 'NONE', #70205 ) ;
#45838=AXIS2_PLACEMENT_3D ( 'NONE', #53275, #48007, #47271 ) ;
#45845=DIRECTION ( 'NONE',  ( -1.000000000000000000, 0.000000000000000000, -0.000000000000000000 ) ) ;
#45849=ADVANCED_FACE ( 'NONE', ( #1841 ), #8556, .T. ) ;
#45850=CARTESIAN_POINT ( 'NONE',  ( 11.99999999999999822, 72.35160999960817207, 20.41045688087850607 ) ) ;
#45852=DIRECTION ( 'NONE',  ( 0.000000000000000000, -0.5877852522924779111, -0.8090169943749440096 ) ) ;
#45862=CARTESIAN_POINT ( 'NONE',  ( 15.00000000000000000, -4.261787119644963262, 26.19803753235780164 ) ) ;
#45870=ORIENTED_EDGE ( 'NONE', *, *, #53153, .F. ) ;
#45880=VERTEX_POINT ( 'NONE', #36338 ) ;
#45882=ORIENTED_EDGE ( 'NONE', *, *, #28076, .F. ) ;
#45883=VERTEX_POINT ( 'NONE', #8525 ) ;
#45887=CIRCLE ( 'NONE', #26641, 82.00000000000000000 ) ;
#45895=ORIENTED_EDGE ( 'NONE', *, *, #14493, .F. ) ;
#45896=ORIENTED_EDGE ( 'NONE', *, *, #59502, .T. ) ;
#45902=EDGE_LOOP ( 'NONE', ( #14145, #50916, #1985, #73690 ) ) ;
#45903=DIRECTION ( 'NONE',  ( -1.000000000000000000, -0.000000000000000000, 0.000000000000000000 ) ) ;
#45907=CARTESIAN_POINT ( 'NONE',  ( 15.00000000000000000, 22.07842321921492612, 8.187992925817123790 ) ) ;
#45912=CARTESIAN_POINT ( 'NONE',  ( 11.99999999999999822, 2.956366410620650420, 75.11725578898469280 ) ) ;
#45917=AXIS2_PLACEMENT_3D ( 'NONE', #43432, #43048, #65236 ) ;
#45920=LINE ( 'NONE', #57568, #64918 ) ;
#45921=ADVANCED_FACE ( 'NONE', ( #66044 ), #25062, .F. ) ;
#45925=CIRCLE ( 'NONE', #71108, 31.99999999999999289 ) ;
#45928=DIRECTION ( 'NONE',  ( -1.000000000000000000, 0.000000000000000000, 0.000000000000000000 ) ) ;
#45929=AXIS2_PLACEMENT_3D ( 'NONE', #38591, #43511, #37488 ) ;
#45933=CIRCLE ( 'NONE', #13491, 31.99999999999998579 ) ;
#45934=DIRECTION ( 'NONE',  ( -1.000000000000000000, 0.000000000000000000, 0.000000000000000000 ) ) ;
#45947=CYLINDRICAL_SURFACE ( 'NONE', #594, 31.99999999999998579 ) ;
#45949=ORIENTED_EDGE ( 'NONE', *, *, #50214, .T. ) ;
#45953=CARTESIAN_POINT ( 'NONE',  ( -10.00000000000000000, 0.000000000000000000, 0.000000000000000000 ) ) ;
#45959=ORIENTED_EDGE ( 'NONE', *, *, #38446, .F. ) ;
#45960=DIRECTION ( 'NONE',  ( 0.000000000000000000, 0.000000000000000000, -1.000000000000000000 ) ) ;
#45967=ORIENTED_EDGE ( 'NONE', *, *, #55605, .T. ) ;
#45973=CARTESIAN_POINT ( 'NONE',  ( 11.99999999999999822, 0.000000000000000000, 0.000000000000000000 ) ) ;
#45977=CIRCLE ( 'NONE', #37547, 82.00000000000000000 ) ;
#45978=EDGE_LOOP ( 'NONE', ( #65309, #40084, #73603, #45223 ) ) ;
#45980=VECTOR ( 'NONE', #48854, 1000.000000000000000 ) ;
#45983=DIRECTION ( 'NONE',  ( -1.000000000000000000, 0.000000000000000000, 0.000000000000000000 ) ) ;
#45999=DIRECTION ( 'NONE',  ( 0.000000000000000000, 0.8526401643540935105, -0.5224985647159466895 ) ) ;
#46001=CARTESIAN_POINT ( 'NONE',  ( 11.99999999999999822, -17.28742895386137945, 75.54627589209938776 ) ) ;
#46004=ORIENTED_EDGE ( 'NONE', *, *, #32683, .T. ) ;
#46005=ORIENTED_EDGE ( 'NONE', *, *, #73396, .F. ) ;
#46009=FACE_OUTER_BOUND ( 'NONE', #19808, .T. ) ;
#46033=CIRCLE ( 'NONE', #20630, 82.00000000000000000 ) ;
#46034=DIRECTION ( 'NONE',  ( -1.000000000000000000, 0.000000000000000000, 0.000000000000000000 ) ) ;
#46035=CARTESIAN_POINT ( 'NONE',  ( 11.99999999999999822, -75.11725578898470701, 2.956366410620372864 ) ) ;
#46036=DIRECTION ( 'NONE',  ( 0.000000000000000000, 0.000000000000000000, 1.000000000000000000 ) ) ;
#46046=ORIENTED_EDGE ( 'NONE', *, *, #58058, .F. ) ;
#46053=VERTEX_POINT ( 'NONE', #4371 ) ;
#46058=ORIENTED_EDGE ( 'NONE', *, *, #63771, .T. ) ;
#46065=LINE ( 'NONE', #32905, #12259 ) ;
#46067=CYLINDRICAL_SURFACE ( 'NONE', #67174, 31.99999999999998579 ) ;
#46068=DIRECTION ( 'NONE',  ( -1.000000000000000000, -0.000000000000000000, -0.000000000000000000 ) ) ;
#46071=ORIENTED_EDGE ( 'NONE', *, *, #59641, .F. ) ;
#46076=AXIS2_PLACEMENT_3D ( 'NONE', #52604, #19133, #53715 ) ;
#46083=DIRECTION ( 'NONE',  ( -1.000000000000000000, 0.000000000000000000, -0.000000000000000000 ) ) ;
#46085=VERTEX_POINT ( 'NONE', #73134 ) ;
#46087=AXIS2_PLACEMENT_3D ( 'NONE', #44251, #73547, #45378 ) ;
#46094=EDGE_CURVE ( 'NONE', #2723, #53818, #14367, .T. ) ;
#46096=DIRECTION ( 'NONE',  ( -1.000000000000000000, 0.000000000000000000, 0.000000000000000000 ) ) ;
#46101=EDGE_CURVE ( 'NONE', #57093, #10768, #56395, .T. ) ;
#46110=LINE ( 'NONE', #28061, #47232 ) ;
#46111=DIRECTION ( 'NONE',  ( 0.000000000000000000, 0.000000000000000000, 1.000000000000000000 ) ) ;
#46113=ADVANCED_FACE ( 'NONE', ( #4004 ), #26904, .T. ) ;
#46116=CARTESIAN_POINT ( 'NONE',  ( 12.00000000000000000, -1.278221433540507546, -26.51162292216071492 ) ) ;
#46118=DIRECTION ( 'NONE',  ( -1.000000000000000000, -0.000000000000000000, 0.000000000000000000 ) ) ;
#46129=CARTESIAN_POINT ( 'NONE',  ( 0.000000000000000000, -15.33399622253541317, 80.55351364060584274 ) ) ;
#46140=CIRCLE ( 'NONE', #36516, 77.49899999999999523 ) ;
#46142=CARTESIAN_POINT ( 'NONE',  ( 11.99999999999999822, 46.53671651294032330, -59.03961581697353012 ) ) ;
#46146=AXIS2_PLACEMENT_3D ( 'NONE', #59111, #36163, #64015 ) ;
#46162=ORIENTED_EDGE ( 'NONE', *, *, #27610, .T. ) ;
#46176=ORIENTED_EDGE ( 'NONE', *, *, #47053, .F. ) ;
#46178=VERTEX_POINT ( 'NONE', #69729 ) ;
#46190=CARTESIAN_POINT ( 'NONE',  ( 11.99999999999999822, -55.38113227695745167, -54.21277698773732823 ) ) ;
#46191=VECTOR ( 'NONE', #3094, 1000.000000000000000 ) ;
#46196=EDGE_CURVE ( 'NONE', #28846, #68067, #5490, .T. ) ;
#46209=DIRECTION ( 'NONE',  ( -1.000000000000000000, 0.000000000000000000, 0.000000000000000000 ) ) ;
#46212=EDGE_CURVE ( 'NONE', #33465, #10745, #63013, .T. ) ;
#46213=DIRECTION ( 'NONE',  ( -1.000000000000000000, -0.000000000000000000, -0.000000000000000000 ) ) ;
#46214=CARTESIAN_POINT ( 'NONE',  ( 11.99999999999999822, -55.19960302592104284, 51.03279382321070301 ) ) ;
#46216=DIRECTION ( 'NONE',  ( -1.000000000000000000, -0.000000000000000000, 0.000000000000000000 ) ) ;
#46217=DIRECTION ( 'NONE',  ( -1.000000000000000000, -0.000000000000000000, 0.000000000000000000 ) ) ;
#46235=AXIS2_PLACEMENT_3D ( 'NONE', #35298, #29634, #15880 ) ;
#46238=LINE ( 'NONE', #57523, #10048 ) ;
#46239=CIRCLE ( 'NONE', #58254, 31.99999999999998579 ) ;
#46247=EDGE_LOOP ( 'NONE', ( #15109, #72565, #12396, #17490 ) ) ;
#46249=EDGE_CURVE ( 'NONE', #11167, #22373, #45716, .T. ) ;
#46262=ADVANCED_FACE ( 'NONE', ( #57722 ), #46067, .T. ) ;
#46269=EDGE_CURVE ( 'NONE', #7045, #11463, #47967, .T. ) ;
#46275=DIRECTION ( 'NONE',  ( 0.000000000000000000, 0.000000000000000000, 1.000000000000000000 ) ) ;
#46280=EDGE_CURVE ( 'NONE', #72968, #55761, #36256, .T. ) ;
#46285=DIRECTION ( 'NONE',  ( -1.000000000000000000, 0.000000000000000000, 0.000000000000000000 ) ) ;
#46290=AXIS2_PLACEMENT_3D ( 'NONE', #2234, #20210, #64249 ) ;
#46295=DIRECTION ( 'NONE',  ( 0.000000000000000000, -0.4539904997395542430, 0.8910065241883641241 ) ) ;
#46297=DIRECTION ( 'NONE',  ( -1.000000000000000000, 0.000000000000000000, -0.000000000000000000 ) ) ;
#46302=ORIENTED_EDGE ( 'NONE', *, *, #20097, .F. ) ;
#46303=CARTESIAN_POINT ( 'NONE',  ( 0.000000000000000000, 0.000000000000000000, 0.000000000000000000 ) ) ;
#46311=DIRECTION ( 'NONE',  ( 0.000000000000000000, 0.000000000000000000, 1.000000000000000000 ) ) ;
#46314=CARTESIAN_POINT ( 'NONE',  ( 15.00000000000000000, 16.83928648764922542, -16.46020748918050458 ) ) ;
#46317=CARTESIAN_POINT ( 'NONE',  ( 11.99999999999999822, 0.000000000000000000, 0.000000000000000000 ) ) ;
#46327=LINE ( 'NONE', #507, #63250 ) ;
#46332=FACE_OUTER_BOUND ( 'NONE', #36672, .T. ) ;
#46339=CIRCLE ( 'NONE', #53525, 31.99999999999998934 ) ;
#46341=PRODUCT_CONTEXT ( 'NONE', #57098, 'mechanical' ) ;
#46343=DIRECTION ( 'NONE',  ( 0.000000000000000000, 0.1564344650402244852, 0.9876883405951387696 ) ) ;
#46347=DIRECTION ( 'NONE',  ( 0.000000000000000000, 0.6691306063588570163, -0.7431448254773953543 ) ) ;
#46356=ORIENTED_EDGE ( 'NONE', *, *, #73671, .T. ) ;
#46363=CARTESIAN_POINT ( 'NONE',  ( 11.99999999999999822, -71.91182617369167929, -28.89263327155821059 ) ) ;
#46366=FACE_OUTER_BOUND ( 'NONE', #58710, .T. ) ;
#46368=AXIS2_PLACEMENT_3D ( 'NONE', #127, #45588, #68511 ) ;
#46373=EDGE_CURVE ( 'NONE', #58617, #35612, #66329, .T. ) ;
#46392=ORIENTED_EDGE ( 'NONE', *, *, #22959, .F. ) ;
#46401=EDGE_CURVE ( 'NONE', #18859, #13504, #39655, .T. ) ;
#46404=VERTEX_POINT ( 'NONE', #59196 ) ;
#46405=CIRCLE ( 'NONE', #3059, 82.00000000000000000 ) ;
#46420=EDGE_LOOP ( 'NONE', ( #27687, #72579, #45702, #17613 ) ) ;
#46433=DIRECTION ( 'NONE',  ( 0.000000000000000000, 0.3090169943749411785, 0.9510565162951556406 ) ) ;
#46459=AXIS2_PLACEMENT_3D ( 'NONE', #26664, #49593, #21024 ) ;
#46460=CARTESIAN_POINT ( 'NONE',  ( 11.99999999999999822, 71.27951684758026829, 30.41916302227139113 ) ) ;
#46464=ORIENTED_EDGE ( 'NONE', *, *, #3862, .F. ) ;
#46465=DIRECTION ( 'NONE',  ( -1.000000000000000000, -0.000000000000000000, -0.000000000000000000 ) ) ;
#46468=CYLINDRICAL_SURFACE ( 'NONE', #59808, 31.99999999999999289 ) ;
#46472=CARTESIAN_POINT ( 'NONE',  ( 11.99999999999999822, 0.000000000000000000, 0.000000000000000000 ) ) ;
#46474=DIRECTION ( 'NONE',  ( -1.000000000000000000, -0.000000000000000000, -0.000000000000000000 ) ) ;
#46479=FACE_OUTER_BOUND ( 'NONE', #59088, .T. ) ;
#46480=ORIENTED_EDGE ( 'NONE', *, *, #33882, .F. ) ;
#46497=ORIENTED_EDGE ( 'NONE', *, *, #25273, .T. ) ;
#46507=ADVANCED_FACE ( 'NONE', ( #27565 ), #44873, .T. ) ;
#46510=ORIENTED_EDGE ( 'NONE', *, *, #13077, .F. ) ;
#46515=CARTESIAN_POINT ( 'NONE',  ( 11.99999999999999822, 68.27212725128275395, -31.46837873495001503 ) ) ;
#46516=CARTESIAN_POINT ( 'NONE',  ( 11.99999999999999822, 79.10210256391397365, -21.60688246758502729 ) ) ;
#46522=ORIENTED_EDGE ( 'NONE', *, *, #2535, .T. ) ;
#46525=ORIENTED_EDGE ( 'NONE', *, *, #14015, .F. ) ;
#46541=FACE_OUTER_BOUND ( 'NONE', #9235, .T. ) ;
#46549=DIRECTION ( 'NONE',  ( 0.000000000000000000, 0.3826834323650841752, 0.9238795325112891810 ) ) ;
#46553=EDGE_LOOP ( 'NONE', ( #21824, #36144, #29987, #35910 ) ) ;
#46555=ORIENTED_EDGE ( 'NONE', *, *, #9275, .F. ) ;
#46563=CARTESIAN_POINT ( 'NONE',  ( 0.000000000000000000, 0.000000000000000000, 0.000000000000000000 ) ) ;
#46564=DIRECTION ( 'NONE',  ( 1.000000000000000000, 0.000000000000000000, 0.000000000000000000 ) ) ;
#46567=LINE ( 'NONE', #24011, #56700 ) ;
#46571=DIRECTION ( 'NONE',  ( -1.000000000000000000, -0.000000000000000000, -0.000000000000000000 ) ) ;
#46582=EDGE_CURVE ( 'NONE', #60145, #70171, #523, .T. ) ;
#46587=EDGE_CURVE ( 'NONE', #5835, #14313, #19188, .T. ) ;
#46591=EDGE_CURVE ( 'NONE', #23135, #69158, #5405, .T. ) ;
#46612=FACE_OUTER_BOUND ( 'NONE', #7557, .T. ) ;
#46617=DIRECTION ( 'NONE',  ( 0.000000000000000000, 0.2079116908177532363, -0.9781476007338069101 ) ) ;
#46624=VECTOR ( 'NONE', #8894, 1000.000000000000000 ) ;
#46625=EDGE_LOOP ( 'NONE', ( #3143, #68061, #69690, #229 ) ) ;
#46627=FACE_OUTER_BOUND ( 'NONE', #34219, .T. ) ;
#46628=VECTOR ( 'NONE', #4804, 1000.000000000000000 ) ;
#46630=ORIENTED_EDGE ( 'NONE', *, *, #41326, .T. ) ;
#46631=EDGE_CURVE ( 'NONE', #48807, #31231, #72046, .T. ) ;
#46637=ORIENTED_EDGE ( 'NONE', *, *, #72967, .F. ) ;
#46638=CARTESIAN_POINT ( 'NONE',  ( 11.99999999999999822, 60.67117009219136037, 55.16347631943064300 ) ) ;
#46644=FACE_OUTER_BOUND ( 'NONE', #67160, .T. ) ;
#46652=ORIENTED_EDGE ( 'NONE', *, *, #63511, .F. ) ;
#46654=VECTOR ( 'NONE', #47851, 1000.000000000000000 ) ;
#46656=DIRECTION ( 'NONE',  ( -1.000000000000000000, -0.000000000000000000, -0.000000000000000000 ) ) ;
#46674=CIRCLE ( 'NONE', #23873, 31.99999999999999289 ) ;
#46682=AXIS2_PLACEMENT_3D ( 'NONE', #3616, #3976, #31771 ) ;
#46683=EDGE_CURVE ( 'NONE', #66942, #50206, #28299, .T. ) ;
#46699=VECTOR ( 'NONE', #21838, 1000.000000000000000 ) ;
#46705=VECTOR ( 'NONE', #73050, 1000.000000000000000 ) ;
#46706=VECTOR ( 'NONE', #40679, 1000.000000000000000 ) ;
#46709=ORIENTED_EDGE ( 'NONE', *, *, #17344, .T. ) ;
#46712=ADVANCED_FACE ( 'NONE', ( #68550 ), #11383, .T. ) ;
#46725=ORIENTED_EDGE ( 'NONE', *, *, #4780, .F. ) ;
#46727=ORIENTED_EDGE ( 'NONE', *, *, #14693, .T. ) ;
#46739=ORIENTED_EDGE ( 'NONE', *, *, #32433, .T. ) ;
#46750=DIRECTION ( 'NONE',  ( 0.000000000000000000, 0.000000000000000000, 1.000000000000000000 ) ) ;
#46757=DIRECTION ( 'NONE',  ( -1.000000000000000000, -0.000000000000000000, 0.000000000000000000 ) ) ;
#46763=DIRECTION ( 'NONE',  ( -1.000000000000000000, -0.000000000000000000, 0.000000000000000000 ) ) ;
#46771=ORIENTED_EDGE ( 'NONE', *, *, #5513, .T. ) ;
#46772=DIRECTION ( 'NONE',  ( 0.000000000000000000, 0.000000000000000000, 1.000000000000000000 ) ) ;
#46793=CIRCLE ( 'NONE', #26388, 77.49900000000000944 ) ;
#46795=EDGE_CURVE ( 'NONE', #39724, #47808, #2377, .T. ) ;
#46796=ADVANCED_FACE ( 'NONE', ( #7602 ), #25268, .T. ) ;
#46802=VERTEX_POINT ( 'NONE', #42556 ) ;
#46816=ORIENTED_EDGE ( 'NONE', *, *, #15778, .T. ) ;
#46823=VERTEX_POINT ( 'NONE', #8711 ) ;
#46836=VECTOR ( 'NONE', #10093, 1000.000000000000000 ) ;
#46837=ADVANCED_FACE ( 'NONE', ( #13237 ), #7236, .T. ) ;
#46839=CARTESIAN_POINT ( 'NONE',  ( 0.000000000000000000, -67.80270845531921964, 46.11716303203162681 ) ) ;
#46844=VECTOR ( 'NONE', #24975, 1000.000000000000227 ) ;
#46849=CARTESIAN_POINT ( 'NONE',  ( 11.99999999999999822, 0.000000000000000000, 0.000000000000000000 ) ) ;
#46851=EDGE_CURVE ( 'NONE', #67331, #64618, #3703, .T. ) ;
#46852=CARTESIAN_POINT ( 'NONE',  ( 11.99999999999999822, -2.543863470247810010, -81.96053171279903893 ) ) ;
#46871=ORIENTED_EDGE ( 'NONE', *, *, #651, .T. ) ;
#46873=DIRECTION ( 'NONE',  ( -1.000000000000000000, 0.000000000000000000, -0.000000000000000000 ) ) ;
#46874=CIRCLE ( 'NONE', #48051, 31.99999999999998224 ) ;
#46876=ORIENTED_EDGE ( 'NONE', *, *, #61730, .F. ) ;
#46879=EDGE_CURVE ( 'NONE', #68468, #34202, #13604, .T. ) ;
#46880=DIRECTION ( 'NONE',  ( 0.000000000000000000, -0.9510565162951500895, -0.3090169943749582204 ) ) ;
#46894=AXIS2_PLACEMENT_3D ( 'NONE', #45534, #63560, #40997 ) ;
#46898=AXIS2_PLACEMENT_3D ( 'NONE', #52616, #34218, #22958 ) ;
#46914=VERTEX_POINT ( 'NONE', #33473 ) ;
#46920=LINE ( 'NONE', #65324, #3605 ) ;
#46925=DIRECTION ( 'NONE',  ( -1.000000000000000000, 0.000000000000000000, 0.000000000000000000 ) ) ;
#46926=VERTEX_POINT ( 'NONE', #61699 ) ;
#46930=CARTESIAN_POINT ( 'NONE',  ( 11.99999999999999822, -62.50329211542465657, 41.76937507738766442 ) ) ;
#46931=AXIS2_PLACEMENT_3D ( 'NONE', #6885, #58771, #46750 ) ;
#46934=DIRECTION ( 'NONE',  ( -1.000000000000000000, -0.000000000000000000, 0.000000000000000000 ) ) ;
#46937=LINE ( 'NONE', #40933, #57990 ) ;
#46938=CARTESIAN_POINT ( 'NONE',  ( 5.999999999999999112, 81.96053171279902472, 2.543863470248677316 ) ) ;
#46942=DIRECTION ( 'NONE',  ( 0.000000000000000000, 0.000000000000000000, 1.000000000000000000 ) ) ;
#46943=AXIS2_PLACEMENT_3D ( 'NONE', #69931, #30811, #19903 ) ;
#46944=EDGE_CURVE ( 'NONE', #21262, #5289, #63703, .T. ) ;
#46947=VECTOR ( 'NONE', #73527, 1000.000000000000114 ) ;
#46952=ORIENTED_EDGE ( 'NONE', *, *, #20005, .T. ) ;
#46961=VERTEX_POINT ( 'NONE', #49653 ) ;
#46963=DIRECTION ( 'NONE',  ( 0.000000000000000000, -0.5224985647159560154, 0.8526401643540879594 ) ) ;
#46964=ORIENTED_EDGE ( 'NONE', *, *, #72989, .T. ) ;
#46970=( GEOMETRIC_REPRESENTATION_CONTEXT ( 3 ) GLOBAL_UNCERTAINTY_ASSIGNED_CONTEXT ( ( #32462 ) ) GLOBAL_UNIT_ASSIGNED_CONTEXT ( ( #17078, #68211, #56183 ) ) REPRESENTATION_CONTEXT ( 'NONE', 'WORKASPACE' ) );
#46972=ORIENTED_EDGE ( 'NONE', *, *, #40513, .F. ) ;
#46974=EDGE_LOOP ( 'NONE', ( #33858, #54279, #31854, #10453 ) ) ;
#46978=AXIS2_PLACEMENT_3D ( 'NONE', #68104, #5338, #72603 ) ;
#46980=EDGE_LOOP ( 'NONE', ( #25174, #58108, #58534, #39138 ) ) ;
#46981=DIRECTION ( 'NONE',  ( 0.000000000000000000, 0.000000000000000000, 1.000000000000000000 ) ) ;
#47004=LINE ( 'NONE', #14993, #49290 ) ;
#47007=DIRECTION ( 'NONE',  ( -1.000000000000000000, 0.000000000000000000, 0.000000000000000000 ) ) ;
#47041=CIRCLE ( 'NONE', #59007, 82.00000000000000000 ) ;
#47043=EDGE_CURVE ( 'NONE', #63132, #60480, #45736, .T. ) ;
#47047=EDGE_CURVE ( 'NONE', #12401, #54007, #57689, .T. ) ;
#47052=EDGE_CURVE ( 'NONE', #50648, #62137, #50471, .T. ) ;
#47053=EDGE_CURVE ( 'NONE', #61582, #34691, #44479, .T. ) ;
#47059=ADVANCED_FACE ( 'NONE', ( #22588 ), #17683, .T. ) ;
#47071=ORIENTED_EDGE ( 'NONE', *, *, #63511, .T. ) ;
#47073=DIRECTION ( 'NONE',  ( -1.000000000000000000, 0.000000000000000000, -0.000000000000000000 ) ) ;
#47075=CARTESIAN_POINT ( 'NONE',  ( 0.000000000000000000, 65.64334221924909230, 41.19522573413756561 ) ) ;
#47077=ORIENTED_EDGE ( 'NONE', *, *, #20697, .F. ) ;
#47085=ORIENTED_EDGE ( 'NONE', *, *, #35924, .F. ) ;
#47089=LINE ( 'NONE', #18496, #54605 ) ;
#47102=CARTESIAN_POINT ( 'NONE',  ( 12.00000000000000000, 22.07842321921492612, 8.187992925817123790 ) ) ;
#47104=DIRECTION ( 'NONE',  ( -1.000000000000000000, 0.000000000000000000, 0.000000000000000000 ) ) ;
#47106=CYLINDRICAL_SURFACE ( 'NONE', #50017, 82.00000000000000000 ) ;
#47109=EDGE_CURVE ( 'NONE', #73028, #15149, #12056, .T. ) ;
#47113=CYLINDRICAL_SURFACE ( 'NONE', #33628, 31.99999999999998579 ) ;
#47123=CARTESIAN_POINT ( 'NONE',  ( 0.000000000000000000, 0.000000000000000000, 0.000000000000000000 ) ) ;
#47124=CARTESIAN_POINT ( 'NONE',  ( 15.00000000000000000, -11.95096189432312350, 23.69967320028773372 ) ) ;
#47126=ORIENTED_EDGE ( 'NONE', *, *, #50123, .F. ) ;
#47127=DIRECTION ( 'NONE',  ( -1.000000000000000000, 0.000000000000000000, 0.000000000000000000 ) ) ;
#47130=CARTESIAN_POINT ( 'NONE',  ( 0.000000000000000000, -35.91791733033525702, 68.67312586194982771 ) ) ;
#47138=DIRECTION ( 'NONE',  ( -1.000000000000000000, 0.000000000000000000, 0.000000000000000000 ) ) ;
#47152=DIRECTION ( 'NONE',  ( 0.000000000000000000, 0.000000000000000000, -1.000000000000000000 ) ) ;
#47157=ORIENTED_EDGE ( 'NONE', *, *, #54975, .F. ) ;
#47158=EDGE_LOOP ( 'NONE', ( #35041, #52037, #63198, #14997 ) ) ;
#47161=ORIENTED_EDGE ( 'NONE', *, *, #892, .T. ) ;
#47176=CARTESIAN_POINT ( 'NONE',  ( 11.99999999999999822, 0.000000000000000000, 0.000000000000000000 ) ) ;
#47178=ORIENTED_EDGE ( 'NONE', *, *, #53632, .T. ) ;
#47183=ORIENTED_EDGE ( 'NONE', *, *, #32652, .F. ) ;
#47187=EDGE_CURVE ( 'NONE', #53812, #61985, #6769, .T. ) ;
#47193=CARTESIAN_POINT ( 'NONE',  ( 11.99999999999999822, 55.20638768913760686, 51.02545421589343988 ) ) ;
#47206=ORIENTED_EDGE ( 'NONE', *, *, #6288, .T. ) ;
#47207=CARTESIAN_POINT ( 'NONE',  ( 0.000000000000000000, 0.000000000000000000, 77.49899999999999523 ) ) ;
#47219=DIRECTION ( 'NONE',  ( 0.000000000000000000, -0.9945218953682732899, 0.1045284632676548031 ) ) ;
#47220=ADVANCED_FACE ( 'NONE', ( #36081 ), #18777, .F. ) ;
#47229=EDGE_CURVE ( 'NONE', #18706, #11201, #42835, .T. ) ;
#47232=VECTOR ( 'NONE', #68680, 999.9999999999998863 ) ;
#47238=VECTOR ( 'NONE', #13395, 1000.000000000000000 ) ;
#47240=EDGE_LOOP ( 'NONE', ( #3265, #19151, #39522, #55102 ) ) ;
#47251=ADVANCED_FACE ( 'NONE', ( #24797 ), #65766, .T. ) ;
#47253=ORIENTED_EDGE ( 'NONE', *, *, #49725, .T. ) ;
#47254=ORIENTED_EDGE ( 'NONE', *, *, #39205, .T. ) ;
#47255=AXIS2_PLACEMENT_3D ( 'NONE', #16042, #10779, #38984 ) ;
#47269=DIRECTION ( 'NONE',  ( -1.000000000000000000, -0.000000000000000000, -0.000000000000000000 ) ) ;
#47270=EDGE_LOOP ( 'NONE', ( #32791, #59912, #41273, #61248 ) ) ;
#47271=DIRECTION ( 'NONE',  ( 0.000000000000000000, -0.4067366430757887730, 0.9135454576426059736 ) ) ;
#47275=VERTEX_POINT ( 'NONE', #35697 ) ;
#47283=PLANE ( 'NONE',  #15901 ) ;
#47284=CARTESIAN_POINT ( 'NONE',  ( 0.000000000000000000, 56.15606465355041621, -59.75363087400017292 ) ) ;
#47303=DIRECTION ( 'NONE',  ( 1.000000000000000000, -0.000000000000000000, -0.000000000000000000 ) ) ;
#47314=VECTOR ( 'NONE', #7285, 1000.000000000000000 ) ;
#47316=LINE ( 'NONE', #13458, #16950 ) ;
#47317=AXIS2_PLACEMENT_3D ( 'NONE', #67084, #38521, #29079 ) ;
#47325=DIRECTION ( 'NONE',  ( -1.000000000000000000, 0.000000000000000000, 0.000000000000000000 ) ) ;
#47329=CARTESIAN_POINT ( 'NONE',  ( 11.99999999999999822, -41.76937507738745836, -62.50329211542482710 ) ) ;
#47332=DIRECTION ( 'NONE',  ( -1.000000000000000000, 0.000000000000000000, -0.000000000000000000 ) ) ;
#47337=CARTESIAN_POINT ( 'NONE',  ( 11.99999999999999822, -77.19088730480518734, -6.903761155838607166 ) ) ;
#47338=ORIENTED_EDGE ( 'NONE', *, *, #60303, .F. ) ;
#47343=DIRECTION ( 'NONE',  ( -1.000000000000000000, -0.000000000000000000, 0.000000000000000000 ) ) ;
#47349=EDGE_CURVE ( 'NONE', #19214, #70942, #50220, .T. ) ;
#47351=DIRECTION ( 'NONE',  ( -1.000000000000000000, -0.000000000000000000, 0.000000000000000000 ) ) ;
#47354=VERTEX_POINT ( 'NONE', #4391 ) ;
#47356=EDGE_LOOP ( 'NONE', ( #60057, #17317, #41225, #55735 ) ) ;
#47358=EDGE_CURVE ( 'NONE', #11199, #63551, #8515, .T. ) ;
#47359=EDGE_CURVE ( 'NONE', #32129, #18143, #2551, .T. ) ;
#47379=ORIENTED_EDGE ( 'NONE', *, *, #8586, .T. ) ;
#47397=EDGE_CURVE ( 'NONE', #31904, #44373, #20257, .T. ) ;
#47400=CARTESIAN_POINT ( 'NONE',  ( 6.000000000000000000, -16.65972982744991171, 80.28980883073752750 ) ) ;
#47401=CIRCLE ( 'NONE', #14924, 31.99999999999998579 ) ;
#47417=DIRECTION ( 'NONE',  ( -1.000000000000000000, 0.000000000000000000, 0.000000000000000000 ) ) ;
#47418=ORIENTED_EDGE ( 'NONE', *, *, #65606, .T. ) ;
#47427=DIRECTION ( 'NONE',  ( 0.000000000000000000, 0.7431448254773939111, 0.6691306063588584596 ) ) ;
#47431=EDGE_LOOP ( 'NONE', ( #13631, #50848, #61780, #73525 ) ) ;
#47432=AXIS2_PLACEMENT_3D ( 'NONE', #17073, #34350, #28712 ) ;
#47437=CARTESIAN_POINT ( 'NONE',  ( 0.000000000000000000, 59.46389618802034960, -49.70050353004825894 ) ) ;
#47439=VERTEX_POINT ( 'NONE', #6958 ) ;
#47444=EDGE_CURVE ( 'NONE', #29284, #63342, #49344, .T. ) ;
#47446=VERTEX_POINT ( 'NONE', #30259 ) ;
#47450=LINE ( 'NONE', #25621, #46191 ) ;
#47451=CARTESIAN_POINT ( 'NONE',  ( 11.99999999999999822, -26.01480285779885904, 70.53064760720306481 ) ) ;
#47455=CARTESIAN_POINT ( 'NONE',  ( 0.000000000000000000, 0.000000000000000000, 0.000000000000000000 ) ) ;
#47464=CIRCLE ( 'NONE', #22241, 77.49900000000000944 ) ;
#47468=FACE_OUTER_BOUND ( 'NONE', #44662, .T. ) ;
#47485=CARTESIAN_POINT ( 'NONE',  ( 0.000000000000000000, 59.46389618801964616, 49.70050353004909738 ) ) ;
#47491=DIRECTION ( 'NONE',  ( -1.000000000000000000, 0.000000000000000000, -0.000000000000000000 ) ) ;
#47494=AXIS2_PLACEMENT_3D ( 'NONE', #38817, #61756, #32422 ) ;
#47495=CARTESIAN_POINT ( 'NONE',  ( 11.99999999999999822, 0.000000000000000000, 0.000000000000000000 ) ) ;
#47498=DIRECTION ( 'NONE',  ( -1.000000000000000000, 0.000000000000000000, -0.000000000000000000 ) ) ;
#47501=DIRECTION ( 'NONE',  ( 1.000000000000000000, 0.000000000000000000, 0.000000000000000000 ) ) ;
#47508=ORIENTED_EDGE ( 'NONE', *, *, #56037, .F. ) ;
#47510=DIRECTION ( 'NONE',  ( 0.000000000000000000, 0.3826834323650904479, -0.9238795325112865164 ) ) ;
#47511=VERTEX_POINT ( 'NONE', #6603 ) ;
#47512=DIRECTION ( 'NONE',  ( -1.000000000000000000, 0.000000000000000000, 0.000000000000000000 ) ) ;
#47522=ORIENTED_EDGE ( 'NONE', *, *, #48535, .F. ) ;
#47526=CIRCLE ( 'NONE', #13912, 31.99999999999998579 ) ;
#47527=AXIS2_PLACEMENT_3D ( 'NONE', #18156, #65145, #58757 ) ;
#47532=ORIENTED_EDGE ( 'NONE', *, *, #23089, .F. ) ;
#47535=CARTESIAN_POINT ( 'NONE',  ( 0.000000000000000000, 46.21855187248630159, 62.20884554314034176 ) ) ;
#47539=AXIS2_PLACEMENT_3D ( 'NONE', #71068, #24483, #7927 ) ;
#47543=DIRECTION ( 'NONE',  ( -1.000000000000000000, -0.000000000000000000, -0.000000000000000000 ) ) ;
#47554=DIRECTION ( 'NONE',  ( -1.000000000000000000, -0.000000000000000000, 0.000000000000000000 ) ) ;
#47563=VERTEX_POINT ( 'NONE', #69022 ) ;
#47571=ORIENTED_EDGE ( 'NONE', *, *, #9348, .F. ) ;
#47576=CYLINDRICAL_SURFACE ( 'NONE', #65350, 31.99999999999997868 ) ;
#47577=CYLINDRICAL_SURFACE ( 'NONE', #4881, 82.00000000000000000 ) ;
#47581=DIRECTION ( 'NONE',  ( -1.000000000000000000, -0.000000000000000000, 0.000000000000000000 ) ) ;
#47595=ORIENTED_EDGE ( 'NONE', *, *, #46795, .T. ) ;
#47600=ORIENTED_EDGE ( 'NONE', *, *, #28333, .F. ) ;
#47603=EDGE_CURVE ( 'NONE', #54492, #9345, #14819, .T. ) ;
#47608=LINE ( 'NONE', #2893, #14671 ) ;
#47610=VECTOR ( 'NONE', #35363, 1000.000000000000000 ) ;
#47615=EDGE_LOOP ( 'NONE', ( #11323, #65830, #51049, #71735 ) ) ;
#47617=VERTEX_POINT ( 'NONE', #71208 ) ;
#47644=EDGE_CURVE ( 'NONE', #2055, #41798, #15701, .T. ) ;
#47647=AXIS2_PLACEMENT_3D ( 'NONE', #47692, #19120, #42068 ) ;
#47650=AXIS2_PLACEMENT_3D ( 'NONE', #132, #12095, #62517 ) ;
#47668=AXIS2_PLACEMENT_3D ( 'NONE', #17978, #6699, #22517 ) ;
#47671=CARTESIAN_POINT ( 'NONE',  ( 11.99999999999999822, 76.66974797899837313, 11.30684508768366747 ) ) ;
#47677=ADVANCED_FACE ( 'NONE', ( #2105 ), #47927, .T. ) ;
#47678=DIRECTION ( 'NONE',  ( 1.000000000000000000, -0.000000000000000000, -0.000000000000000000 ) ) ;
#47679=EDGE_CURVE ( 'NONE', #12399, #17939, #31735, .T. ) ;
#47686=CYLINDRICAL_SURFACE ( 'NONE', #41610, 77.49899999999999523 ) ;
#47692=CARTESIAN_POINT ( 'NONE',  ( 0.000000000000000000, 0.000000000000000000, 0.000000000000000000 ) ) ;
#47699=ORIENTED_EDGE ( 'NONE', *, *, #42954, .F. ) ;
#47704=CARTESIAN_POINT ( 'NONE',  ( 12.00000000000000000, 18.84667830672605859, 18.68964196561243085 ) ) ;
#47709=EDGE_CURVE ( 'NONE', #13922, #9966, #6176, .T. ) ;
#47712=ADVANCED_FACE ( 'NONE', ( #11044 ), #67061, .F. ) ;
#47715=VERTEX_POINT ( 'NONE', #44521 ) ;
#47719=AXIS2_PLACEMENT_3D ( 'NONE', #35344, #17306, #29311 ) ;
#47722=DIRECTION ( 'NONE',  ( -1.000000000000000000, 0.000000000000000000, 0.000000000000000000 ) ) ;
#47725=ORIENTED_EDGE ( 'NONE', *, *, #48790, .T. ) ;
#47726=AXIS2_PLACEMENT_3D ( 'NONE', #19721, #13348, #59977 ) ;
#47732=VERTEX_POINT ( 'NONE', #4309 ) ;
#47740=DIRECTION ( 'NONE',  ( 0.000000000000000000, -0.8910065241883723397, 0.4539904997395382003 ) ) ;
#47746=DIRECTION ( 'NONE',  ( -1.000000000000000000, 0.000000000000000000, -0.000000000000000000 ) ) ;
#47750=EDGE_CURVE ( 'NONE', #70108, #36401, #59019, .T. ) ;
#47752=DIRECTION ( 'NONE',  ( -1.000000000000000000, 0.000000000000000000, 0.000000000000000000 ) ) ;
#47753=FACE_OUTER_BOUND ( 'NONE', #15559, .T. ) ;
#47758=LINE ( 'NONE', #65442, #13096 ) ;
#47766=AXIS2_PLACEMENT_3D ( 'NONE', #18666, #67680, #28850 ) ;
#47775=AXIS2_PLACEMENT_3D ( 'NONE', #45191, #10970, #15868 ) ;
#47777=ORIENTED_EDGE ( 'NONE', *, *, #49535, .F. ) ;
#47778=LINE ( 'NONE', #64713, #38302 ) ;
#47807=VERTEX_POINT ( 'NONE', #67810 ) ;
#47808=VERTEX_POINT ( 'NONE', #73806 ) ;
#47812=DIRECTION ( 'NONE',  ( -1.000000000000000000, -0.000000000000000000, -0.000000000000000000 ) ) ;
#47821=ORIENTED_EDGE ( 'NONE', *, *, #74077, .F. ) ;
#47823=ORIENTED_EDGE ( 'NONE', *, *, #18727, .T. ) ;
#47825=CARTESIAN_POINT ( 'NONE',  ( 11.99999999999999822, 54.21277698773752007, -55.38113227695726692 ) ) ;
#47826=CARTESIAN_POINT ( 'NONE',  ( 11.99999999999999822, 0.000000000000000000, 0.000000000000000000 ) ) ;
#47828=DIRECTION ( 'NONE',  ( -1.000000000000000000, 0.000000000000000000, -0.000000000000000000 ) ) ;
#47838=CIRCLE ( 'NONE', #53852, 31.99999999999998579 ) ;
#47839=DIRECTION ( 'NONE',  ( 0.000000000000000000, 0.9945218953682742891, 0.1045284632676436315 ) ) ;
#47845=CARTESIAN_POINT ( 'NONE',  ( 11.99999999999999822, -65.64334221924882229, -41.19522573413803457 ) ) ;
#47846=EDGE_LOOP ( 'NONE', ( #30212, #74264, #30610, #5824 ) ) ;
#47851=DIRECTION ( 'NONE',  ( -1.000000000000000000, 0.000000000000000000, 0.000000000000000000 ) ) ;
#47857=CIRCLE ( 'NONE', #38247, 31.99999999999999289 ) ;
#47867=DIRECTION ( 'NONE',  ( -1.000000000000000000, -0.000000000000000000, -0.000000000000000000 ) ) ;
#47873=DIRECTION ( 'NONE',  ( 1.000000000000000000, 0.000000000000000000, 0.000000000000000000 ) ) ;
#47874=CYLINDRICAL_SURFACE ( 'NONE', #66705, 31.99999999999998579 ) ;
#47883=EDGE_CURVE ( 'NONE', #48585, #36787, #3803, .T. ) ;
#47888=ORIENTED_EDGE ( 'NONE', *, *, #8772, .T. ) ;
#47889=DIRECTION ( 'NONE',  ( -1.000000000000000000, 0.000000000000000000, -0.000000000000000000 ) ) ;
#47899=ORIENTED_EDGE ( 'NONE', *, *, #61147, .F. ) ;
#47900=ORIENTED_EDGE ( 'NONE', *, *, #48225, .T. ) ;
#47911=DIRECTION ( 'NONE',  ( -1.000000000000000000, 0.000000000000000000, 0.000000000000000000 ) ) ;
#47925=CARTESIAN_POINT ( 'NONE',  ( 12.00000000000000000, -18.13022148937263012, -15.02647892043543898 ) ) ;
#47927=CYLINDRICAL_SURFACE ( 'NONE', #12099, 31.99999999999998579 ) ;
#47929=ORIENTED_EDGE ( 'NONE', *, *, #41326, .F. ) ;
#47942=CARTESIAN_POINT ( 'NONE',  ( 0.000000000000000000, -46.53671651293991118, 59.03961581697383565 ) ) ;
#47943=CARTESIAN_POINT ( 'NONE',  ( 5.999999999999999112, -77.16300072079681627, 27.74655509720641433 ) ) ;
#47945=EDGE_CURVE ( 'NONE', #44992, #4927, #17779, .T. ) ;
#47947=CARTESIAN_POINT ( 'NONE',  ( 11.99999999999999822, -12.93880638057260946, -76.41127070299286572 ) ) ;
#47952=DIRECTION ( 'NONE',  ( -1.000000000000000000, 0.000000000000000000, 0.000000000000000000 ) ) ;
#47954=EDGE_CURVE ( 'NONE', #47807, #48711, #48168, .T. ) ;
#47961=AXIS2_PLACEMENT_3D ( 'NONE', #22508, #44708, #34151 ) ;
#47964=CARTESIAN_POINT ( 'NONE',  ( 0.000000000000000000, 0.000000000000000000, 0.000000000000000000 ) ) ;
#47967=CIRCLE ( 'NONE', #1214, 31.99999999999998579 ) ;
#47969=VECTOR ( 'NONE', #15904, 1000.000000000000000 ) ;
#47973=CARTESIAN_POINT ( 'NONE',  ( 0.000000000000000000, 0.000000000000000000, 0.000000000000000000 ) ) ;
#47980=CARTESIAN_POINT ( 'NONE',  ( -10.00000000000000000, 0.000000000000000000, 0.000000000000000000 ) ) ;
#47982=CARTESIAN_POINT ( 'NONE',  ( 11.99999999999999822, 2.543863470249544623, -81.96053171279901051 ) ) ;
#47987=LINE ( 'NONE', #8120, #47238 ) ;
#47989=AXIS2_PLACEMENT_3D ( 'NONE', #3749, #60514, #38313 ) ;
#48002=AXIS2_PLACEMENT_3D ( 'NONE', #4817, #26962, #61195 ) ;
#48003=CARTESIAN_POINT ( 'NONE',  ( 0.000000000000000000, 75.11764819372149304, 29.05362095685338275 ) ) ;
#48007=DIRECTION ( 'NONE',  ( -1.000000000000000000, 0.000000000000000000, 0.000000000000000000 ) ) ;
#48008=EDGE_LOOP ( 'NONE', ( #30874, #59587, #63335, #58888 ) ) ;
#48016=CARTESIAN_POINT ( 'NONE',  ( 15.00000000000000000, -23.29833615347104470, 3.418703333116808629 ) ) ;
#48021=ORIENTED_EDGE ( 'NONE', *, *, #23857, .T. ) ;
#48038=CARTESIAN_POINT ( 'NONE',  ( 6.000000000000000000, 81.34940948281337114, 10.30890764327411446 ) ) ;
#48045=AXIS2_PLACEMENT_3D ( 'NONE', #26081, #9164, #72317 ) ;
#48051=AXIS2_PLACEMENT_3D ( 'NONE', #45379, #73548, #22056 ) ;
#48052=DIRECTION ( 'NONE',  ( 0.000000000000000000, 0.9510565162951523099, 0.3090169943749514481 ) ) ;
#48059=CARTESIAN_POINT ( 'NONE',  ( 5.999999999999999112, 68.55367621811141987, 44.99326035066079044 ) ) ;
#48068=ORIENTED_EDGE ( 'NONE', *, *, #12166, .T. ) ;
#48070=CARTESIAN_POINT ( 'NONE',  ( 0.000000000000000000, -75.11725578898470701, 2.956366410620372864 ) ) ;
#48071=VERTEX_POINT ( 'NONE', #25643 ) ;
#48072=CARTESIAN_POINT ( 'NONE',  ( 12.00000000000000000, -22.67460108101782268, -6.353146135317906840 ) ) ;
#48074=ORIENTED_EDGE ( 'NONE', *, *, #41544, .T. ) ;
#48078=ORIENTED_EDGE ( 'NONE', *, *, #54685, .T. ) ;
#48082=FACE_OUTER_BOUND ( 'NONE', #68731, .T. ) ;
#48083=ORIENTED_EDGE ( 'NONE', *, *, #24701, .T. ) ;
#48090=ORIENTED_EDGE ( 'NONE', *, *, #71051, .T. ) ;
#48100=ORIENTED_EDGE ( 'NONE', *, *, #10612, .F. ) ;
#48111=DIRECTION ( 'NONE',  ( 0.000000000000000000, 0.000000000000000000, 1.000000000000000000 ) ) ;
#48117=CARTESIAN_POINT ( 'NONE',  ( 12.00000000000000000, -10.45096189432344502, -21.10159698893425073 ) ) ;
#48125=DIRECTION ( 'NONE',  ( -1.000000000000000000, -0.000000000000000000, 0.000000000000000000 ) ) ;
#48139=DIRECTION ( 'NONE',  ( 0.000000000000000000, 0.8910065241883690090, -0.4539904997395446395 ) ) ;
#48142=CARTESIAN_POINT ( 'NONE',  ( 11.99999999999999822, -72.35432306680469594, -20.40083707022958848 ) ) ;
#48145=EDGE_CURVE ( 'NONE', #39502, #70850, #14725, .T. ) ;
#48147=EDGE_CURVE ( 'NONE', #33344, #19604, #37676, .T. ) ;
#48168=CIRCLE ( 'NONE', #54187, 77.49900000000002365 ) ;
#48179=DIRECTION ( 'NONE',  ( -1.000000000000000000, -0.000000000000000000, 0.000000000000000000 ) ) ;
#48188=VERTEX_POINT ( 'NONE', #59492 ) ;
#48193=CARTESIAN_POINT ( 'NONE',  ( 11.99999999999999822, 66.50666863322055633, -39.78640506895536078 ) ) ;
#48209=AXIS2_PLACEMENT_3D ( 'NONE', #29782, #53107, #58005 ) ;
#48216=ORIENTED_EDGE ( 'NONE', *, *, #31381, .F. ) ;
#48225=EDGE_CURVE ( 'NONE', #47275, #36497, #25283, .T. ) ;
#48231=LINE ( 'NONE', #59515, #21403 ) ;
#48234=DIRECTION ( 'NONE',  ( 0.000000000000000000, 0.8090169943749486725, -0.5877852522924713607 ) ) ;
#48243=CARTESIAN_POINT ( 'NONE',  ( 0.000000000000000000, 0.000000000000000000, 0.000000000000000000 ) ) ;
#48250=ORIENTED_EDGE ( 'NONE', *, *, #13986, .T. ) ;
#48252=CARTESIAN_POINT ( 'NONE',  ( 0.000000000000000000, -10.30890764327323161, -81.34940948281348483 ) ) ;
#48253=VERTEX_POINT ( 'NONE', #27860 ) ;
#48256=CIRCLE ( 'NONE', #69870, 82.00000000000000000 ) ;
#48260=ORIENTED_EDGE ( 'NONE', *, *, #14015, .T. ) ;
#48265=ORIENTED_EDGE ( 'NONE', *, *, #24759, .F. ) ;
#48268=DIRECTION ( 'NONE',  ( -1.000000000000000000, -0.000000000000000000, 0.000000000000000000 ) ) ;
#48272=ORIENTED_EDGE ( 'NONE', *, *, #28181, .T. ) ;
#48273=CYLINDRICAL_SURFACE ( 'NONE', #21459, 31.99999999999997868 ) ;
#48274=CIRCLE ( 'NONE', #48333, 31.99999999999998224 ) ;
#48276=CIRCLE ( 'NONE', #5096, 31.99999999999998579 ) ;
#48282=ADVANCED_FACE ( 'NONE', ( #4959 ), #38408, .T. ) ;
#48292=DIRECTION ( 'NONE',  ( -1.000000000000000000, 0.000000000000000000, 0.000000000000000000 ) ) ;
#48298=ORIENTED_EDGE ( 'NONE', *, *, #7576, .F. ) ;
#48299=CARTESIAN_POINT ( 'NONE',  ( 11.99999999999999822, -65.59268652807183742, -36.72794159290312166 ) ) ;
#48305=LINE ( 'NONE', #38132, #43559 ) ;
#48310=ORIENTED_EDGE ( 'NONE', *, *, #1685, .F. ) ;
#48313=CARTESIAN_POINT ( 'NONE',  ( 0.000000000000000000, 75.54627589209970040, -17.28742895386005785 ) ) ;
#48315=FACE_OUTER_BOUND ( 'NONE', #50458, .T. ) ;
#48320=CARTESIAN_POINT ( 'NONE',  ( 0.000000000000000000, 0.000000000000000000, 0.000000000000000000 ) ) ;
#48321=DIRECTION ( 'NONE',  ( 0.000000000000000000, 0.000000000000000000, 1.000000000000000000 ) ) ;
#48324=EDGE_CURVE ( 'NONE', #11454, #73113, #68093, .T. ) ;
#48333=AXIS2_PLACEMENT_3D ( 'NONE', #10434, #61579, #16452 ) ;
#48336=VERTEX_POINT ( 'NONE', #72592 ) ;
#48342=CYLINDRICAL_SURFACE ( 'NONE', #39631, 31.99999999999998579 ) ;
#48347=CARTESIAN_POINT ( 'NONE',  ( 0.000000000000000000, 0.000000000000000000, 0.000000000000000000 ) ) ;
#48356=ORIENTED_EDGE ( 'NONE', *, *, #23770, .F. ) ;
#48358=EDGE_CURVE ( 'NONE', #65292, #64440, #27103, .T. ) ;
#48370=ORIENTED_EDGE ( 'NONE', *, *, #16647, .F. ) ;
#48372=CIRCLE ( 'NONE', #24338, 31.99999999999998934 ) ;
#48377=EDGE_CURVE ( 'NONE', #47617, #69188, #36247, .T. ) ;
#48378=LINE ( 'NONE', #28403, #4883 ) ;
#48384=ORIENTED_EDGE ( 'NONE', *, *, #65606, .F. ) ;
#48390=ORIENTED_EDGE ( 'NONE', *, *, #71770, .F. ) ;
#48393=ORIENTED_EDGE ( 'NONE', *, *, #70005, .T. ) ;
#48397=EDGE_CURVE ( 'NONE', #62137, #13883, #69205, .T. ) ;
#48404=CARTESIAN_POINT ( 'NONE',  ( 0.000000000000000000, -36.72794159290197769, -65.59268652807249111 ) ) ;
#48407=ADVANCED_FACE ( 'NONE', ( #6432 ), #22985, .T. ) ;
#48417=VECTOR ( 'NONE', #35314, 1000.000000000000000 ) ;
#48418=DIRECTION ( 'NONE',  ( 0.000000000000000000, 0.1045284632676449221, -0.9945218953682741780 ) ) ;
#48419=VERTEX_POINT ( 'NONE', #16965 ) ;
#48421=CARTESIAN_POINT ( 'NONE',  ( 0.000000000000000000, 58.39081064771751528, 50.95692526931350841 ) ) ;
#48425=CIRCLE ( 'NONE', #49599, 82.00000000000000000 ) ;
#48433=CARTESIAN_POINT ( 'NONE',  ( 0.000000000000000000, 77.16300072079698680, -27.74655509720590985 ) ) ;
#48439=CARTESIAN_POINT ( 'NONE',  ( 15.00000000000000000, -14.54903810567644484, 22.19967320028775504 ) ) ;
#48461=AXIS2_PLACEMENT_3D ( 'NONE', #3138, #10590, #37703 ) ;
#48469=ADVANCED_FACE ( 'NONE', ( #62472 ), #62852, .F. ) ;
#48476=CYLINDRICAL_SURFACE ( 'NONE', #5964, 31.99999999999998579 ) ;
#48482=ORIENTED_EDGE ( 'NONE', *, *, #68133, .T. ) ;
#48484=DIRECTION ( 'NONE',  ( -1.000000000000000000, 0.000000000000000000, 0.000000000000000000 ) ) ;
#48485=CARTESIAN_POINT ( 'NONE',  ( 0.000000000000000000, 2.543863470249533965, -81.96053171279901051 ) ) ;
#48486=CARTESIAN_POINT ( 'NONE',  ( 15.00000000000000000, -23.29833615347104470, 3.418703333116808629 ) ) ;
#48491=EDGE_CURVE ( 'NONE', #55710, #69920, #2651, .T. ) ;
#48492=CYLINDRICAL_SURFACE ( 'NONE', #46943, 31.99999999999998579 ) ;
#48498=CARTESIAN_POINT ( 'NONE',  ( 0.000000000000000000, -71.87247863392384772, -39.47590169984923136 ) ) ;
#48502=AXIS2_PLACEMENT_3D ( 'NONE', #41081, #45983, #46343 ) ;
#48503=DIRECTION ( 'NONE',  ( -1.000000000000000000, 0.000000000000000000, -0.000000000000000000 ) ) ;
#48520=AXIS2_PLACEMENT_3D ( 'NONE', #14224, #72477, #71730 ) ;
#48525=EDGE_CURVE ( 'NONE', #14207, #1863, #33835, .T. ) ;
#48532=AXIS2_PLACEMENT_3D ( 'NONE', #27036, #49969, #21393 ) ;
#48535=EDGE_CURVE ( 'NONE', #29646, #20333, #73208, .T. ) ;
#48536=ORIENTED_EDGE ( 'NONE', *, *, #10951, .T. ) ;
#48543=CYLINDRICAL_SURFACE ( 'NONE', #23815, 31.99999999999998579 ) ;
#48549=CIRCLE ( 'NONE', #16146, 77.49900000000002365 ) ;
#48555=ORIENTED_EDGE ( 'NONE', *, *, #21311, .T. ) ;
#48560=ORIENTED_EDGE ( 'NONE', *, *, #23621, .F. ) ;
#48562=DIRECTION ( 'NONE',  ( 0.000000000000000000, -0.1564344650402381687, 0.9876883405951365491 ) ) ;
#48564=EDGE_CURVE ( 'NONE', #64009, #43683, #21714, .T. ) ;
#48566=EDGE_CURVE ( 'NONE', #67235, #73160, #53056, .T. ) ;
#48573=DIRECTION ( 'NONE',  ( 0.000000000000000000, 0.8660254037844370423, -0.5000000000000029976 ) ) ;
#48576=CARTESIAN_POINT ( 'NONE',  ( 11.99999999999999822, 40.65526001592611749, 71.21200624218811015 ) ) ;
#48581=EDGE_LOOP ( 'NONE', ( #27843, #67127, #9895, #14522 ) ) ;
#48583=EDGE_CURVE ( 'NONE', #43856, #70465, #48274, .T. ) ;
#48584=AXIS2_PLACEMENT_3D ( 'NONE', #27742, #17208, #45800 ) ;
#48585=VERTEX_POINT ( 'NONE', #50653 ) ;
#48590=DIRECTION ( 'NONE',  ( -1.000000000000000000, -0.000000000000000000, 0.000000000000000000 ) ) ;
#48595=AXIS2_PLACEMENT_3D ( 'NONE', #13954, #59847, #8335 ) ;
#48597=FACE_OUTER_BOUND ( 'NONE', #11809, .T. ) ;
#48608=FACE_OUTER_BOUND ( 'NONE', #64561, .T. ) ;
#48618=LINE ( 'NONE', #2435, #27623 ) ;
#48621=ADVANCED_FACE ( 'NONE', ( #73953 ), #67956, .F. ) ;
#48622=FACE_OUTER_BOUND ( 'NONE', #7829, .T. ) ;
#48624=EDGE_CURVE ( 'NONE', #1062, #71384, #45933, .T. ) ;
#48630=ORIENTED_EDGE ( 'NONE', *, *, #42886, .T. ) ;
#48638=ADVANCED_FACE ( 'NONE', ( #10816 ), #56687, .T. ) ;
#48640=CARTESIAN_POINT ( 'NONE',  ( 0.000000000000000000, 27.74655509720669500, 77.16300072079670258 ) ) ;
#48646=AXIS2_PLACEMENT_3D ( 'NONE', #57040, #5550, #68696 ) ;
#48651=DIRECTION ( 'NONE',  ( -1.000000000000000000, 0.000000000000000000, 0.000000000000000000 ) ) ;
#48654=CARTESIAN_POINT ( 'NONE',  ( 15.00000000000000000, -19.89357724624986545, 12.59942793731086219 ) ) ;
#48669=DIRECTION ( 'NONE',  ( -1.000000000000000000, 0.000000000000000000, 0.000000000000000000 ) ) ;
#48674=DIRECTION ( 'NONE',  ( 0.000000000000000000, -0.3090169943749461745, 0.9510565162951539753 ) ) ;
#48680=DIRECTION ( 'NONE',  ( -1.000000000000000000, -0.000000000000000000, -0.000000000000000000 ) ) ;
#48682=CARTESIAN_POINT ( 'NONE',  ( 12.00000000000000000, 23.59884966291521735, -12.14883922797262805 ) ) ;
#48685=FACE_OUTER_BOUND ( 'NONE', #64078, .T. ) ;
#48687=CARTESIAN_POINT ( 'NONE',  ( 11.99999999999999822, -41.76106447765443619, -62.50884508063471401 ) ) ;
#48693=ORIENTED_EDGE ( 'NONE', *, *, #74004, .T. ) ;
#48700=ORIENTED_EDGE ( 'NONE', *, *, #27209, .F. ) ;
#48701=EDGE_CURVE ( 'NONE', #3672, #26361, #55526, .T. ) ;
#48706=ORIENTED_EDGE ( 'NONE', *, *, #33971, .T. ) ;
#48709=CARTESIAN_POINT ( 'NONE',  ( 12.00000000000000000, 16.61724383029361718, -20.69703378468927113 ) ) ;
#48711=VERTEX_POINT ( 'NONE', #29936 ) ;
#48719=DIRECTION ( 'NONE',  ( -1.000000000000000000, -0.000000000000000000, -0.000000000000000000 ) ) ;
#48721=VERTEX_POINT ( 'NONE', #29560 ) ;
#48722=ORIENTED_EDGE ( 'NONE', *, *, #13483, .T. ) ;
#48729=CARTESIAN_POINT ( 'NONE',  ( 12.00000000000000000, 5.835314593368777558, 22.81335362449846471 ) ) ;
#48731=DIRECTION ( 'NONE',  ( 1.000000000000000000, 0.000000000000000000, -0.000000000000000000 ) ) ;
#48746=CARTESIAN_POINT ( 'NONE',  ( 11.99999999999999822, 81.90746397400387480, 3.894527615418187150 ) ) ;
#48750=ORIENTED_EDGE ( 'NONE', *, *, #64934, .T. ) ;
#48756=FACE_OUTER_BOUND ( 'NONE', #8073, .T. ) ;
#48759=CARTESIAN_POINT ( 'NONE',  ( 11.99999999999999822, 0.000000000000000000, 0.000000000000000000 ) ) ;
#48764=CARTESIAN_POINT ( 'NONE',  ( 0.000000000000000000, -8.830959090341869100, -74.65491531819127147 ) ) ;
#48770=CARTESIAN_POINT ( 'NONE',  ( 12.00000000000000000, 23.49999999999999645, 1.499999999999995337 ) ) ;
#48773=CARTESIAN_POINT ( 'NONE',  ( 11.99999999999999822, -24.73286445877655382, -73.44644590900085745 ) ) ;
#48775=EDGE_CURVE ( 'NONE', #20377, #19673, #42333, .T. ) ;
#48781=EDGE_CURVE ( 'NONE', #17154, #30036, #23946, .T. ) ;
#48790=EDGE_CURVE ( 'NONE', #51135, #62092, #11539, .T. ) ;
#48795=ORIENTED_EDGE ( 'NONE', *, *, #7877, .T. ) ;
#48796=DIRECTION ( 'NONE',  ( 1.000000000000000000, 0.000000000000000000, 0.000000000000000000 ) ) ;
#48807=VERTEX_POINT ( 'NONE', #53255 ) ;
#48817=VERTEX_POINT ( 'NONE', #65649 ) ;
#48818=DIRECTION ( 'NONE',  ( 1.000000000000000000, 0.000000000000000000, 0.000000000000000000 ) ) ;
#48820=CARTESIAN_POINT ( 'NONE',  ( 11.99999999999999822, 35.91791733033570466, -68.67312586194960033 ) ) ;
#48830=ORIENTED_EDGE ( 'NONE', *, *, #58324, .T. ) ;
#48846=DIRECTION ( 'NONE',  ( 0.000000000000000000, 0.000000000000000000, 1.000000000000000000 ) ) ;
#48848=FACE_OUTER_BOUND ( 'NONE', #1627, .T. ) ;
#48849=AXIS2_PLACEMENT_3D ( 'NONE', #25602, #25250, #2720 ) ;
#48854=DIRECTION ( 'NONE',  ( -1.000000000000000000, 0.000000000000000000, 0.000000000000000000 ) ) ;
#48861=CARTESIAN_POINT ( 'NONE',  ( 0.000000000000000000, 80.55351364060611274, -15.33399622253397609 ) ) ;
#48864=EDGE_CURVE ( 'NONE', #42164, #8127, #13760, .T. ) ;
#48873=EDGE_CURVE ( 'NONE', #13281, #10460, #47608, .T. ) ;
#48874=AXIS2_PLACEMENT_3D ( 'NONE', #50833, #73762, #39570 ) ;
#48889=ORIENTED_EDGE ( 'NONE', *, *, #43666, .T. ) ;
#48898=CYLINDRICAL_SURFACE ( 'NONE', #58095, 31.99999999999998579 ) ;
#48901=CARTESIAN_POINT ( 'NONE',  ( 0.000000000000000000, 3.894527615417885169, 81.90746397400390322 ) ) ;
#48909=EDGE_LOOP ( 'NONE', ( #6597, #9545, #37931, #63536 ) ) ;
#48915=VERTEX_POINT ( 'NONE', #43101 ) ;
#48918=LINE ( 'NONE', #67612, #26964 ) ;
#48926=DIRECTION ( 'NONE',  ( 0.000000000000000000, 0.2079116908177532086, -0.9781476007338069101 ) ) ;
#48928=DIRECTION ( 'NONE',  ( 0.000000000000000000, 0.000000000000000000, 1.000000000000000000 ) ) ;
#48948=CARTESIAN_POINT ( 'NONE',  ( 15.00000000000000000, 5.835314593368777558, 22.81335362449846471 ) ) ;
#48958=CARTESIAN_POINT ( 'NONE',  ( 11.99999999999999822, 0.000000000000000000, 0.000000000000000000 ) ) ;
#48960=FACE_OUTER_BOUND ( 'NONE', #26700, .T. ) ;
#48961=CYLINDRICAL_SURFACE ( 'NONE', #28620, 82.00000000000000000 ) ;
#48965=CARTESIAN_POINT ( 'NONE',  ( 11.99999999999999822, 0.000000000000000000, 0.000000000000000000 ) ) ;
#48966=CARTESIAN_POINT ( 'NONE',  ( -10.00000000000000000, 0.000000000000000000, 0.000000000000000000 ) ) ;
#48971=ORIENTED_EDGE ( 'NONE', *, *, #4147, .F. ) ;
#48979=ORIENTED_EDGE ( 'NONE', *, *, #45201, .F. ) ;
#48980=ORIENTED_EDGE ( 'NONE', *, *, #3818, .T. ) ;
#48988=CARTESIAN_POINT ( 'NONE',  ( 0.000000000000000000, -0.8261519478436571973, 77.49459641780886443 ) ) ;
#48993=LINE ( 'NONE', #20438, #29980 ) ;
#49003=CARTESIAN_POINT ( 'NONE',  ( 11.99999999999999822, -36.72794159290197769, -65.59268652807249111 ) ) ;
#49004=AXIS2_PLACEMENT_3D ( 'NONE', #25654, #48590, #53856 ) ;
#49005=DIRECTION ( 'NONE',  ( -1.000000000000000000, -0.000000000000000000, 0.000000000000000000 ) ) ;
#49013=ORIENTED_EDGE ( 'NONE', *, *, #65529, .T. ) ;
#49019=DIRECTION ( 'NONE',  ( -1.000000000000000000, -0.000000000000000000, -0.000000000000000000 ) ) ;
#49024=AXIS2_PLACEMENT_3D ( 'NONE', #33624, #47867, #29450 ) ;
#49027=ORIENTED_EDGE ( 'NONE', *, *, #69684, .F. ) ;
#49032=AXIS2_PLACEMENT_3D ( 'NONE', #36209, #1315, #53508 ) ;
#49035=DIRECTION ( 'NONE',  ( 0.000000000000000000, -0.3090169943749349613, -0.9510565162951576390 ) ) ;
#49049=DIRECTION ( 'NONE',  ( 0.000000000000000000, 0.9238795325112851842, 0.3826834323650937786 ) ) ;
#49052=DIRECTION ( 'NONE',  ( 0.000000000000000000, 0.000000000000000000, 1.000000000000000000 ) ) ;
#49054=CARTESIAN_POINT ( 'NONE',  ( 11.99999999999999822, -51.03279382321048985, -55.19960302592120627 ) ) ;
#49055=EDGE_CURVE ( 'NONE', #24686, #35768, #7545, .T. ) ;
#49057=AXIS2_PLACEMENT_3D ( 'NONE', #43776, #38114, #41094 ) ;
#49067=VECTOR ( 'NONE', #37248, 1000.000000000000000 ) ;
#49072=( NAMED_UNIT ( * ) SI_UNIT ( $, .STERADIAN. ) SOLID_ANGLE_UNIT ( ) );
#49074=DIRECTION ( 'NONE',  ( 0.000000000000000000, 0.000000000000000000, 1.000000000000000000 ) ) ;
#49079=AXIS2_PLACEMENT_3D ( 'NONE', #14608, #61232, #27360 ) ;
#49114=CIRCLE ( 'NONE', #27483, 82.00000000000000000 ) ;
#49116=CARTESIAN_POINT ( 'NONE',  ( 5.999999999999999112, 55.16347631943042984, 60.67117009219155932 ) ) ;
#49130=ORIENTED_EDGE ( 'NONE', *, *, #20978, .F. ) ;
#49133=AXIS2_PLACEMENT_3D ( 'NONE', #61546, #72065, #20575 ) ;
#49139=DIRECTION ( 'NONE',  ( 0.000000000000000000, 0.000000000000000000, 1.000000000000000000 ) ) ;
#49142=DIRECTION ( 'NONE',  ( -1.000000000000000000, -0.000000000000000000, -0.000000000000000000 ) ) ;
#49147=VECTOR ( 'NONE', #10137, 1000.000000000000114 ) ;
#49148=DIRECTION ( 'NONE',  ( 1.000000000000000000, 0.000000000000000000, -0.000000000000000000 ) ) ;
#49149=CARTESIAN_POINT ( 'NONE',  ( 15.00000000000000000, 0.000000000000000000, 0.000000000000000000 ) ) ;
#49150=EDGE_CURVE ( 'NONE', #61762, #20511, #45977, .T. ) ;
#49155=CARTESIAN_POINT ( 'NONE',  ( 15.00000000000000000, -26.23277895567245466, 4.042438405570107918 ) ) ;
#49165=AXIS2_PLACEMENT_3D ( 'NONE', #38244, #15691, #14945 ) ;
#49173=LINE ( 'NONE', #20608, #23206 ) ;
#49174=CARTESIAN_POINT ( 'NONE',  ( 15.00000000000000000, -19.89357724625003598, -12.59942793731059041 ) ) ;
#49183=CIRCLE ( 'NONE', #44434, 82.00000000000000000 ) ;
#49199=ORIENTED_EDGE ( 'NONE', *, *, #52726, .T. ) ;
#49202=EDGE_LOOP ( 'NONE', ( #72398, #27351, #30856, #51881 ) ) ;
#49207=ORIENTED_EDGE ( 'NONE', *, *, #24508, .T. ) ;
#49209=CARTESIAN_POINT ( 'NONE',  ( 11.99999999999999822, -75.54627589209931671, -17.28742895386162814 ) ) ;
#49211=CARTESIAN_POINT ( 'NONE',  ( 11.99999999999999822, -74.65491531819124305, 8.830959090342128448 ) ) ;
#49216=DIRECTION ( 'NONE',  ( -0.000000000000000000, 0.5000000000000019984, 0.8660254037844374864 ) ) ;
#49219=EDGE_CURVE ( 'NONE', #73384, #20377, #50137, .T. ) ;
#49222=DIRECTION ( 'NONE',  ( -1.000000000000000000, 0.000000000000000000, 0.000000000000000000 ) ) ;
#49228=DIRECTION ( 'NONE',  ( -1.000000000000000000, 0.000000000000000000, 0.000000000000000000 ) ) ;
#49230=DIRECTION ( 'NONE',  ( 0.000000000000000000, 0.000000000000000000, 1.000000000000000000 ) ) ;
#49243=VECTOR ( 'NONE', #21071, 1000.000000000000000 ) ;
#49247=EDGE_CURVE ( 'NONE', #30413, #33465, #59172, .T. ) ;
#49248=ORIENTED_EDGE ( 'NONE', *, *, #55925, .T. ) ;
#49249=DIRECTION ( 'NONE',  ( -1.000000000000000000, -0.000000000000000000, 0.000000000000000000 ) ) ;
#49252=CARTESIAN_POINT ( 'NONE',  ( 11.99999999999999822, 77.49459641780886443, 0.8261519478433866359 ) ) ;
#49253=VECTOR ( 'NONE', #35295, 1000.000000000000000 ) ;
#49256=CARTESIAN_POINT ( 'NONE',  ( 0.000000000000000000, 0.000000000000000000, 0.000000000000000000 ) ) ;
#49258=ORIENTED_EDGE ( 'NONE', *, *, #64197, .F. ) ;
#49264=CIRCLE ( 'NONE', #72079, 31.99999999999998579 ) ;
#49268=CIRCLE ( 'NONE', #61305, 77.49900000000000944 ) ;
#49273=DIRECTION ( 'NONE',  ( -1.000000000000000000, 0.000000000000000000, -0.000000000000000000 ) ) ;
#49276=FACE_OUTER_BOUND ( 'NONE', #9520, .T. ) ;
#49290=VECTOR ( 'NONE', #13518, 1000.000000000000000 ) ;
#49295=DIRECTION ( 'NONE',  ( -1.000000000000000000, 0.000000000000000000, 0.000000000000000000 ) ) ;
#49310=ORIENTED_EDGE ( 'NONE', *, *, #19832, .F. ) ;
#49320=EDGE_CURVE ( 'NONE', #69188, #11199, #71166, .T. ) ;
#49321=CARTESIAN_POINT ( 'NONE',  ( 0.000000000000000000, 8.830959090343430518, -74.65491531819107252 ) ) ;
#49323=AXIS2_PLACEMENT_3D ( 'NONE', #67432, #21179, #44131 ) ;
#49328=DIRECTION ( 'NONE',  ( 0.000000000000000000, 0.000000000000000000, 1.000000000000000000 ) ) ;
#49342=FACE_OUTER_BOUND ( 'NONE', #868, .T. ) ;
#49344=CIRCLE ( 'NONE', #63759, 82.00000000000000000 ) ;
#49345=AXIS2_PLACEMENT_3D ( 'NONE', #21362, #45072, #44320 ) ;
#49355=VERTEX_POINT ( 'NONE', #68940 ) ;
#49359=ORIENTED_EDGE ( 'NONE', *, *, #62108, .T. ) ;
#49363=LINE ( 'NONE', #65564, #13095 ) ;
#49364=ORIENTED_EDGE ( 'NONE', *, *, #23625, .F. ) ;
#49371=ORIENTED_EDGE ( 'NONE', *, *, #52550, .F. ) ;
#49387=ADVANCED_FACE ( 'NONE', ( #57283 ), #63304, .T. ) ;
#49388=FACE_OUTER_BOUND ( 'NONE', #65601, .T. ) ;
#49389=EDGE_CURVE ( 'NONE', #43677, #54048, #62954, .T. ) ;
#49392=CIRCLE ( 'NONE', #32590, 77.49899999999998101 ) ;
#49398=FACE_OUTER_BOUND ( 'NONE', #50380, .T. ) ;
#49407=ORIENTED_EDGE ( 'NONE', *, *, #9855, .T. ) ;
#49417=DIRECTION ( 'NONE',  ( 0.000000000000000000, 0.000000000000000000, 1.000000000000000000 ) ) ;
#49429=DIRECTION ( 'NONE',  ( -1.000000000000000000, 0.000000000000000000, 0.000000000000000000 ) ) ;
#49438=DIRECTION ( 'NONE',  ( 0.000000000000000000, -0.8910065241883626808, -0.4539904997395569075 ) ) ;
#49439=CIRCLE ( 'NONE', #27807, 77.49900000000000944 ) ;
#49441=ORIENTED_EDGE ( 'NONE', *, *, #31473, .F. ) ;
#49445=CIRCLE ( 'NONE', #71058, 82.00000000000000000 ) ;
#49449=VECTOR ( 'NONE', #72234, 1000.000000000000000 ) ;
#49460=EDGE_CURVE ( 'NONE', #41863, #4461, #70292, .T. ) ;
#49464=ORIENTED_EDGE ( 'NONE', *, *, #57955, .F. ) ;
#49472=DIRECTION ( 'NONE',  ( 0.000000000000000000, 0.4539904997395478037, -0.8910065241883673437 ) ) ;
#49476=ORIENTED_EDGE ( 'NONE', *, *, #67295, .F. ) ;
#49478=ORIENTED_EDGE ( 'NONE', *, *, #22776, .F. ) ;
#49494=EDGE_CURVE ( 'NONE', #12380, #72968, #21920, .T. ) ;
#49496=EDGE_CURVE ( 'NONE', #18859, #50834, #61643, .T. ) ;
#49501=ORIENTED_EDGE ( 'NONE', *, *, #67635, .T. ) ;
#49503=ORIENTED_EDGE ( 'NONE', *, *, #44994, .T. ) ;
#49521=PLANE ( 'NONE',  #58783 ) ;
#49523=ORIENTED_EDGE ( 'NONE', *, *, #71691, .F. ) ;
#49529=DIRECTION ( 'NONE',  ( 0.000000000000000000, -0.07845909572785224328, 0.9969173337331274087 ) ) ;
#49535=EDGE_CURVE ( 'NONE', #1681, #11576, #48425, .T. ) ;
#49540=DIRECTION ( 'NONE',  ( -1.000000000000000000, 0.000000000000000000, 0.000000000000000000 ) ) ;
#49554=CARTESIAN_POINT ( 'NONE',  ( 0.000000000000000000, -74.65491531819111515, -8.830959090343204920 ) ) ;
#49558=DIRECTION ( 'NONE',  ( 1.000000000000000000, -0.000000000000000000, -0.000000000000000000 ) ) ;
#49561=DIRECTION ( 'NONE',  ( -1.000000000000000000, -0.000000000000000000, 0.000000000000000000 ) ) ;
#49565=EDGE_LOOP ( 'NONE', ( #17465, #68627, #60187, #10190 ) ) ;
#49568=DIRECTION ( 'NONE',  ( -1.000000000000000000, 0.000000000000000000, 0.000000000000000000 ) ) ;
#49586=DIRECTION ( 'NONE',  ( -1.000000000000000000, -0.000000000000000000, -0.000000000000000000 ) ) ;
#49588=CARTESIAN_POINT ( 'NONE',  ( 15.00000000000000000, 23.49999999999999645, -1.500000000000003997 ) ) ;
#49593=DIRECTION ( 'NONE',  ( -1.000000000000000000, 0.000000000000000000, 0.000000000000000000 ) ) ;
#49599=AXIS2_PLACEMENT_3D ( 'NONE', #55241, #38324, #9751 ) ;
#49602=AXIS2_PLACEMENT_3D ( 'NONE', #6710, #36013, #59321 ) ;
#49605=ADVANCED_FACE ( 'NONE', ( #33796 ), #11, .T. ) ;
#49622=ADVANCED_FACE ( 'NONE', ( #67271 ), #68011, .T. ) ;
#49623=VERTEX_POINT ( 'NONE', #43809 ) ;
#49638=EDGE_LOOP ( 'NONE', ( #5924, #27746, #57800, #27630 ) ) ;
#49645=CIRCLE ( 'NONE', #44845, 82.00000000000000000 ) ;
#49648=AXIS2_PLACEMENT_3D ( 'NONE', #68678, #73182, #45381 ) ;
#49653=CARTESIAN_POINT ( 'NONE',  ( 0.000000000000000000, 77.32052557432849937, -5.256550761632002633 ) ) ;
#49661=ORIENTED_EDGE ( 'NONE', *, *, #57531, .T. ) ;
#49663=DIRECTION ( 'NONE',  ( 0.000000000000000000, 0.000000000000000000, 1.000000000000000000 ) ) ;
#49669=DIRECTION ( 'NONE',  ( -1.000000000000000000, 0.000000000000000000, -0.000000000000000000 ) ) ;
#49676=DIRECTION ( 'NONE',  ( -1.000000000000000000, 0.000000000000000000, 0.000000000000000000 ) ) ;
#49678=CARTESIAN_POINT ( 'NONE',  ( 11.99999999999999822, -81.34940948281344220, 10.30890764327355491 ) ) ;
#49680=AXIS2_PLACEMENT_3D ( 'NONE', #9943, #20854, #66726 ) ;
#49685=AXIS2_PLACEMENT_3D ( 'NONE', #18847, #24867, #53807 ) ;
#49686=DIRECTION ( 'NONE',  ( -1.000000000000000000, -0.000000000000000000, -0.000000000000000000 ) ) ;
#49689=CARTESIAN_POINT ( 'NONE',  ( 11.99999999999999822, 14.66109333815564852, -73.73191006444555740 ) ) ;
#49694=CYLINDRICAL_SURFACE ( 'NONE', #27449, 31.99999999999998579 ) ;
#49700=LINE ( 'NONE', #31310, #2330 ) ;
#49705=FACE_OUTER_BOUND ( 'NONE', #6998, .T. ) ;
#49707=DIRECTION ( 'NONE',  ( 1.000000000000000000, -0.000000000000000000, 0.000000000000000000 ) ) ;
#49709=ORIENTED_EDGE ( 'NONE', *, *, #7381, .T. ) ;
#49714=CIRCLE ( 'NONE', #67720, 31.99999999999998579 ) ;
#49725=EDGE_CURVE ( 'NONE', #29672, #59759, #1113, .T. ) ;
#49729=EDGE_CURVE ( 'NONE', #33851, #18122, #68846, .T. ) ;
#49731=ORIENTED_EDGE ( 'NONE', *, *, #74116, .T. ) ;
#49732=ORIENTED_EDGE ( 'NONE', *, *, #30687, .T. ) ;
#49736=EDGE_LOOP ( 'NONE', ( #26475, #37292, #36784, #40698 ) ) ;
#49748=EDGE_CURVE ( 'NONE', #68450, #60009, #40022, .T. ) ;
#49753=ORIENTED_EDGE ( 'NONE', *, *, #55605, .F. ) ;
#49765=DIRECTION ( 'NONE',  ( -1.000000000000000000, -0.000000000000000000, -0.000000000000000000 ) ) ;
#49766=ORIENTED_EDGE ( 'NONE', *, *, #24140, .F. ) ;
#49771=DIRECTION ( 'NONE',  ( 0.000000000000000000, 0.07845909572783797692, 0.9969173337331285190 ) ) ;
#49792=VERTEX_POINT ( 'NONE', #1844 ) ;
#49799=ADVANCED_FACE ( 'NONE', ( #7447 ), #69134, .T. ) ;
#49810=AXIS2_PLACEMENT_3D ( 'NONE', #48966, #30934, #38440 ) ;
#49813=AXIS2_PLACEMENT_3D ( 'NONE', #42395, #60800, #30723 ) ;
#49814=EDGE_CURVE ( 'NONE', #72105, #10184, #26788, .T. ) ;
#49820=DIRECTION ( 'NONE',  ( 0.000000000000000000, -0.8660254037844432595, -0.4999999999999920064 ) ) ;
#49832=AXIS2_PLACEMENT_3D ( 'NONE', #14469, #19729, #2858 ) ;
#49842=EDGE_LOOP ( 'NONE', ( #12102, #26271, #2477, #48560 ) ) ;
#49849=CARTESIAN_POINT ( 'NONE',  ( 0.000000000000000000, 0.000000000000000000, 0.000000000000000000 ) ) ;
#49852=ORIENTED_EDGE ( 'NONE', *, *, #72816, .T. ) ;
#49856=VERTEX_POINT ( 'NONE', #64230 ) ;
#49857=CYLINDRICAL_SURFACE ( 'NONE', #61213, 31.99999999999998579 ) ;
#49858=DIRECTION ( 'NONE',  ( 0.000000000000000000, 0.5877852522924708056, -0.8090169943749491166 ) ) ;
#49859=CARTESIAN_POINT ( 'NONE',  ( 11.99999999999999822, 0.000000000000000000, 0.000000000000000000 ) ) ;
#49861=ORIENTED_EDGE ( 'NONE', *, *, #39213, .F. ) ;
#49882=ORIENTED_EDGE ( 'NONE', *, *, #61306, .F. ) ;
#49885=FACE_OUTER_BOUND ( 'NONE', #72730, .T. ) ;
#49886=ADVANCED_FACE ( 'NONE', ( #69848 ), #35278, .T. ) ;
#49890=ORIENTED_EDGE ( 'NONE', *, *, #6862, .T. ) ;
#49895=EDGE_CURVE ( 'NONE', #8127, #44775, #58104, .T. ) ;
#49910=CARTESIAN_POINT ( 'NONE',  ( 0.000000000000000000, -14.66109333815410487, -73.73191006444587003 ) ) ;
#49914=DIRECTION ( 'NONE',  ( 1.000000000000000000, 0.000000000000000000, 0.000000000000000000 ) ) ;
#49920=ORIENTED_EDGE ( 'NONE', *, *, #35132, .F. ) ;
#49929=ORIENTED_EDGE ( 'NONE', *, *, #65007, .F. ) ;
#49934=VERTEX_POINT ( 'NONE', #72068 ) ;
#49942=ORIENTED_EDGE ( 'NONE', *, *, #67240, .T. ) ;
#49943=CARTESIAN_POINT ( 'NONE',  ( 0.000000000000000000, 0.000000000000000000, 0.000000000000000000 ) ) ;
#49945=CARTESIAN_POINT ( 'NONE',  ( 11.99999999999999822, 58.39081064771751528, 50.95692526931350841 ) ) ;
#49953=CARTESIAN_POINT ( 'NONE',  ( 11.99999999999999822, 50.23322058963442061, -64.81221759200288091 ) ) ;
#49957=EDGE_CURVE ( 'NONE', #38652, #50748, #49645, .T. ) ;
#49962=CYLINDRICAL_SURFACE ( 'NONE', #40705, 31.99999999999998579 ) ;
#49969=DIRECTION ( 'NONE',  ( -0.000000000000000000, 0.8660254037844432595, 0.4999999999999921729 ) ) ;
#49988=CARTESIAN_POINT ( 'NONE',  ( 0.000000000000000000, -44.99326035066101781, 68.55367621811126355 ) ) ;
#50000=ORIENTED_EDGE ( 'NONE', *, *, #43666, .F. ) ;
#50009=AXIS2_PLACEMENT_3D ( 'NONE', #12419, #5691, #52273 ) ;
#50014=DIRECTION ( 'NONE',  ( 0.000000000000000000, 0.000000000000000000, 1.000000000000000000 ) ) ;
#50016=ORIENTED_EDGE ( 'NONE', *, *, #14693, .F. ) ;
#50017=AXIS2_PLACEMENT_3D ( 'NONE', #64397, #14360, #2756 ) ;
#50035=DIRECTION ( 'NONE',  ( -1.000000000000000000, 0.000000000000000000, -0.000000000000000000 ) ) ;
#50044=CIRCLE ( 'NONE', #71677, 77.49899999999999523 ) ;
#50050=EDGE_LOOP ( 'NONE', ( #30789, #47532, #74045, #20718 ) ) ;
#50052=EDGE_CURVE ( 'NONE', #64186, #47715, #2856, .T. ) ;
#50053=EDGE_CURVE ( 'NONE', #26486, #69892, #33314, .T. ) ;
#50062=VECTOR ( 'NONE', #48484, 1000.000000000000000 ) ;
#50067=ORIENTED_EDGE ( 'NONE', *, *, #47679, .T. ) ;
#50069=DIRECTION ( 'NONE',  ( -1.000000000000000000, 0.000000000000000000, -0.000000000000000000 ) ) ;
#50070=AXIS2_PLACEMENT_3D ( 'NONE', #18428, #30439, #58658 ) ;
#50077=VERTEX_POINT ( 'NONE', #15679 ) ;
#50079=CARTESIAN_POINT ( 'NONE',  ( 11.99999999999999822, 0.000000000000000000, 0.000000000000000000 ) ) ;
#50082=ORIENTED_EDGE ( 'NONE', *, *, #39464, .T. ) ;
#50087=EDGE_LOOP ( 'NONE', ( #22462, #35449, #62337, #59038 ) ) ;
#50092=ORIENTED_EDGE ( 'NONE', *, *, #44414, .T. ) ;
#50106=PLANE ( 'NONE',  #36771 ) ;
#50115=DIRECTION ( 'NONE',  ( -1.000000000000000000, -0.000000000000000000, 0.000000000000000000 ) ) ;
#50123=EDGE_CURVE ( 'NONE', #4061, #53067, #16419, .T. ) ;
#50124=DIRECTION ( 'NONE',  ( -1.000000000000000000, -0.000000000000000000, -0.000000000000000000 ) ) ;
#50137=LINE ( 'NONE', #38133, #17157 ) ;
#50148=AXIS2_PLACEMENT_3D ( 'NONE', #68318, #16811, #5547 ) ;
#50149=CARTESIAN_POINT ( 'NONE',  ( 11.99999999999999822, 31.47745569255140552, 68.26794271651274926 ) ) ;
#50153=VECTOR ( 'NONE', #18538, 1000.000000000000000 ) ;
#50154=EDGE_CURVE ( 'NONE', #13883, #11059, #7650, .T. ) ;
#50156=ADVANCED_FACE ( 'NONE', ( #68301 ), #55531, .T. ) ;
#50159=CYLINDRICAL_SURFACE ( 'NONE', #53058, 31.99999999999998579 ) ;
#50175=DIRECTION ( 'NONE',  ( 0.000000000000000000, 0.1564344650402312020, -0.9876883405951376593 ) ) ;
#50184=CARTESIAN_POINT ( 'NONE',  ( 15.00000000000000000, 23.59884966291538078, 12.14883922797231008 ) ) ;
#50188=ORIENTED_EDGE ( 'NONE', *, *, #9071, .T. ) ;
#50192=CIRCLE ( 'NONE', #67064, 31.99999999999998579 ) ;
#50196=VECTOR ( 'NONE', #32920, 1000.000000000000000 ) ;
#50201=VECTOR ( 'NONE', #69946, 1000.000000000000000 ) ;
#50206=VERTEX_POINT ( 'NONE', #16796 ) ;
#50214=EDGE_CURVE ( 'NONE', #22824, #24493, #45753, .T. ) ;
#50215=DIRECTION ( 'NONE',  ( -1.000000000000000000, 0.000000000000000000, -0.000000000000000000 ) ) ;
#50220=LINE ( 'NONE', #3014, #46947 ) ;
#50221=DIRECTION ( 'NONE',  ( -1.000000000000000000, 0.000000000000000000, 0.000000000000000000 ) ) ;
#50236=AXIS2_PLACEMENT_3D ( 'NONE', #29374, #52316, #39940 ) ;
#50238=EDGE_CURVE ( 'NONE', #46961, #51872, #28038, .T. ) ;
#50240=AXIS2_PLACEMENT_3D ( 'NONE', #56832, #5337, #35002 ) ;
#50244=CARTESIAN_POINT ( 'NONE',  ( 11.99999999999999822, 0.000000000000000000, 0.000000000000000000 ) ) ;
#50246=CYLINDRICAL_SURFACE ( 'NONE', #11250, 31.99999999999998579 ) ;
#50258=DIRECTION ( 'NONE',  ( -1.000000000000000000, -0.000000000000000000, 0.000000000000000000 ) ) ;
#50259=CIRCLE ( 'NONE', #7068, 31.99999999999998579 ) ;
#50263=EDGE_CURVE ( 'NONE', #54483, #29284, #32858, .T. ) ;
#50264=ORIENTED_EDGE ( 'NONE', *, *, #12889, .F. ) ;
#50275=CARTESIAN_POINT ( 'NONE',  ( 11.99999999999999822, 0.000000000000000000, 0.000000000000000000 ) ) ;
#50277=DIRECTION ( 'NONE',  ( 0.000000000000000000, -0.6494480483301739993, -0.7604059656000391465 ) ) ;
#50279=DIRECTION ( 'NONE',  ( 1.000000000000000000, -0.000000000000000000, -0.000000000000000000 ) ) ;
#50286=EDGE_LOOP ( 'NONE', ( #63371, #6997, #45048, #43314 ) ) ;
#50290=CIRCLE ( 'NONE', #44357, 31.99999999999998579 ) ;
#50292=DIRECTION ( 'NONE',  ( 0.000000000000000000, -0.7071067811865535679, 0.7071067811865414665 ) ) ;
#50299=FACE_OUTER_BOUND ( 'NONE', #30030, .T. ) ;
#50302=ORIENTED_EDGE ( 'NONE', *, *, #11687, .T. ) ;
#50304=LINE ( 'NONE', #33013, #4082 ) ;
#50305=CIRCLE ( 'NONE', #5909, 31.99999999999998579 ) ;
#50310=DIRECTION ( 'NONE',  ( 0.000000000000000000, -0.8660254037844421493, -0.4999999999999939493 ) ) ;
#50311=CIRCLE ( 'NONE', #70689, 31.99999999999998579 ) ;
#50312=AXIS2_PLACEMENT_3D ( 'NONE', #61526, #54764, #20170 ) ;
#50320=ADVANCED_FACE ( 'NONE', ( #41945 ), #70481, .F. ) ;
#50321=ORIENTED_EDGE ( 'NONE', *, *, #10518, .T. ) ;
#50322=CARTESIAN_POINT ( 'NONE',  ( 11.99999999999999822, -20.41045688087772092, -72.35160999960838524 ) ) ;
#50325=VERTEX_POINT ( 'NONE', #35918 ) ;
#50328=ORIENTED_EDGE ( 'NONE', *, *, #55997, .T. ) ;
#50329=DIRECTION ( 'NONE',  ( 0.000000000000000000, 0.4067366430757887730, -0.9135454576426059736 ) ) ;
#50343=CARTESIAN_POINT ( 'NONE',  ( 15.00000000000000000, -4.261787119645322974, -26.19803753235774835 ) ) ;
#50349=VECTOR ( 'NONE', #30893, 1000.000000000000000 ) ;
#50352=ADVANCED_FACE ( 'NONE', ( #23911 ), #69764, .T. ) ;
#50355=AXIS2_PLACEMENT_3D ( 'NONE', #54438, #26598, #65726 ) ;
#50363=VECTOR ( 'NONE', #11851, 1000.000000000000000 ) ;
#50367=ORIENTED_EDGE ( 'NONE', *, *, #35146, .T. ) ;
#50370=ORIENTED_EDGE ( 'NONE', *, *, #37379, .T. ) ;
#50380=EDGE_LOOP ( 'NONE', ( #39607, #52434, #56771, #46356 ) ) ;
#50396=DIRECTION ( 'NONE',  ( -1.000000000000000000, -0.000000000000000000, -0.000000000000000000 ) ) ;
#50398=ORIENTED_EDGE ( 'NONE', *, *, #61567, .F. ) ;
#50399=ADVANCED_FACE ( 'NONE', ( #17524 ), #47576, .T. ) ;
#50409=DIRECTION ( 'NONE',  ( -1.000000000000000000, -0.000000000000000000, -0.000000000000000000 ) ) ;
#50412=VERTEX_POINT ( 'NONE', #8472 ) ;
#50414=FACE_OUTER_BOUND ( 'NONE', #22101, .T. ) ;
#50417=AXIS2_PLACEMENT_3D ( 'NONE', #37861, #61164, #15283 ) ;
#50419=LINE ( 'NONE', #44799, #4346 ) ;
#50421=DIRECTION ( 'NONE',  ( -1.000000000000000000, 0.000000000000000000, 0.000000000000000000 ) ) ;
#50427=CIRCLE ( 'NONE', #28811, 31.99999999999998579 ) ;
#50437=DIRECTION ( 'NONE',  ( -1.000000000000000000, -0.000000000000000000, -0.000000000000000000 ) ) ;
#50440=ADVANCED_FACE ( 'NONE', ( #48685 ), #2506, .T. ) ;
#50441=LINE ( 'NONE', #66003, #34628 ) ;
#50452=AXIS2_PLACEMENT_3D ( 'NONE', #8178, #52941, #31104 ) ;
#50457=CARTESIAN_POINT ( 'NONE',  ( 11.99999999999999822, 0.000000000000000000, 0.000000000000000000 ) ) ;
#50458=EDGE_LOOP ( 'NONE', ( #9881, #5759, #12103, #63716 ) ) ;
#50459=CARTESIAN_POINT ( 'NONE',  ( 11.99999999999999822, 0.8261519478441983200, -77.49459641780885022 ) ) ;
#50461=VERTEX_POINT ( 'NONE', #36661 ) ;
#50468=ORIENTED_EDGE ( 'NONE', *, *, #63771, .F. ) ;
#50471=CIRCLE ( 'NONE', #26490, 77.49899999999999523 ) ;
#50473=ORIENTED_EDGE ( 'NONE', *, *, #31999, .F. ) ;
#50475=EDGE_CURVE ( 'NONE', #31594, #1097, #20104, .T. ) ;
#50485=ORIENTED_EDGE ( 'NONE', *, *, #58819, .F. ) ;
#50492=DIRECTION ( 'NONE',  ( -1.000000000000000000, -0.000000000000000000, -0.000000000000000000 ) ) ;
#50494=LINE ( 'NONE', #39228, #7719 ) ;
#50497=LINE ( 'NONE', #62160, #36018 ) ;
#50500=ORIENTED_EDGE ( 'NONE', *, *, #17080, .F. ) ;
#50507=DIRECTION ( 'NONE',  ( -1.000000000000000000, 0.000000000000000000, -0.000000000000000000 ) ) ;
#50508=DIRECTION ( 'NONE',  ( -1.000000000000000000, -0.000000000000000000, -0.000000000000000000 ) ) ;
#50511=DIRECTION ( 'NONE',  ( 0.000000000000000000, 0.6494480483301793283, 0.7604059656000345946 ) ) ;
#50512=DIRECTION ( 'NONE',  ( -1.000000000000000000, -0.000000000000000000, 0.000000000000000000 ) ) ;
#50522=FACE_OUTER_BOUND ( 'NONE', #21084, .T. ) ;
#50523=DIRECTION ( 'NONE',  ( 0.000000000000000000, 0.000000000000000000, -1.000000000000000000 ) ) ;
#50533=AXIS2_PLACEMENT_3D ( 'NONE', #6057, #6770, #11657 ) ;
#50538=VECTOR ( 'NONE', #28906, 1000.000000000000000 ) ;
#50550=LINE ( 'NONE', #66385, #11840 ) ;
#50552=CARTESIAN_POINT ( 'NONE',  ( 11.99999999999999822, -64.81221759200380461, 50.23322058963326242 ) ) ;
#50555=AXIS2_PLACEMENT_3D ( 'NONE', #3200, #65972, #37398 ) ;
#50564=ORIENTED_EDGE ( 'NONE', *, *, #73040, .T. ) ;
#50570=EDGE_CURVE ( 'NONE', #29646, #36497, #31681, .T. ) ;
#50572=ORIENTED_EDGE ( 'NONE', *, *, #51999, .F. ) ;
#50577=CARTESIAN_POINT ( 'NONE',  ( 0.000000000000000000, 0.000000000000000000, 0.000000000000000000 ) ) ;
#50579=AXIS2_PLACEMENT_3D ( 'NONE', #9948, #38532, #61468 ) ;
#50585=EDGE_LOOP ( 'NONE', ( #49861, #47126, #41641, #32612 ) ) ;
#50598=ORIENTED_EDGE ( 'NONE', *, *, #6117, .T. ) ;
#50607=EDGE_CURVE ( 'NONE', #10745, #9630, #67755, .T. ) ;
#50610=EDGE_LOOP ( 'NONE', ( #29011, #73010 ) ) ;
#50622=CARTESIAN_POINT ( 'NONE',  ( 11.99999999999999822, 59.46389618801966037, 49.70050353004911159 ) ) ;
#50625=FACE_OUTER_BOUND ( 'NONE', #28956, .T. ) ;
#50638=ORIENTED_EDGE ( 'NONE', *, *, #43480, .F. ) ;
#50640=CARTESIAN_POINT ( 'NONE',  ( 15.00000000000000000, 14.60985201121703980, -18.46759930825707841 ) ) ;
#50641=CARTESIAN_POINT ( 'NONE',  ( 6.000000000000000000, 29.01471420065563933, 76.69515212746026123 ) ) ;
#50642=ADVANCED_FACE ( 'NONE', ( #66723 ), #38145, .T. ) ;
#50648=VERTEX_POINT ( 'NONE', #61080 ) ;
#50651=CIRCLE ( 'NONE', #33618, 31.99999999999997868 ) ;
#50653=CARTESIAN_POINT ( 'NONE',  ( 11.99999999999999822, -59.46389618801999433, 49.70050353004867816 ) ) ;
#50658=EDGE_LOOP ( 'NONE', ( #22925, #9079, #31956, #30519 ) ) ;
#50682=DIRECTION ( 'NONE',  ( -1.000000000000000000, 0.000000000000000000, 0.000000000000000000 ) ) ;
#50687=DIRECTION ( 'NONE',  ( -1.000000000000000000, 0.000000000000000000, 0.000000000000000000 ) ) ;
#50688=VECTOR ( 'NONE', #35952, 1000.000000000000000 ) ;
#50690=VECTOR ( 'NONE', #64848, 1000.000000000000000 ) ;
#50696=ADVANCED_FACE ( 'NONE', ( #21207 ), #44159, .F. ) ;
#50703=PLANE ( 'NONE',  #56038 ) ;
#50705=DIRECTION ( 'NONE',  ( -1.000000000000000000, 0.000000000000000000, 0.000000000000000000 ) ) ;
#50707=FACE_OUTER_BOUND ( 'NONE', #31907, .T. ) ;
#50710=DIRECTION ( 'NONE',  ( -1.000000000000000000, -0.000000000000000000, -0.000000000000000000 ) ) ;
#50711=DIRECTION ( 'NONE',  ( -1.000000000000000000, 0.000000000000000000, 0.000000000000000000 ) ) ;
#50724=CIRCLE ( 'NONE', #14714, 77.49899999999999523 ) ;
#50732=AXIS2_PLACEMENT_3D ( 'NONE', #3579, #32484, #50523 ) ;
#50733=AXIS2_PLACEMENT_3D ( 'NONE', #42861, #41738, #42129 ) ;
#50748=VERTEX_POINT ( 'NONE', #1309 ) ;
#50773=CARTESIAN_POINT ( 'NONE',  ( 11.99999999999999822, 0.000000000000000000, 0.000000000000000000 ) ) ;
#50776=VERTEX_POINT ( 'NONE', #17798 ) ;
#50777=DIRECTION ( 'NONE',  ( 0.000000000000000000, -0.9510565162951503115, 0.3090169943749573878 ) ) ;
#50779=ORIENTED_EDGE ( 'NONE', *, *, #53622, .F. ) ;
#50790=DIRECTION ( 'NONE',  ( -1.000000000000000000, 0.000000000000000000, -0.000000000000000000 ) ) ;
#50793=CARTESIAN_POINT ( 'NONE',  ( 15.00000000000000000, 18.84667830672579569, -18.68964196561269375 ) ) ;
#50803=DIRECTION ( 'NONE',  ( -1.000000000000000000, 0.000000000000000000, 0.000000000000000000 ) ) ;
#50810=VERTEX_POINT ( 'NONE', #57297 ) ;
#50821=DIRECTION ( 'NONE',  ( 0.000000000000000000, -0.3826834323650969427, 0.9238795325112837409 ) ) ;
#50833=CARTESIAN_POINT ( 'NONE',  ( 15.00000000000000000, 0.000000000000000000, 0.000000000000000000 ) ) ;
#50834=VERTEX_POINT ( 'NONE', #562 ) ;
#50836=LINE ( 'NONE', #44095, #60998 ) ;
#50844=CYLINDRICAL_SURFACE ( 'NONE', #4763, 31.99999999999998579 ) ;
#50846=EDGE_CURVE ( 'NONE', #24130, #8991, #29440, .T. ) ;
#50848=ORIENTED_EDGE ( 'NONE', *, *, #72333, .F. ) ;
#50853=CIRCLE ( 'NONE', #71290, 31.99999999999998224 ) ;
#50854=ORIENTED_EDGE ( 'NONE', *, *, #32044, .F. ) ;
#50855=ORIENTED_EDGE ( 'NONE', *, *, #17836, .T. ) ;
#50857=ORIENTED_EDGE ( 'NONE', *, *, #59736, .T. ) ;
#50863=CARTESIAN_POINT ( 'NONE',  ( 11.99999999999999822, -36.73666225445845157, -65.58780272294114866 ) ) ;
#50865=CARTESIAN_POINT ( 'NONE',  ( 0.000000000000000000, 0.000000000000000000, 0.000000000000000000 ) ) ;
#50870=ORIENTED_EDGE ( 'NONE', *, *, #16049, .F. ) ;
#50875=DIRECTION ( 'NONE',  ( 0.000000000000000000, -0.9510565162951502005, -0.3090169943749581094 ) ) ;
#50891=DIRECTION ( 'NONE',  ( 0.000000000000000000, -0.9876883405951359940, -0.1564344650402420545 ) ) ;
#50905=DIRECTION ( 'NONE',  ( 0.000000000000000000, 0.9876883405951383255, -0.1564344650402276216 ) ) ;
#50915=CYLINDRICAL_SURFACE ( 'NONE', #8629, 77.49899999999999523 ) ;
#50916=ORIENTED_EDGE ( 'NONE', *, *, #45070, .F. ) ;
#50920=EDGE_CURVE ( 'NONE', #53249, #42793, #55623, .T. ) ;
#50923=ORIENTED_EDGE ( 'NONE', *, *, #48873, .T. ) ;
#50924=CIRCLE ( 'NONE', #12499, 31.99999999999998934 ) ;
#50925=CARTESIAN_POINT ( 'NONE',  ( 11.99999999999999822, -70.53064760720336324, 26.01480285779810231 ) ) ;
#50929=ORIENTED_EDGE ( 'NONE', *, *, #72418, .T. ) ;
#50930=VECTOR ( 'NONE', #2419, 1000.000000000000000 ) ;
#50931=CARTESIAN_POINT ( 'NONE',  ( 11.99999999999999822, 0.000000000000000000, 0.000000000000000000 ) ) ;
#50932=VECTOR ( 'NONE', #43296, 999.9999999999998863 ) ;
#50933=ORIENTED_EDGE ( 'NONE', *, *, #70082, .T. ) ;
#50938=EDGE_CURVE ( 'NONE', #68378, #72362, #53364, .T. ) ;
#50939=ORIENTED_EDGE ( 'NONE', *, *, #10342, .F. ) ;
#50948=VERTEX_POINT ( 'NONE', #36205 ) ;
#50956=CARTESIAN_POINT ( 'NONE',  ( 0.000000000000000000, 0.000000000000000000, 0.000000000000000000 ) ) ;
#50973=VECTOR ( 'NONE', #28487, 1000.000000000000000 ) ;
#50974=DIRECTION ( 'NONE',  ( -1.000000000000000000, -0.000000000000000000, -0.000000000000000000 ) ) ;
#50976=DIRECTION ( 'NONE',  ( 0.000000000000000000, -0.5877852522924689183, 0.8090169943749504489 ) ) ;
#50986=CARTESIAN_POINT ( 'NONE',  ( 12.00000000000000000, 16.83928648764945635, 16.46020748918027010 ) ) ;
#50987=DIRECTION ( 'NONE',  ( 0.000000000000000000, 0.000000000000000000, 1.000000000000000000 ) ) ;
#50999=CARTESIAN_POINT ( 'NONE',  ( 0.000000000000000000, 71.91182617369230456, -28.89263327155667938 ) ) ;
#51011=LINE ( 'NONE', #68686, #68637 ) ;
#51021=EDGE_CURVE ( 'NONE', #6219, #1606, #14942, .T. ) ;
#51029=DIRECTION ( 'NONE',  ( -1.000000000000000000, 0.000000000000000000, -0.000000000000000000 ) ) ;
#51030=DIRECTION ( 'NONE',  ( 0.000000000000000000, 0.000000000000000000, -1.000000000000000000 ) ) ;
#51032=DIRECTION ( 'NONE',  ( -1.000000000000000000, -0.000000000000000000, -0.000000000000000000 ) ) ;
#51038=FACE_OUTER_BOUND ( 'NONE', #18233, .T. ) ;
#51049=ORIENTED_EDGE ( 'NONE', *, *, #61687, .T. ) ;
#51055=CIRCLE ( 'NONE', #43880, 31.99999999999998579 ) ;
#51056=ORIENTED_EDGE ( 'NONE', *, *, #27326, .T. ) ;
#51058=FACE_OUTER_BOUND ( 'NONE', #25495, .T. ) ;
#51078=DIRECTION ( 'NONE',  ( 0.000000000000000000, -0.1045284632676558301, -0.9945218953682731788 ) ) ;
#51086=DIRECTION ( 'NONE',  ( 0.000000000000000000, 0.000000000000000000, 1.000000000000000000 ) ) ;
#51089=DIRECTION ( 'NONE',  ( -1.000000000000000000, -0.000000000000000000, -0.000000000000000000 ) ) ;
#51098=CYLINDRICAL_SURFACE ( 'NONE', #66574, 31.99999999999998579 ) ;
#51109=EDGE_CURVE ( 'NONE', #12392, #65491, #24553, .T. ) ;
#51114=AXIS2_PLACEMENT_3D ( 'NONE', #28424, #1014, #64137 ) ;
#51115=ORIENTED_EDGE ( 'NONE', *, *, #917, .F. ) ;
#51116=ADVANCED_FACE ( 'NONE', ( #21489 ), #22250, .T. ) ;
#51117=CARTESIAN_POINT ( 'NONE',  ( 11.99999999999999822, 0.000000000000000000, 0.000000000000000000 ) ) ;
#51130=EDGE_LOOP ( 'NONE', ( #22025, #8445, #66068, #27500 ) ) ;
#51134=DIRECTION ( 'NONE',  ( 0.000000000000000000, 0.000000000000000000, 1.000000000000000000 ) ) ;
#51135=VERTEX_POINT ( 'NONE', #67365 ) ;
#51154=AXIS2_PLACEMENT_3D ( 'NONE', #56909, #50507, #22694 ) ;
#51159=EDGE_CURVE ( 'NONE', #2154, #31895, #6805, .T. ) ;
#51160=DIRECTION ( 'NONE',  ( -1.000000000000000000, -0.000000000000000000, -0.000000000000000000 ) ) ;
#51164=DIRECTION ( 'NONE',  ( 0.000000000000000000, 0.000000000000000000, 1.000000000000000000 ) ) ;
#51171=CARTESIAN_POINT ( 'NONE',  ( 11.99999999999999822, -75.11764819372145041, -2.946379043147127064 ) ) ;
#51172=AXIS2_PLACEMENT_3D ( 'NONE', #6793, #51912, #18081 ) ;
#51175=ORIENTED_EDGE ( 'NONE', *, *, #35638, .T. ) ;
#51179=CARTESIAN_POINT ( 'NONE',  ( 0.000000000000000000, -55.19960302592029677, -51.03279382321147750 ) ) ;
#51218=EDGE_LOOP ( 'NONE', ( #66139, #32572, #47077, #26985 ) ) ;
#51233=CARTESIAN_POINT ( 'NONE',  ( 0.000000000000000000, 54.21277698773675979, 55.38113227695801299 ) ) ;
#51234=DIRECTION ( 'NONE',  ( 0.000000000000000000, -0.2079116908177533474, 0.9781476007338069101 ) ) ;
#51243=ORIENTED_EDGE ( 'NONE', *, *, #27863, .T. ) ;
#51245=CARTESIAN_POINT ( 'NONE',  ( 11.99999999999999822, -76.66974797899830207, -11.30684508768420571 ) ) ;
#51250=CARTESIAN_POINT ( 'NONE',  ( -10.00000000000000000, 0.000000000000000000, 0.000000000000000000 ) ) ;
#51251=CARTESIAN_POINT ( 'NONE',  ( 0.000000000000000000, -73.44644590900043113, -24.73286445877782924 ) ) ;
#51255=ORIENTED_EDGE ( 'NONE', *, *, #15867, .F. ) ;
#51258=DIRECTION ( 'NONE',  ( 0.000000000000000000, -0.9969173337331271867, -0.07845909572785571273 ) ) ;
#51274=CARTESIAN_POINT ( 'NONE',  ( 11.99999999999999822, 0.000000000000000000, 0.000000000000000000 ) ) ;
#51283=ORIENTED_EDGE ( 'NONE', *, *, #61518, .F. ) ;
#51288=EDGE_CURVE ( 'NONE', #43739, #27052, #13549, .T. ) ;
#51297=ORIENTED_EDGE ( 'NONE', *, *, #51109, .T. ) ;
#51298=CARTESIAN_POINT ( 'NONE',  ( 6.000000000000000000, 80.55351364060611274, -15.33399622253396899 ) ) ;
#51299=ORIENTED_EDGE ( 'NONE', *, *, #46249, .F. ) ;
#51300=ORIENTED_EDGE ( 'NONE', *, *, #31480, .T. ) ;
#51303=VERTEX_POINT ( 'NONE', #71055 ) ;
#51309=VECTOR ( 'NONE', #50310, 1000.000000000000000 ) ;
#51331=ORIENTED_EDGE ( 'NONE', *, *, #32942, .F. ) ;
#51335=EDGE_CURVE ( 'NONE', #3018, #27662, #42419, .T. ) ;
#51336=LINE ( 'NONE', #68275, #12191 ) ;
#51345=EDGE_LOOP ( 'NONE', ( #61565, #33921, #26620, #70639 ) ) ;
#51349=LINE ( 'NONE', #17148, #2500 ) ;
#51354=EDGE_CURVE ( 'NONE', #32448, #41826, #11245, .T. ) ;
#51355=EDGE_LOOP ( 'NONE', ( #55328, #63258, #50000, #70221 ) ) ;
#51356=CYLINDRICAL_SURFACE ( 'NONE', #33065, 31.99999999999998579 ) ;
#51358=CARTESIAN_POINT ( 'NONE',  ( 0.000000000000000000, -81.50828551894234408, 8.966570791700414489 ) ) ;
#51360=CARTESIAN_POINT ( 'NONE',  ( 11.99999999999999822, 76.41127070299273782, 12.93880638057342836 ) ) ;
#51368=AXIS2_PLACEMENT_3D ( 'NONE', #67965, #67220, #39775 ) ;
#51370=AXIS2_PLACEMENT_3D ( 'NONE', #63054, #52110, #45005 ) ;
#51373=ORIENTED_EDGE ( 'NONE', *, *, #54571, .T. ) ;
#51374=CARTESIAN_POINT ( 'NONE',  ( 11.99999999999999822, 59.03961581697399907, 46.53671651293969802 ) ) ;
#51376=AXIS2_PLACEMENT_3D ( 'NONE', #71962, #55049, #2848 ) ;
#51385=AXIS2_PLACEMENT_3D ( 'NONE', #39043, #73238, #67610 ) ;
#51389=AXIS2_PLACEMENT_3D ( 'NONE', #2410, #47491, #42231 ) ;
#51391=CARTESIAN_POINT ( 'NONE',  ( 11.99999999999999822, 0.000000000000000000, 77.49899999999999523 ) ) ;
#51392=DIRECTION ( 'NONE',  ( 0.000000000000000000, 0.000000000000000000, 1.000000000000000000 ) ) ;
#51394=DIRECTION ( 'NONE',  ( 0.000000000000000000, 0.000000000000000000, 1.000000000000000000 ) ) ;
#51410=ADVANCED_FACE ( 'NONE', ( #18811 ), #41751, .T. ) ;
#51414=DIRECTION ( 'NONE',  ( -1.000000000000000000, 0.000000000000000000, 0.000000000000000000 ) ) ;
#51423=CIRCLE ( 'NONE', #31021, 77.49899999999999523 ) ;
#51434=FACE_BOUND ( 'NONE', #50585, .T. ) ;
#51435=ORIENTED_EDGE ( 'NONE', *, *, #74205, .T. ) ;
#51444=CARTESIAN_POINT ( 'NONE',  ( 12.00000000000000000, -3.948201729842355068, -23.21447184625292692 ) ) ;
#51447=DIRECTION ( 'NONE',  ( 0.000000000000000000, -0.9510565162951544194, -0.3090169943749450643 ) ) ;
#51453=FACE_OUTER_BOUND ( 'NONE', #25416, .T. ) ;
#51458=EDGE_CURVE ( 'NONE', #25082, #17154, #36454, .T. ) ;
#51463=DIRECTION ( 'NONE',  ( 0.000000000000000000, 0.6494480483301793283, 0.7604059656000345946 ) ) ;
#51464=EDGE_CURVE ( 'NONE', #24628, #52585, #67649, .T. ) ;
#51465=CARTESIAN_POINT ( 'NONE',  ( 0.000000000000000000, -12.93880638057369659, 76.41127070299266677 ) ) ;
#51466=LINE ( 'NONE', #57859, #9752 ) ;
#51472=AXIS2_PLACEMENT_3D ( 'NONE', #18947, #59189, #31707 ) ;
#51473=DIRECTION ( 'NONE',  ( 1.000000000000000000, -0.000000000000000000, 0.000000000000000000 ) ) ;
#51485=CARTESIAN_POINT ( 'NONE',  ( 11.99999999999999822, 18.89407956138362010, -75.16055320797013906 ) ) ;
#51494=ORIENTED_EDGE ( 'NONE', *, *, #6731, .F. ) ;
#51500=ADVANCED_FACE ( 'NONE', ( #40107 ), #63061, .T. ) ;
#51505=CIRCLE ( 'NONE', #53871, 31.99999999999998934 ) ;
#51509=ORIENTED_EDGE ( 'NONE', *, *, #52108, .T. ) ;
#51510=MECHANICAL_DESIGN_GEOMETRIC_PRESENTATION_REPRESENTATION('',(#20266),#71890);
#51511=CARTESIAN_POINT ( 'NONE',  ( 0.000000000000000000, 80.28980883073781172, -16.65972982744850128 ) ) ;
#51514=ORIENTED_EDGE ( 'NONE', *, *, #3779, .T. ) ;
#51523=VECTOR ( 'NONE', #37298, 1000.000000000000114 ) ;
#51526=FACE_OUTER_BOUND ( 'NONE', #14486, .T. ) ;
#51530=VERTEX_POINT ( 'NONE', #54884 ) ;
#51534=DIRECTION ( 'NONE',  ( 0.000000000000000000, -0.7431448254773878048, 0.6691306063588654540 ) ) ;
#51562=AXIS2_PLACEMENT_3D ( 'NONE', #68343, #964, #30230 ) ;
#51571=VERTEX_POINT ( 'NONE', #73558 ) ;
#51574=ORIENTED_EDGE ( 'NONE', *, *, #31396, .F. ) ;
#51579=EDGE_CURVE ( 'NONE', #18566, #63634, #66182, .T. ) ;
#51580=CYLINDRICAL_SURFACE ( 'NONE', #47650, 31.99999999999998579 ) ;
#51582=ORIENTED_EDGE ( 'NONE', *, *, #20360, .F. ) ;
#51586=ORIENTED_EDGE ( 'NONE', *, *, #9424, .T. ) ;
#51596=DIRECTION ( 'NONE',  ( 0.000000000000000000, 0.000000000000000000, -1.000000000000000000 ) ) ;
#51605=VECTOR ( 'NONE', #51612, 1000.000000000000000 ) ;
#51611=CARTESIAN_POINT ( 'NONE',  ( 15.00000000000000000, 16.83928648764922542, -16.46020748918050458 ) ) ;
#51612=DIRECTION ( 'NONE',  ( 1.000000000000000000, -0.000000000000000000, 0.000000000000000000 ) ) ;
#51614=CIRCLE ( 'NONE', #40785, 31.99999999999998579 ) ;
#51622=LINE ( 'NONE', #47102, #37152 ) ;
#51623=DIRECTION ( 'NONE',  ( -1.000000000000000000, -0.000000000000000000, -0.000000000000000000 ) ) ;
#51625=CARTESIAN_POINT ( 'NONE',  ( 0.000000000000000000, -2.946379043145784582, -75.11764819372150725 ) ) ;
#51628=CARTESIAN_POINT ( 'NONE',  ( 11.99999999999999822, -35.91791733033525702, 68.67312586194982771 ) ) ;
#51631=EDGE_CURVE ( 'NONE', #71207, #52228, #13641, .T. ) ;
#51635=ORIENTED_EDGE ( 'NONE', *, *, #22615, .F. ) ;
#51650=DIRECTION ( 'NONE',  ( -1.000000000000000000, -0.000000000000000000, 0.000000000000000000 ) ) ;
#51653=DIRECTION ( 'NONE',  ( -1.000000000000000000, 0.000000000000000000, -0.000000000000000000 ) ) ;
#51654=DIRECTION ( 'NONE',  ( 0.000000000000000000, 0.1564344650402312020, -0.9876883405951376593 ) ) ;
#51676=EDGE_CURVE ( 'NONE', #9142, #45831, #12264, .T. ) ;
#51684=EDGE_CURVE ( 'NONE', #20558, #60145, #25610, .T. ) ;
#51687=VERTEX_POINT ( 'NONE', #41575 ) ;
#51694=ORIENTED_EDGE ( 'NONE', *, *, #43037, .T. ) ;
#51695=FACE_OUTER_BOUND ( 'NONE', #34481, .T. ) ;
#51705=EDGE_CURVE ( 'NONE', #47354, #44992, #52017, .T. ) ;
#51711=ORIENTED_EDGE ( 'NONE', *, *, #3493, .F. ) ;
#51714=ORIENTED_EDGE ( 'NONE', *, *, #7025, .T. ) ;
#51718=VECTOR ( 'NONE', #73263, 1000.000000000000000 ) ;
#51720=VERTEX_POINT ( 'NONE', #53598 ) ;
#51724=VECTOR ( 'NONE', #71104, 1000.000000000000000 ) ;
#51727=CARTESIAN_POINT ( 'NONE',  ( 11.99999999999999822, 12.93880638057426502, -76.41127070299258150 ) ) ;
#51730=ORIENTED_EDGE ( 'NONE', *, *, #743, .T. ) ;
#51741=CARTESIAN_POINT ( 'NONE',  ( 0.000000000000000000, 0.000000000000000000, 0.000000000000000000 ) ) ;
#51743=FACE_OUTER_BOUND ( 'NONE', #17518, .T. ) ;
#51744=CARTESIAN_POINT ( 'NONE',  ( 0.000000000000000000, 0.000000000000000000, 0.000000000000000000 ) ) ;
#51749=VERTEX_POINT ( 'NONE', #64895 ) ;
#51751=CARTESIAN_POINT ( 'NONE',  ( 15.00000000000000000, -13.04903810567675393, -19.60159698893424718 ) ) ;
#51757=CARTESIAN_POINT ( 'NONE',  ( 0.000000000000000000, 70.53064760720316428, -26.01480285779861035 ) ) ;
#51764=CIRCLE ( 'NONE', #19351, 82.00000000000000000 ) ;
#51770=ORIENTED_EDGE ( 'NONE', *, *, #4006, .T. ) ;
#51778=LINE ( 'NONE', #62333, #53697 ) ;
#51791=CARTESIAN_POINT ( 'NONE',  ( 0.000000000000000000, 15.33399622253601713, -80.55351364060572905 ) ) ;
#51793=EDGE_CURVE ( 'NONE', #31332, #68814, #59328, .T. ) ;
#51800=DIRECTION ( 'NONE',  ( 0.000000000000000000, 0.8910065241883691201, -0.4539904997395446951 ) ) ;
#51802=LINE ( 'NONE', #67987, #50973 ) ;
#51808=EDGE_CURVE ( 'NONE', #55194, #66496, #52078, .T. ) ;
#51812=VERTEX_POINT ( 'NONE', #25403 ) ;
#51813=FACE_BOUND ( 'NONE', #65197, .T. ) ;
#51814=CIRCLE ( 'NONE', #39801, 77.49899999999999523 ) ;
#51823=LINE ( 'NONE', #68392, #26676 ) ;
#51842=ADVANCED_FACE ( 'NONE', ( #59619 ), #31025, .T. ) ;
#51847=FACE_OUTER_BOUND ( 'NONE', #28281, .T. ) ;
#51852=AXIS2_PLACEMENT_3D ( 'NONE', #45912, #6779, #40257 ) ;
#51859=EDGE_LOOP ( 'NONE', ( #25704, #30668, #59803, #26276 ) ) ;
#51864=LINE ( 'NONE', #69163, #9982 ) ;
#51868=ORIENTED_EDGE ( 'NONE', *, *, #25058, .F. ) ;
#51872=VERTEX_POINT ( 'NONE', #2872 ) ;
#51881=ORIENTED_EDGE ( 'NONE', *, *, #58678, .F. ) ;
#51885=DIRECTION ( 'NONE',  ( -1.000000000000000000, -0.000000000000000000, -0.000000000000000000 ) ) ;
#51889=ORIENTED_EDGE ( 'NONE', *, *, #63915, .T. ) ;
#51895=DIRECTION ( 'NONE',  ( 0.000000000000000000, 0.9510565162951544194, -0.3090169943749446757 ) ) ;
#51896=DIRECTION ( 'NONE',  ( 0.000000000000000000, -0.9723699203976741146, -0.2334453638559160493 ) ) ;
#51908=DIRECTION ( 'NONE',  ( 0.000000000000000000, -0.7071067811865535679, 0.7071067811865414665 ) ) ;
#51912=DIRECTION ( 'NONE',  ( -1.000000000000000000, -0.000000000000000000, -0.000000000000000000 ) ) ;
#51924=CARTESIAN_POINT ( 'NONE',  ( 0.000000000000000000, 75.16055320797030959, 18.89407956138283851 ) ) ;
#51944=LINE ( 'NONE', #69241, #46706 ) ;
#51947=CARTESIAN_POINT ( 'NONE',  ( 0.000000000000000000, -14.67089635893658794, -73.72996012237454977 ) ) ;
#51956=ORIENTED_EDGE ( 'NONE', *, *, #15038, .F. ) ;
#51962=ORIENTED_EDGE ( 'NONE', *, *, #30558, .T. ) ;
#51966=ORIENTED_EDGE ( 'NONE', *, *, #45678, .F. ) ;
#51999=EDGE_CURVE ( 'NONE', #64000, #40627, #6470, .T. ) ;
#52006=CARTESIAN_POINT ( 'NONE',  ( 11.99999999999999822, -71.87247863392384772, -39.47590169984923136 ) ) ;
#52008=EDGE_CURVE ( 'NONE', #8374, #48253, #12905, .T. ) ;
#52009=AXIS2_PLACEMENT_3D ( 'NONE', #7842, #3713, #36407 ) ;
#52014=SURFACE_SIDE_STYLE ('',( #1673 ) ) ;
#52017=CIRCLE ( 'NONE', #40065, 77.49899999999999523 ) ;
#52023=FACE_OUTER_BOUND ( 'NONE', #7260, .T. ) ;
#52031=ORIENTED_EDGE ( 'NONE', *, *, #69019, .T. ) ;
#52033=ADVANCED_FACE ( 'NONE', ( #52023 ), #63700, .T. ) ;
#52034=ORIENTED_EDGE ( 'NONE', *, *, #58819, .T. ) ;
#52037=ORIENTED_EDGE ( 'NONE', *, *, #22848, .F. ) ;
#52040=ORIENTED_EDGE ( 'NONE', *, *, #70440, .F. ) ;
#52044=EDGE_CURVE ( 'NONE', #19421, #2104, #23464, .T. ) ;
#52047=ORIENTED_EDGE ( 'NONE', *, *, #66822, .T. ) ;
#52049=EDGE_CURVE ( 'NONE', #68067, #53386, #14879, .T. ) ;
#52054=ORIENTED_EDGE ( 'NONE', *, *, #60751, .F. ) ;
#52055=ORIENTED_EDGE ( 'NONE', *, *, #4186, .F. ) ;
#52078=CIRCLE ( 'NONE', #553, 82.00000000000000000 ) ;
#52080=CARTESIAN_POINT ( 'NONE',  ( 11.99999999999999822, 41.76106447765580043, -62.50884508063379741 ) ) ;
#52082=CARTESIAN_POINT ( 'NONE',  ( 5.999999999999999112, 50.23322058963442771, -64.81221759200288091 ) ) ;
#52087=VECTOR ( 'NONE', #4144, 1000.000000000000000 ) ;
#52088=LINE ( 'NONE', #51727, #50363 ) ;
#52096=ORIENTED_EDGE ( 'NONE', *, *, #30537, .T. ) ;
#52098=ADVANCED_FACE ( 'NONE', ( #70404 ), #6548, .T. ) ;
#52099=CARTESIAN_POINT ( 'NONE',  ( 0.000000000000000000, 0.000000000000000000, 0.000000000000000000 ) ) ;
#52108=EDGE_CURVE ( 'NONE', #65473, #72308, #72509, .T. ) ;
#52109=CARTESIAN_POINT ( 'NONE',  ( 15.00000000000000000, 24.81905959214260804, -9.408202855044828894 ) ) ;
#52110=DIRECTION ( 'NONE',  ( -1.000000000000000000, 0.000000000000000000, 0.000000000000000000 ) ) ;
#52112=EDGE_CURVE ( 'NONE', #4678, #23323, #35477, .T. ) ;
#52117=DIRECTION ( 'NONE',  ( -1.000000000000000000, -0.000000000000000000, -0.000000000000000000 ) ) ;
#52119=AXIS2_PLACEMENT_3D ( 'NONE', #33087, #57526, #39495 ) ;
#52129=VECTOR ( 'NONE', #5454, 1000.000000000000000 ) ;
#52138=DIRECTION ( 'NONE',  ( -1.000000000000000000, 0.000000000000000000, 0.000000000000000000 ) ) ;
#52146=DIRECTION ( 'NONE',  ( 0.000000000000000000, -0.5224985647159380298, -0.8526401643540988395 ) ) ;
#52149=CARTESIAN_POINT ( 'NONE',  ( 11.99999999999999822, -22.90783923731685334, 78.73519480814947258 ) ) ;
#52155=ORIENTED_EDGE ( 'NONE', *, *, #58930, .T. ) ;
#52170=AXIS2_PLACEMENT_3D ( 'NONE', #49554, #20235, #19499 ) ;
#52179=ORIENTED_EDGE ( 'NONE', *, *, #63996, .T. ) ;
#52180=CIRCLE ( 'NONE', #67748, 31.99999999999998934 ) ;
#52199=DIRECTION ( 'NONE',  ( -1.000000000000000000, 0.000000000000000000, -0.000000000000000000 ) ) ;
#52201=EDGE_CURVE ( 'NONE', #21432, #26057, #52180, .T. ) ;
#52203=CIRCLE ( 'NONE', #56999, 31.99999999999998934 ) ;
#52206=PLANE ( 'NONE',  #8937 ) ;
#52228=VERTEX_POINT ( 'NONE', #25676 ) ;
#52231=ORIENTED_EDGE ( 'NONE', *, *, #60444, .F. ) ;
#52241=CARTESIAN_POINT ( 'NONE',  ( 0.000000000000000000, 31.47745569255237896, -68.26794271651228030 ) ) ;
#52244=DIRECTION ( 'NONE',  ( -1.000000000000000000, 0.000000000000000000, 0.000000000000000000 ) ) ;
#52251=ORIENTED_EDGE ( 'NONE', *, *, #23845, .F. ) ;
#52253=ORIENTED_EDGE ( 'NONE', *, *, #40385, .F. ) ;
#52254=CARTESIAN_POINT ( 'NONE',  ( 11.99999999999999822, 73.95703589263975175, 23.16143007188452785 ) ) ;
#52261=CYLINDRICAL_SURFACE ( 'NONE', #32494, 31.99999999999998579 ) ;
#52273=DIRECTION ( 'NONE',  ( 0.000000000000000000, 0.4067366430758009854, 0.9135454576426004225 ) ) ;
#52283=CARTESIAN_POINT ( 'NONE',  ( 12.00000000000000000, -20.55727247249748757, -16.78983467731284662 ) ) ;
#52290=VECTOR ( 'NONE', #53561, 1000.000000000000000 ) ;
#52293=CARTESIAN_POINT ( 'NONE',  ( 0.000000000000000000, 67.80270845531887858, 46.11716303203210288 ) ) ;
#52295=DIRECTION ( 'NONE',  ( 0.000000000000000000, 0.000000000000000000, -1.000000000000000000 ) ) ;
#52296=CARTESIAN_POINT ( 'NONE',  ( 0.000000000000000000, 76.41127070299273782, 12.93880638057342836 ) ) ;
#52300=DIRECTION ( 'NONE',  ( -1.000000000000000000, 0.000000000000000000, -0.000000000000000000 ) ) ;
#52305=DIRECTION ( 'NONE',  ( 0.000000000000000000, -0.9723699203976789995, 0.2334453638558956767 ) ) ;
#52316=DIRECTION ( 'NONE',  ( -1.000000000000000000, 0.000000000000000000, 0.000000000000000000 ) ) ;
#52324=ORIENTED_EDGE ( 'NONE', *, *, #34734, .F. ) ;
#52325=ORIENTED_EDGE ( 'NONE', *, *, #15118, .F. ) ;
#52328=ORIENTED_EDGE ( 'NONE', *, *, #51335, .F. ) ;
#52334=ORIENTED_EDGE ( 'NONE', *, *, #30363, .F. ) ;
#52335=ORIENTED_EDGE ( 'NONE', *, *, #49150, .T. ) ;
#52340=CARTESIAN_POINT ( 'NONE',  ( 0.000000000000000000, -2.543863470247813119, -81.96053171279903893 ) ) ;
#52342=DIRECTION ( 'NONE',  ( 0.000000000000000000, 0.3826834323650905589, -0.9238795325112864054 ) ) ;
#52346=DIRECTION ( 'NONE',  ( 0.000000000000000000, -0.9876883405951394357, 0.1564344650402205716 ) ) ;
#52352=CIRCLE ( 'NONE', #31898, 31.99999999999998579 ) ;
#52357=CARTESIAN_POINT ( 'NONE',  ( 12.00000000000000355, 0.000000000000000000, 0.000000000000000000 ) ) ;
#52364=DIRECTION ( 'NONE',  ( -1.000000000000000000, 0.000000000000000000, 0.000000000000000000 ) ) ;
#52372=FACE_OUTER_BOUND ( 'NONE', #18762, .T. ) ;
#52376=ORIENTED_EDGE ( 'NONE', *, *, #56825, .T. ) ;
#52378=PLANE ( 'NONE',  #72719 ) ;
#52379=CARTESIAN_POINT ( 'NONE',  ( 0.000000000000000000, -27.74655509720726343, 77.16300072079651784 ) ) ;
#52382=CARTESIAN_POINT ( 'NONE',  ( 15.00000000000000000, 23.49999999999999645, 1.499999999999995337 ) ) ;
#52384=SURFACE_STYLE_USAGE ( .BOTH. , #52014 ) ;
#52386=LINE ( 'NONE', #41125, #40836 ) ;
#52390=CARTESIAN_POINT ( 'NONE',  ( 0.000000000000000000, 0.000000000000000000, 0.000000000000000000 ) ) ;
#52393=CARTESIAN_POINT ( 'NONE',  ( 15.00000000000000000, -3.948201729842032215, 23.21447184625297666 ) ) ;
#52396=CIRCLE ( 'NONE', #6791, 31.99999999999998579 ) ;
#52399=VERTEX_POINT ( 'NONE', #5357 ) ;
#52404=VERTEX_POINT ( 'NONE', #10229 ) ;
#52407=VERTEX_POINT ( 'NONE', #33151 ) ;
#52425=DIRECTION ( 'NONE',  ( 0.000000000000000000, -0.9876883405951359940, -0.1564344650402420822 ) ) ;
#52427=DIRECTION ( 'NONE',  ( 1.000000000000000000, 0.000000000000000000, -0.000000000000000000 ) ) ;
#52434=ORIENTED_EDGE ( 'NONE', *, *, #18913, .F. ) ;
#52440=DIRECTION ( 'NONE',  ( 0.000000000000000000, 0.000000000000000000, 1.000000000000000000 ) ) ;
#52443=DIRECTION ( 'NONE',  ( 0.000000000000000000, 0.9510565162951521989, 0.3090169943749515591 ) ) ;
#52467=DIRECTION ( 'NONE',  ( -0.000000000000000000, 0.3090169943749573878, 0.9510565162951503115 ) ) ;
#52469=CARTESIAN_POINT ( 'NONE',  ( 15.00000000000000000, -23.29833615347104470, 3.418703333116808629 ) ) ;
#52472=CIRCLE ( 'NONE', #28434, 31.99999999999998579 ) ;
#52480=DIRECTION ( 'NONE',  ( 0.000000000000000000, 0.000000000000000000, 1.000000000000000000 ) ) ;
#52487=EDGE_LOOP ( 'NONE', ( #13242, #16189, #17472, #64086 ) ) ;
#52492=ORIENTED_EDGE ( 'NONE', *, *, #36408, .T. ) ;
#52498=FACE_OUTER_BOUND ( 'NONE', #68512, .T. ) ;
#52517=AXIS2_PLACEMENT_3D ( 'NONE', #5755, #30045, #51596 ) ;
#52520=VERTEX_POINT ( 'NONE', #41044 ) ;
#52521=CARTESIAN_POINT ( 'NONE',  ( 0.000000000000000000, 41.19522573413732403, 65.64334221924923440 ) ) ;
#52524=EDGE_CURVE ( 'NONE', #49623, #35138, #118, .T. ) ;
#52530=DIRECTION ( 'NONE',  ( 0.000000000000000000, 0.07845909572783793529, 0.9969173337331285190 ) ) ;
#52531=EDGE_CURVE ( 'NONE', #25593, #70390, #2955, .T. ) ;
#52533=ORIENTED_EDGE ( 'NONE', *, *, #42886, .F. ) ;
#52538=DIRECTION ( 'NONE',  ( 0.000000000000000000, 0.000000000000000000, 1.000000000000000000 ) ) ;
#52546=AXIS2_PLACEMENT_3D ( 'NONE', #32992, #49914, #15721 ) ;
#52549=ORIENTED_EDGE ( 'NONE', *, *, #43989, .F. ) ;
#52550=EDGE_CURVE ( 'NONE', #18854, #61291, #63974, .T. ) ;
#52551=CIRCLE ( 'NONE', #53730, 77.49899999999999523 ) ;
#52554=ADVANCED_FACE ( 'NONE', ( #23014 ), #45947, .T. ) ;
#52556=AXIS2_PLACEMENT_3D ( 'NONE', #18977, #60340, #48674 ) ;
#52557=DIRECTION ( 'NONE',  ( 0.000000000000000000, 0.000000000000000000, -1.000000000000000000 ) ) ;
#52581=CARTESIAN_POINT ( 'NONE',  ( 0.000000000000000000, 0.000000000000000000, 0.000000000000000000 ) ) ;
#52585=VERTEX_POINT ( 'NONE', #9031 ) ;
#52586=DIRECTION ( 'NONE',  ( 0.000000000000000000, 0.000000000000000000, 1.000000000000000000 ) ) ;
#52600=CARTESIAN_POINT ( 'NONE',  ( 11.99999999999999822, 0.000000000000000000, 0.000000000000000000 ) ) ;
#52604=CARTESIAN_POINT ( 'NONE',  ( -10.00000000000000000, 0.000000000000000000, 0.000000000000000000 ) ) ;
#52605=AXIS2_PLACEMENT_3D ( 'NONE', #48142, #70677, #61557 ) ;
#52607=DIRECTION ( 'NONE',  ( -1.000000000000000000, 0.000000000000000000, 0.000000000000000000 ) ) ;
#52611=EDGE_CURVE ( 'NONE', #15234, #41319, #60552, .T. ) ;
#52616=CARTESIAN_POINT ( 'NONE',  ( 0.000000000000000000, 55.20638768913831029, -51.02545421589267960 ) ) ;
#52617=ORIENTED_EDGE ( 'NONE', *, *, #46631, .F. ) ;
#52627=CIRCLE ( 'NONE', #71822, 77.49899999999999523 ) ;
#52629=CARTESIAN_POINT ( 'NONE',  ( 11.99999999999999822, 72.35432306680455383, 20.40083707023012494 ) ) ;
#52632=ADVANCED_FACE ( 'NONE', ( #7923 ), #13918, .T. ) ;
#52640=DIRECTION ( 'NONE',  ( 0.000000000000000000, 0.000000000000000000, -1.000000000000000000 ) ) ;
#52658=ORIENTED_EDGE ( 'NONE', *, *, #42954, .T. ) ;
#52659=CARTESIAN_POINT ( 'NONE',  ( 11.99999999999999822, -68.67312586194971402, -35.91791733033549860 ) ) ;
#52669=VECTOR ( 'NONE', #65453, 1000.000000000000000 ) ;
#52673=DIRECTION ( 'NONE',  ( 0.000000000000000000, 0.000000000000000000, 1.000000000000000000 ) ) ;
#52677=AXIS2_PLACEMENT_3D ( 'NONE', #59395, #70647, #19526 ) ;
#52682=AXIS2_PLACEMENT_3D ( 'NONE', #16240, #60988, #61375 ) ;
#52687=AXIS2_PLACEMENT_3D ( 'NONE', #17639, #2142, #36682 ) ;
#52694=EDGE_LOOP ( 'NONE', ( #39590, #55380, #52997, #8865 ) ) ;
#52701=CARTESIAN_POINT ( 'NONE',  ( 12.00000000000000000, -3.948201729842032215, 23.21447184625297666 ) ) ;
#52702=ORIENTED_EDGE ( 'NONE', *, *, #17541, .F. ) ;
#52704=DIRECTION ( 'NONE',  ( -1.000000000000000000, 0.000000000000000000, -0.000000000000000000 ) ) ;
#52712=CIRCLE ( 'NONE', #56314, 77.49899999999999523 ) ;
#52714=VERTEX_POINT ( 'NONE', #13192 ) ;
#52726=EDGE_CURVE ( 'NONE', #69188, #55213, #59069, .T. ) ;
#52731=ORIENTED_EDGE ( 'NONE', *, *, #58163, .T. ) ;
#52734=CARTESIAN_POINT ( 'NONE',  ( 11.99999999999999822, 0.000000000000000000, 0.000000000000000000 ) ) ;
#52737=AXIS2_PLACEMENT_3D ( 'NONE', #56455, #50790, #73717 ) ;
#52739=LINE ( 'NONE', #46363, #21056 ) ;
#52741=CARTESIAN_POINT ( 'NONE',  ( 11.99999999999999822, 0.000000000000000000, 0.000000000000000000 ) ) ;
#52742=CYLINDRICAL_SURFACE ( 'NONE', #10283, 31.99999999999998579 ) ;
#52743=DIRECTION ( 'NONE',  ( 0.000000000000000000, -0.8526401643540970632, 0.5224985647159410274 ) ) ;
#52746=EDGE_CURVE ( 'NONE', #32129, #21226, #4907, .T. ) ;
#52748=VERTEX_POINT ( 'NONE', #49252 ) ;
#52750=CIRCLE ( 'NONE', #69540, 82.00000000000000000 ) ;
#52752=CYLINDRICAL_SURFACE ( 'NONE', #4399, 82.00000000000000000 ) ;
#52755=DIRECTION ( 'NONE',  ( -1.000000000000000000, 0.000000000000000000, -0.000000000000000000 ) ) ;
#52764=DIRECTION ( 'NONE',  ( -1.000000000000000000, -0.000000000000000000, -0.000000000000000000 ) ) ;
#52769=CIRCLE ( 'NONE', #1236, 31.99999999999998579 ) ;
#52772=ADVANCED_FACE ( 'NONE', ( #9772 ), #56767, .T. ) ;
#52773=CIRCLE ( 'NONE', #21514, 31.99999999999999289 ) ;
#52779=VECTOR ( 'NONE', #15840, 1000.000000000000227 ) ;
#52785=ORIENTED_EDGE ( 'NONE', *, *, #52791, .F. ) ;
#52789=DIRECTION ( 'NONE',  ( 0.000000000000000000, 0.000000000000000000, 1.000000000000000000 ) ) ;
#52791=EDGE_CURVE ( 'NONE', #30232, #59737, #24591, .T. ) ;
#52793=DIRECTION ( 'NONE',  ( 0.000000000000000000, 0.000000000000000000, 1.000000000000000000 ) ) ;
#52798=AXIS2_PLACEMENT_3D ( 'NONE', #30382, #53328, #1129 ) ;
#52803=CARTESIAN_POINT ( 'NONE',  ( 15.00000000000000000, -22.32062822937469093, 14.36278369418830181 ) ) ;
#52808=ORIENTED_EDGE ( 'NONE', *, *, #45070, .T. ) ;
#52826=VECTOR ( 'NONE', #18784, 1000.000000000000000 ) ;
#52832=CIRCLE ( 'NONE', #9570, 82.00000000000000000 ) ;
#52833=DIRECTION ( 'NONE',  ( 0.000000000000000000, 0.000000000000000000, 1.000000000000000000 ) ) ;
#52836=ORIENTED_EDGE ( 'NONE', *, *, #62980, .T. ) ;
#52839=ORIENTED_EDGE ( 'NONE', *, *, #58838, .T. ) ;
#52842=DIRECTION ( 'NONE',  ( -1.000000000000000000, -0.000000000000000000, -0.000000000000000000 ) ) ;
#52843=CARTESIAN_POINT ( 'NONE',  ( 0.000000000000000000, 0.000000000000000000, 0.000000000000000000 ) ) ;
#52844=CARTESIAN_POINT ( 'NONE',  ( 11.99999999999999822, -11.30684508768284680, -76.66974797899850103 ) ) ;
#52851=CIRCLE ( 'NONE', #4838, 77.49900000000000944 ) ;
#52857=AXIS2_PLACEMENT_3D ( 'NONE', #58262, #23678, #12390 ) ;
#52866=EDGE_CURVE ( 'NONE', #22274, #27546, #10210, .T. ) ;
#52877=VECTOR ( 'NONE', #65522, 1000.000000000000000 ) ;
#52881=ORIENTED_EDGE ( 'NONE', *, *, #20303, .T. ) ;
#52882=EDGE_LOOP ( 'NONE', ( #25221, #48, #57088, #44089 ) ) ;
#52889=DIRECTION ( 'NONE',  ( -1.000000000000000000, 0.000000000000000000, 0.000000000000000000 ) ) ;
#52891=VECTOR ( 'NONE', #10203, 1000.000000000000000 ) ;
#52918=CARTESIAN_POINT ( 'NONE',  ( 0.000000000000000000, -62.20884554313985149, -46.21855187248698371 ) ) ;
#52922=EDGE_LOOP ( 'NONE', ( #4481, #58336, #12376, #9887 ) ) ;
#52923=ORIENTED_EDGE ( 'NONE', *, *, #20727, .T. ) ;
#52924=CYLINDRICAL_SURFACE ( 'NONE', #38569, 31.99999999999998579 ) ;
#52929=EDGE_LOOP ( 'NONE', ( #53816, #30966, #52324, #56738 ) ) ;
#52930=CARTESIAN_POINT ( 'NONE',  ( 0.000000000000000000, -77.16300072079681627, 27.74655509720641433 ) ) ;
#52932=ORIENTED_EDGE ( 'NONE', *, *, #70592, .T. ) ;
#52939=DIRECTION ( 'NONE',  ( 0.000000000000000000, 0.000000000000000000, 1.000000000000000000 ) ) ;
#52941=DIRECTION ( 'NONE',  ( -1.000000000000000000, 0.000000000000000000, 0.000000000000000000 ) ) ;
#52944=DIRECTION ( 'NONE',  ( 0.000000000000000000, -0.9876883405951394357, 0.1564344650402205716 ) ) ;
#52954=ADVANCED_FACE ( 'NONE', ( #23290 ), #28917, .F. ) ;
#52960=DIRECTION ( 'NONE',  ( -1.000000000000000000, -0.000000000000000000, 0.000000000000000000 ) ) ;
#52974=ORIENTED_EDGE ( 'NONE', *, *, #57960, .T. ) ;
#52978=ORIENTED_EDGE ( 'NONE', *, *, #20356, .F. ) ;
#52984=LINE ( 'NONE', #34573, #5720 ) ;
#52985=CIRCLE ( 'NONE', #26726, 77.49900000000002365 ) ;
#52992=ORIENTED_EDGE ( 'NONE', *, *, #36221, .F. ) ;
#52993=CYLINDRICAL_SURFACE ( 'NONE', #21487, 82.00000000000000000 ) ;
#52997=ORIENTED_EDGE ( 'NONE', *, *, #59072, .F. ) ;
#53005=ORIENTED_EDGE ( 'NONE', *, *, #62075, .T. ) ;
#53025=DIRECTION ( 'NONE',  ( -1.000000000000000000, -0.000000000000000000, -0.000000000000000000 ) ) ;
#53029=CARTESIAN_POINT ( 'NONE',  ( 0.000000000000000000, 0.000000000000000000, 0.000000000000000000 ) ) ;
#53030=LINE ( 'NONE', #58662, #6054 ) ;
#53038=CIRCLE ( 'NONE', #61411, 21.00000000000000000 ) ;
#53039=EDGE_CURVE ( 'NONE', #1337, #19859, #70198, .T. ) ;
#53040=FACE_OUTER_BOUND ( 'NONE', #63804, .T. ) ;
#53054=CARTESIAN_POINT ( 'NONE',  ( 11.99999999999999822, -29.01471420065616513, 76.69515212746006227 ) ) ;
#53056=CIRCLE ( 'NONE', #62695, 31.99999999999998224 ) ;
#53058=AXIS2_PLACEMENT_3D ( 'NONE', #21595, #44550, #67469 ) ;
#53063=CYLINDRICAL_SURFACE ( 'NONE', #47539, 31.99999999999998579 ) ;
#53064=VERTEX_POINT ( 'NONE', #72423 ) ;
#53067=VERTEX_POINT ( 'NONE', #50986 ) ;
#53091=DIRECTION ( 'NONE',  ( 0.000000000000000000, 0.000000000000000000, 1.000000000000000000 ) ) ;
#53092=AXIS2_PLACEMENT_3D ( 'NONE', #28156, #69140, #40553 ) ;
#53100=CIRCLE ( 'NONE', #61532, 31.99999999999998579 ) ;
#53103=AXIS2_PLACEMENT_3D ( 'NONE', #25453, #13786, #19799 ) ;
#53106=FACE_OUTER_BOUND ( 'NONE', #28112, .T. ) ;
#53107=DIRECTION ( 'NONE',  ( -1.000000000000000000, -0.000000000000000000, -0.000000000000000000 ) ) ;
#53109=DIRECTION ( 'NONE',  ( 1.000000000000000000, 0.000000000000000000, 0.000000000000000000 ) ) ;
#53120=FACE_OUTER_BOUND ( 'NONE', #7567, .T. ) ;
#53129=FACE_OUTER_BOUND ( 'NONE', #66062, .T. ) ;
#53132=CARTESIAN_POINT ( 'NONE',  ( 15.00000000000000000, 22.07842321921492612, 8.187992925817123790 ) ) ;
#53153=EDGE_CURVE ( 'NONE', #4121, #6916, #38218, .T. ) ;
#53163=EDGE_CURVE ( 'NONE', #30036, #68106, #47464, .T. ) ;
#53176=DIRECTION ( 'NONE',  ( 0.000000000000000000, 0.000000000000000000, 1.000000000000000000 ) ) ;
#53182=CARTESIAN_POINT ( 'NONE',  ( 0.000000000000000000, 5.256550761632864166, 77.32052557432842832 ) ) ;
#53197=DIRECTION ( 'NONE',  ( -1.000000000000000000, 0.000000000000000000, 0.000000000000000000 ) ) ;
#53206=CARTESIAN_POINT ( 'NONE',  ( 11.99999999999999822, -81.50828551894234408, 8.966570791700414489 ) ) ;
#53207=CARTESIAN_POINT ( 'NONE',  ( 0.000000000000000000, -76.66974797899844418, 11.30684508768314522 ) ) ;
#53210=FACE_OUTER_BOUND ( 'NONE', #6367, .T. ) ;
#53220=FACE_OUTER_BOUND ( 'NONE', #67683, .T. ) ;
#53221=EDGE_CURVE ( 'NONE', #47617, #68616, #41552, .T. ) ;
#53224=DIRECTION ( 'NONE',  ( -1.000000000000000000, -0.000000000000000000, 0.000000000000000000 ) ) ;
#53225=PLANE ( 'NONE',  #42151 ) ;
#53238=EDGE_CURVE ( 'NONE', #27772, #50461, #58242, .T. ) ;
#53240=EDGE_CURVE ( 'NONE', #24576, #855, #17149, .T. ) ;
#53242=VECTOR ( 'NONE', #68305, 1000.000000000000000 ) ;
#53243=ORIENTED_EDGE ( 'NONE', *, *, #9921, .F. ) ;
#53247=VECTOR ( 'NONE', #55475, 1000.000000000000114 ) ;
#53249=VERTEX_POINT ( 'NONE', #23168 ) ;
#53255=CARTESIAN_POINT ( 'NONE',  ( 0.000000000000000000, -11.30684508768284680, -76.66974797899850103 ) ) ;
#53257=DIRECTION ( 'NONE',  ( -1.000000000000000000, 0.000000000000000000, -0.000000000000000000 ) ) ;
#53260=ORIENTED_EDGE ( 'NONE', *, *, #24386, .T. ) ;
#53265=AXIS2_PLACEMENT_3D ( 'NONE', #35921, #43349, #6267 ) ;
#53271=ORIENTED_EDGE ( 'NONE', *, *, #6451, .F. ) ;
#53274=VERTEX_POINT ( 'NONE', #63392 ) ;
#53275=CARTESIAN_POINT ( 'NONE',  ( 15.00000000000000000, 0.000000000000000000, 0.000000000000000000 ) ) ;
#53279=VERTEX_POINT ( 'NONE', #34811 ) ;
#53280=CARTESIAN_POINT ( 'NONE',  ( 11.99999999999999822, 0.000000000000000000, 0.000000000000000000 ) ) ;
#53290=FACE_OUTER_BOUND ( 'NONE', #62801, .T. ) ;
#53303=CIRCLE ( 'NONE', #6518, 31.99999999999999289 ) ;
#53305=DIRECTION ( 'NONE',  ( 0.000000000000000000, 0.000000000000000000, 1.000000000000000000 ) ) ;
#53307=DIRECTION ( 'NONE',  ( 0.000000000000000000, 0.000000000000000000, 1.000000000000000000 ) ) ;
#53322=LINE ( 'NONE', #24744, #37158 ) ;
#53326=DIRECTION ( 'NONE',  ( 0.000000000000000000, -0.4067366430757887730, 0.9135454576426059736 ) ) ;
#53328=DIRECTION ( 'NONE',  ( -1.000000000000000000, 0.000000000000000000, 0.000000000000000000 ) ) ;
#53329=CARTESIAN_POINT ( 'NONE',  ( 12.00000000000000000, -19.89357724625003598, -12.59942793731059041 ) ) ;
#53335=DIRECTION ( 'NONE',  ( 0.000000000000000000, 0.5877852522924684742, 0.8090169943749506709 ) ) ;
#53336=ORIENTED_EDGE ( 'NONE', *, *, #23015, .T. ) ;
#53337=VECTOR ( 'NONE', #37862, 1000.000000000000000 ) ;
#53340=ORIENTED_EDGE ( 'NONE', *, *, #38308, .F. ) ;
#53350=DIRECTION ( 'NONE',  ( -1.000000000000000000, -0.000000000000000000, 0.000000000000000000 ) ) ;
#53358=VERTEX_POINT ( 'NONE', #70507 ) ;
#53364=CIRCLE ( 'NONE', #22144, 77.49899999999999523 ) ;
#53366=CYLINDRICAL_SURFACE ( 'NONE', #39307, 77.49899999999999523 ) ;
#53370=EDGE_CURVE ( 'NONE', #27662, #47563, #58893, .T. ) ;
#53372=ORIENTED_EDGE ( 'NONE', *, *, #73915, .F. ) ;
#53380=DIRECTION ( 'NONE',  ( 0.000000000000000000, 0.000000000000000000, 1.000000000000000000 ) ) ;
#53386=VERTEX_POINT ( 'NONE', #7389 ) ;
#53389=CARTESIAN_POINT ( 'NONE',  ( 11.99999999999999822, 14.66109333815460225, 73.73191006444577056 ) ) ;
#53395=DIRECTION ( 'NONE',  ( -1.000000000000000000, 0.000000000000000000, -0.000000000000000000 ) ) ;
#53400=CYLINDRICAL_SURFACE ( 'NONE', #43081, 77.49899999999999523 ) ;
#53405=DIRECTION ( 'NONE',  ( -1.000000000000000000, -0.000000000000000000, 0.000000000000000000 ) ) ;
#53420=CARTESIAN_POINT ( 'NONE',  ( 11.99999999999999822, -72.35432306680498016, 20.40083707022857951 ) ) ;
#53421=AXIS2_PLACEMENT_3D ( 'NONE', #21501, #44459, #45582 ) ;
#53429=DIRECTION ( 'NONE',  ( 0.000000000000000000, 0.000000000000000000, 1.000000000000000000 ) ) ;
#53430=ORIENTED_EDGE ( 'NONE', *, *, #61564, .F. ) ;
#53432=CARTESIAN_POINT ( 'NONE',  ( 12.00000000000000000, -10.45096189432314127, 21.10159698893440350 ) ) ;
#53440=CARTESIAN_POINT ( 'NONE',  ( 11.99999999999999822, 0.000000000000000000, 0.000000000000000000 ) ) ;
#53446=ORIENTED_EDGE ( 'NONE', *, *, #59020, .F. ) ;
#53454=CIRCLE ( 'NONE', #73902, 77.49899999999999523 ) ;
#53459=DIRECTION ( 'NONE',  ( -1.000000000000000000, -0.000000000000000000, 0.000000000000000000 ) ) ;
#53463=ADVANCED_FACE ( 'NONE', ( #8112 ), #61393, .T. ) ;
#53464=CYLINDRICAL_SURFACE ( 'NONE', #38328, 77.49899999999999523 ) ;
#53471=PLANE ( 'NONE',  #38332 ) ;
#53474=LINE ( 'NONE', #54583, #14593 ) ;
#53475=AXIS2_PLACEMENT_3D ( 'NONE', #12398, #68070, #22582 ) ;
#53485=VERTEX_POINT ( 'NONE', #65279 ) ;
#53508=DIRECTION ( 'NONE',  ( 0.000000000000000000, 0.000000000000000000, 1.000000000000000000 ) ) ;
#53511=ORIENTED_EDGE ( 'NONE', *, *, #72401, .T. ) ;
#53525=AXIS2_PLACEMENT_3D ( 'NONE', #5850, #28759, #7322 ) ;
#53527=AXIS2_PLACEMENT_3D ( 'NONE', #4250, #27139, #50821 ) ;
#53530=ORIENTED_EDGE ( 'NONE', *, *, #56690, .F. ) ;
#53534=VECTOR ( 'NONE', #19991, 1000.000000000000000 ) ;
#53553=ADVANCED_FACE ( 'NONE', ( #55372 ), #21144, .T. ) ;
#53560=LINE ( 'NONE', #24984, #25346 ) ;
#53561=DIRECTION ( 'NONE',  ( -1.000000000000000000, 0.000000000000000000, 0.000000000000000000 ) ) ;
#53563=CARTESIAN_POINT ( 'NONE',  ( 11.99999999999999822, 73.44644590900061587, 24.73286445877730699 ) ) ;
#53571=EDGE_CURVE ( 'NONE', #19421, #53274, #3052, .T. ) ;
#53574=DIRECTION ( 'NONE',  ( 1.000000000000000000, 0.000000000000000000, 0.000000000000000000 ) ) ;
#53582=DIRECTION ( 'NONE',  ( -1.000000000000000000, 0.000000000000000000, 0.000000000000000000 ) ) ;
#53589=DIRECTION ( 'NONE',  ( 0.000000000000000000, 0.000000000000000000, 1.000000000000000000 ) ) ;
#53592=VECTOR ( 'NONE', #49676, 1000.000000000000000 ) ;
#53598=CARTESIAN_POINT ( 'NONE',  ( 15.00000000000000000, -14.54903810567676636, -22.19967320028755964 ) ) ;
#53603=CYLINDRICAL_SURFACE ( 'NONE', #52687, 31.99999999999998579 ) ;
#53622=EDGE_CURVE ( 'NONE', #14085, #3697, #52472, .T. ) ;
#53623=VECTOR ( 'NONE', #30499, 1000.000000000000000 ) ;
#53626=ORIENTED_EDGE ( 'NONE', *, *, #51458, .T. ) ;
#53632=EDGE_CURVE ( 'NONE', #2660, #21827, #64509, .T. ) ;
#53640=CYLINDRICAL_SURFACE ( 'NONE', #34761, 82.00000000000000000 ) ;
#53649=DIRECTION ( 'NONE',  ( 0.000000000000000000, -0.9945218953682740670, -0.1045284632676459352 ) ) ;
#53654=LINE ( 'NONE', #65320, #2396 ) ;
#53659=EDGE_CURVE ( 'NONE', #21226, #56853, #50044, .T. ) ;
#53666=CARTESIAN_POINT ( 'NONE',  ( 0.000000000000000000, 0.000000000000000000, 0.000000000000000000 ) ) ;
#53679=DIRECTION ( 'NONE',  ( -1.000000000000000000, -0.000000000000000000, 0.000000000000000000 ) ) ;
#53685=DIRECTION ( 'NONE',  ( 1.000000000000000000, -0.000000000000000000, -0.000000000000000000 ) ) ;
#53686=CIRCLE ( 'NONE', #23689, 31.99999999999998934 ) ;
#53695=EDGE_CURVE ( 'NONE', #69733, #68386, #39286, .T. ) ;
#53697=VECTOR ( 'NONE', #33743, 1000.000000000000000 ) ;
#53699=ADVANCED_FACE ( 'NONE', ( #56865 ), #6110, .T. ) ;
#53715=DIRECTION ( 'NONE',  ( 0.000000000000000000, 0.000000000000000000, 1.000000000000000000 ) ) ;
#53716=ORIENTED_EDGE ( 'NONE', *, *, #42295, .F. ) ;
#53720=ORIENTED_EDGE ( 'NONE', *, *, #47750, .T. ) ;
#53723=ORIENTED_EDGE ( 'NONE', *, *, #42173, .F. ) ;
#53724=ORIENTED_EDGE ( 'NONE', *, *, #537, .T. ) ;
#53729=ORIENTED_EDGE ( 'NONE', *, *, #67831, .T. ) ;
#53730=AXIS2_PLACEMENT_3D ( 'NONE', #3678, #66808, #55529 ) ;
#53732=EDGE_LOOP ( 'NONE', ( #53260, #18766, #1751, #65374 ) ) ;
#53739=DIRECTION ( 'NONE',  ( 0.000000000000000000, -0.4999999999999930611, 0.8660254037844425934 ) ) ;
#53744=ADVANCED_FACE ( 'NONE', ( #63627 ), #51580, .T. ) ;
#53747=ORIENTED_EDGE ( 'NONE', *, *, #29627, .F. ) ;
#53752=CARTESIAN_POINT ( 'NONE',  ( 0.000000000000000000, -71.27951684758045303, 30.41916302227090085 ) ) ;
#53762=CIRCLE ( 'NONE', #71777, 82.00000000000000000 ) ;
#53765=CARTESIAN_POINT ( 'NONE',  ( 15.00000000000000000, -13.04903810567646971, 19.60159698893442481 ) ) ;
#53772=CARTESIAN_POINT ( 'NONE',  ( 11.99999999999999822, 0.000000000000000000, 0.000000000000000000 ) ) ;
#53776=CIRCLE ( 'NONE', #52546, 31.99999999999998579 ) ;
#53781=CIRCLE ( 'NONE', #38166, 77.49899999999999523 ) ;
#53783=ADVANCED_FACE ( 'NONE', ( #5002 ), #27904, .F. ) ;
#53787=ORIENTED_EDGE ( 'NONE', *, *, #50938, .F. ) ;
#53789=EDGE_CURVE ( 'NONE', #46404, #11277, #53795, .T. ) ;
#53794=ORIENTED_EDGE ( 'NONE', *, *, #73915, .T. ) ;
#53795=LINE ( 'NONE', #2710, #35662 ) ;
#53799=EDGE_LOOP ( 'NONE', ( #34977, #71714, #12320, #32372 ) ) ;
#53804=DIRECTION ( 'NONE',  ( 0.000000000000000000, 0.000000000000000000, -1.000000000000000000 ) ) ;
#53807=DIRECTION ( 'NONE',  ( 0.000000000000000000, 0.7604059656000322631, -0.6494480483301821039 ) ) ;
#53812=VERTEX_POINT ( 'NONE', #53432 ) ;
#53815=EDGE_CURVE ( 'NONE', #1543, #29672, #54886, .T. ) ;
#53816=ORIENTED_EDGE ( 'NONE', *, *, #42039, .T. ) ;
#53817=ORIENTED_EDGE ( 'NONE', *, *, #38896, .T. ) ;
#53818=VERTEX_POINT ( 'NONE', #1603 ) ;
#53823=ORIENTED_EDGE ( 'NONE', *, *, #72883, .T. ) ;
#53825=DIRECTION ( 'NONE',  ( 0.000000000000000000, 0.000000000000000000, 1.000000000000000000 ) ) ;
#53826=CARTESIAN_POINT ( 'NONE',  ( 11.99999999999999822, 76.41127070299273782, 12.93880638057342836 ) ) ;
#53837=DIRECTION ( 'NONE',  ( -0.000000000000000000, -0.9135454576426006446, 0.4067366430758008744 ) ) ;
#53839=DIRECTION ( 'NONE',  ( 0.000000000000000000, 0.000000000000000000, 1.000000000000000000 ) ) ;
#53840=DIRECTION ( 'NONE',  ( 1.000000000000000000, -0.000000000000000000, 0.000000000000000000 ) ) ;
#53841=CARTESIAN_POINT ( 'NONE',  ( 6.000000000000000000, 71.87247863392471459, -39.47590169984771080 ) ) ;
#53845=CARTESIAN_POINT ( 'NONE',  ( 6.000000000000000000, 8.966570791701871102, -81.50828551894218776 ) ) ;
#53852=AXIS2_PLACEMENT_3D ( 'NONE', #2317, #59422, #19191 ) ;
#53856=DIRECTION ( 'NONE',  ( 0.000000000000000000, -0.07845909572783055230, -0.9969173337331290741 ) ) ;
#53863=AXIS2_PLACEMENT_3D ( 'NONE', #6041, #52244, #27832 ) ;
#53865=CARTESIAN_POINT ( 'NONE',  ( 0.000000000000000000, -62.50329211542465657, 41.76937507738766442 ) ) ;
#53871=AXIS2_PLACEMENT_3D ( 'NONE', #26407, #66639, #20762 ) ;
#53874=AXIS2_PLACEMENT_3D ( 'NONE', #47973, #9217, #8859 ) ;
#53882=CARTESIAN_POINT ( 'NONE',  ( 0.000000000000000000, -68.27212725128254078, -31.46837873495049465 ) ) ;
#53892=ORIENTED_EDGE ( 'NONE', *, *, #14922, .F. ) ;
#53900=VECTOR ( 'NONE', #26297, 1000.000000000000114 ) ;
#53903=VECTOR ( 'NONE', #9770, 1000.000000000000000 ) ;
#53912=DIRECTION ( 'NONE',  ( 0.000000000000000000, 0.000000000000000000, 1.000000000000000000 ) ) ;
#53917=ORIENTED_EDGE ( 'NONE', *, *, #49389, .T. ) ;
#53938=AXIS2_PLACEMENT_3D ( 'NONE', #7388, #24667, #36315 ) ;
#53955=DIRECTION ( 'NONE',  ( 0.000000000000000000, 0.000000000000000000, -1.000000000000000000 ) ) ;
#53966=CARTESIAN_POINT ( 'NONE',  ( 0.000000000000000000, -35.91791733033427647, -68.67312586195032509 ) ) ;
#53980=ADVANCED_FACE ( 'NONE', ( #19684 ), #2460, .T. ) ;
#53982=VECTOR ( 'NONE', #25716, 1000.000000000000000 ) ;
#53984=ADVANCED_FACE ( 'NONE', ( #2077 ), #3540, .T. ) ;
#53985=VECTOR ( 'NONE', #1346, 1000.000000000000000 ) ;
#53991=ORIENTED_EDGE ( 'NONE', *, *, #58678, .T. ) ;
#54007=VERTEX_POINT ( 'NONE', #48640 ) ;
#54038=ORIENTED_EDGE ( 'NONE', *, *, #55264, .F. ) ;
#54039=VERTEX_POINT ( 'NONE', #36611 ) ;
#54048=VERTEX_POINT ( 'NONE', #65942 ) ;
#54057=CARTESIAN_POINT ( 'NONE',  ( 0.000000000000000000, 0.000000000000000000, 0.000000000000000000 ) ) ;
#54058=LINE ( 'NONE', #65342, #57505 ) ;
#54064=CIRCLE ( 'NONE', #6098, 31.99999999999998579 ) ;
#54074=EDGE_CURVE ( 'NONE', #33637, #24497, #72655, .T. ) ;
#54088=DIRECTION ( 'NONE',  ( -1.000000000000000000, 0.000000000000000000, 0.000000000000000000 ) ) ;
#54091=CARTESIAN_POINT ( 'NONE',  ( 5.999999999999999112, -50.23322058963393744, 64.81221759200325039 ) ) ;
#54099=LINE ( 'NONE', #65741, #70558 ) ;
#54101=ADVANCED_FACE ( 'NONE', ( #55385 ), #56130, .T. ) ;
#54103=ORIENTED_EDGE ( 'NONE', *, *, #2741, .F. ) ;
#54107=ORIENTED_EDGE ( 'NONE', *, *, #5186, .T. ) ;
#54109=DIRECTION ( 'NONE',  ( -1.000000000000000000, -0.000000000000000000, -0.000000000000000000 ) ) ;
#54111=ORIENTED_EDGE ( 'NONE', *, *, #65954, .T. ) ;
#54116=CIRCLE ( 'NONE', #30105, 31.99999999999998934 ) ;
#54125=DIRECTION ( 'NONE',  ( -1.000000000000000000, -0.000000000000000000, -0.000000000000000000 ) ) ;
#54130=ORIENTED_EDGE ( 'NONE', *, *, #53221, .T. ) ;
#54138=VECTOR ( 'NONE', #28978, 1000.000000000000000 ) ;
#54166=EDGE_CURVE ( 'NONE', #44200, #30664, #74152, .T. ) ;
#54167=DIRECTION ( 'NONE',  ( 0.000000000000000000, 0.000000000000000000, 1.000000000000000000 ) ) ;
#54176=DIRECTION ( 'NONE',  ( -1.000000000000000000, -0.000000000000000000, 0.000000000000000000 ) ) ;
#54185=DIRECTION ( 'NONE',  ( -1.000000000000000000, -0.000000000000000000, 0.000000000000000000 ) ) ;
#54187=AXIS2_PLACEMENT_3D ( 'NONE', #52741, #11756, #64033 ) ;
#54191=ORIENTED_EDGE ( 'NONE', *, *, #10898, .T. ) ;
#54192=DIRECTION ( 'NONE',  ( 0.000000000000000000, 0.000000000000000000, 1.000000000000000000 ) ) ;
#54195=DIRECTION ( 'NONE',  ( 0.000000000000000000, 0.5877852522924684742, 0.8090169943749507819 ) ) ;
#54197=EDGE_LOOP ( 'NONE', ( #62692, #866, #69012, #38467 ) ) ;
#54201=ORIENTED_EDGE ( 'NONE', *, *, #18899, .F. ) ;
#54220=VERTEX_POINT ( 'NONE', #1896 ) ;
#54225=CARTESIAN_POINT ( 'NONE',  ( 0.000000000000000000, -74.65491531819111515, -8.830959090343204920 ) ) ;
#54227=( GEOMETRIC_REPRESENTATION_CONTEXT ( 3 ) GLOBAL_UNCERTAINTY_ASSIGNED_CONTEXT ( ( #3927 ) ) GLOBAL_UNIT_ASSIGNED_CONTEXT ( ( #1311, #70039, #34731 ) ) REPRESENTATION_CONTEXT ( 'NONE', 'WORKASPACE' ) );
#54231=CIRCLE ( 'NONE', #31402, 31.99999999999998579 ) ;
#54243=CARTESIAN_POINT ( 'NONE',  ( 12.00000000000000000, -1.278221433540145391, 26.51162292216073979 ) ) ;
#54247=EDGE_CURVE ( 'NONE', #73160, #59759, #26120, .T. ) ;
#54248=AXIS2_PLACEMENT_3D ( 'NONE', #5331, #68474, #51908 ) ;
#54250=VECTOR ( 'NONE', #51414, 1000.000000000000000 ) ;
#54258=CARTESIAN_POINT ( 'NONE',  ( 11.99999999999999822, -39.78640506895559525, -66.50666863322042843 ) ) ;
#54261=ORIENTED_EDGE ( 'NONE', *, *, #41501, .F. ) ;
#54262=DIRECTION ( 'NONE',  ( -1.000000000000000000, -0.000000000000000000, 0.000000000000000000 ) ) ;
#54268=EDGE_CURVE ( 'NONE', #60480, #35604, #70256, .T. ) ;
#54269=LINE ( 'NONE', #42991, #57691 ) ;
#54272=CARTESIAN_POINT ( 'NONE',  ( -10.00000000000000000, 0.000000000000000000, 0.000000000000000000 ) ) ;
#54277=ORIENTED_EDGE ( 'NONE', *, *, #4681, .T. ) ;
#54279=ORIENTED_EDGE ( 'NONE', *, *, #14075, .F. ) ;
#54280=CARTESIAN_POINT ( 'NONE',  ( 11.99999999999999822, 0.000000000000000000, 0.000000000000000000 ) ) ;
#54293=AXIS2_PLACEMENT_3D ( 'NONE', #5192, #51032, #45411 ) ;
#54308=ORIENTED_EDGE ( 'NONE', *, *, #3696, .F. ) ;
#54325=CARTESIAN_POINT ( 'NONE',  ( 11.99999999999999822, -36.73666225445845157, -65.58780272294114866 ) ) ;
#54328=EDGE_CURVE ( 'NONE', #60196, #40964, #27293, .T. ) ;
#54329=CARTESIAN_POINT ( 'NONE',  ( 11.99999999999999822, -76.41127070299262414, -12.93880638057396304 ) ) ;
#54332=DIRECTION ( 'NONE',  ( 0.000000000000000000, 0.8910065241883656784, 0.4539904997395511344 ) ) ;
#54354=ORIENTED_EDGE ( 'NONE', *, *, #7311, .T. ) ;
#54358=ORIENTED_EDGE ( 'NONE', *, *, #42713, .F. ) ;
#54365=CARTESIAN_POINT ( 'NONE',  ( -10.00000000000000000, 0.000000000000000000, 0.000000000000000000 ) ) ;
#54380=EDGE_LOOP ( 'NONE', ( #70064, #8627, #61170, #64635 ) ) ;
#54400=ORIENTED_EDGE ( 'NONE', *, *, #1175, .T. ) ;
#54404=CARTESIAN_POINT ( 'NONE',  ( 11.99999999999999822, 5.256550761632864166, 77.32052557432842832 ) ) ;
#54408=CARTESIAN_POINT ( 'NONE',  ( 11.99999999999999822, 44.88180994100376608, 63.18004540533043922 ) ) ;
#54415=FACE_OUTER_BOUND ( 'NONE', #67725, .T. ) ;
#54418=DIRECTION ( 'NONE',  ( 0.000000000000000000, 0.6494480483301849905, -0.7604059656000298206 ) ) ;
#54430=AXIS2_PLACEMENT_3D ( 'NONE', #9127, #14026, #54629 ) ;
#54431=DIRECTION ( 'NONE',  ( 0.000000000000000000, 0.000000000000000000, 1.000000000000000000 ) ) ;
#54436=AXIS2_PLACEMENT_3D ( 'NONE', #31944, #28441, #45390 ) ;
#54438=CARTESIAN_POINT ( 'NONE',  ( 11.99999999999999822, 14.67089635893713684, 73.72996012237443608 ) ) ;
#54443=ORIENTED_EDGE ( 'NONE', *, *, #55880, .T. ) ;
#54445=DIRECTION ( 'NONE',  ( 0.000000000000000000, 0.000000000000000000, -1.000000000000000000 ) ) ;
#54478=VERTEX_POINT ( 'NONE', #48820 ) ;
#54480=DIRECTION ( 'NONE',  ( 0.000000000000000000, 0.5877852522924797984, 0.8090169943749426773 ) ) ;
#54483=VERTEX_POINT ( 'NONE', #10082 ) ;
#54485=AXIS2_PLACEMENT_3D ( 'NONE', #53440, #71080, #54192 ) ;
#54491=EDGE_CURVE ( 'NONE', #35768, #12556, #20240, .T. ) ;
#54492=VERTEX_POINT ( 'NONE', #15344 ) ;
#54510=CARTESIAN_POINT ( 'NONE',  ( 11.99999999999999822, 0.000000000000000000, 0.000000000000000000 ) ) ;
#54521=CARTESIAN_POINT ( 'NONE',  ( 6.000000000000000000, 40.65526001592611749, 71.21200624218811015 ) ) ;
#54533=ORIENTED_EDGE ( 'NONE', *, *, #27792, .T. ) ;
#54534=CIRCLE ( 'NONE', #26888, 82.00000000000000000 ) ;
#54547=ORIENTED_EDGE ( 'NONE', *, *, #33106, .T. ) ;
#54552=EDGE_CURVE ( 'NONE', #26000, #48188, #38630, .T. ) ;
#54556=ORIENTED_EDGE ( 'NONE', *, *, #30736, .T. ) ;
#54561=EDGE_CURVE ( 'NONE', #68066, #61610, #16854, .T. ) ;
#54568=ORIENTED_EDGE ( 'NONE', *, *, #47349, .T. ) ;
#54571=EDGE_CURVE ( 'NONE', #13817, #2580, #65036, .T. ) ;
#54574=DIRECTION ( 'NONE',  ( -1.000000000000000000, 0.000000000000000000, 0.000000000000000000 ) ) ;
#54580=CARTESIAN_POINT ( 'NONE',  ( 15.00000000000000000, 22.07842321921480888, -8.187992925817425771 ) ) ;
#54583=CARTESIAN_POINT ( 'NONE',  ( 6.000000000000000000, 8.966570791700705811, 81.50828551894228724 ) ) ;
#54590=DIRECTION ( 'NONE',  ( 1.000000000000000000, 0.000000000000000000, -0.000000000000000000 ) ) ;
#54603=VECTOR ( 'NONE', #15787, 1000.000000000000000 ) ;
#54605=VECTOR ( 'NONE', #41436, 1000.000000000000000 ) ;
#54610=DIRECTION ( 'NONE',  ( 0.000000000000000000, -0.9876883405951359940, -0.1564344650402420545 ) ) ;
#54613=CARTESIAN_POINT ( 'NONE',  ( 0.000000000000000000, 0.000000000000000000, 0.000000000000000000 ) ) ;
#54617=CARTESIAN_POINT ( 'NONE',  ( 0.000000000000000000, 0.000000000000000000, 0.000000000000000000 ) ) ;
#54625=ORIENTED_EDGE ( 'NONE', *, *, #23838, .F. ) ;
#54629=DIRECTION ( 'NONE',  ( 0.000000000000000000, 0.000000000000000000, 1.000000000000000000 ) ) ;
#54635=VERTEX_POINT ( 'NONE', #23970 ) ;
#54636=EDGE_CURVE ( 'NONE', #1681, #2580, #58925, .T. ) ;
#54637=VERTEX_POINT ( 'NONE', #25067 ) ;
#54645=CARTESIAN_POINT ( 'NONE',  ( 11.99999999999999822, -14.67089635893658794, -73.72996012237454977 ) ) ;
#54647=DIRECTION ( 'NONE',  ( -1.000000000000000000, -0.000000000000000000, -0.000000000000000000 ) ) ;
#54662=FACE_OUTER_BOUND ( 'NONE', #37909, .T. ) ;
#54672=DIRECTION ( 'NONE',  ( 0.000000000000000000, 0.000000000000000000, 1.000000000000000000 ) ) ;
#54683=ADVANCED_FACE ( 'NONE', ( #36344 ), #59287, .F. ) ;
#54685=EDGE_CURVE ( 'NONE', #62821, #51135, #7780, .T. ) ;
#54687=DIRECTION ( 'NONE',  ( -1.000000000000000000, -0.000000000000000000, 0.000000000000000000 ) ) ;
#54690=DIRECTION ( 'NONE',  ( 0.000000000000000000, 0.000000000000000000, 1.000000000000000000 ) ) ;
#54697=LINE ( 'NONE', #38143, #2206 ) ;
#54699=CARTESIAN_POINT ( 'NONE',  ( 6.000000000000000000, 78.73519480814955784, 22.90783923731656557 ) ) ;
#54721=ORIENTED_EDGE ( 'NONE', *, *, #7118, .T. ) ;
#54726=ORIENTED_EDGE ( 'NONE', *, *, #8804, .T. ) ;
#54732=CARTESIAN_POINT ( 'NONE',  ( 5.999999999999999112, 59.75363087400076267, 56.15606465354979093 ) ) ;
#54735=ORIENTED_EDGE ( 'NONE', *, *, #55330, .F. ) ;
#54739=ORIENTED_EDGE ( 'NONE', *, *, #21457, .F. ) ;
#54746=CARTESIAN_POINT ( 'NONE',  ( 0.000000000000000000, 65.58780272294129077, -36.73666225445822420 ) ) ;
#54750=LINE ( 'NONE', #72758, #11049 ) ;
#54754=VERTEX_POINT ( 'NONE', #52521 ) ;
#54764=DIRECTION ( 'NONE',  ( -1.000000000000000000, 0.000000000000000000, -0.000000000000000000 ) ) ;
#54778=VERTEX_POINT ( 'NONE', #37096 ) ;
#54781=DIRECTION ( 'NONE',  ( 1.000000000000000000, -0.000000000000000000, -0.000000000000000000 ) ) ;
#54785=DIRECTION ( 'NONE',  ( -1.000000000000000000, -0.000000000000000000, 0.000000000000000000 ) ) ;
#54798=CARTESIAN_POINT ( 'NONE',  ( 11.99999999999999822, 0.000000000000000000, 0.000000000000000000 ) ) ;
#54799=ORIENTED_EDGE ( 'NONE', *, *, #5812, .T. ) ;
#54817=DIRECTION ( 'NONE',  ( 0.000000000000000000, -0.9945218953682730678, 0.1045284632676569680 ) ) ;
#54819=FACE_OUTER_BOUND ( 'NONE', #55760, .T. ) ;
#54836=EDGE_CURVE ( 'NONE', #51720, #21751, #54750, .T. ) ;
#54843=CARTESIAN_POINT ( 'NONE',  ( 11.99999999999999822, 0.000000000000000000, 0.000000000000000000 ) ) ;
#54844=ORIENTED_EDGE ( 'NONE', *, *, #41249, .T. ) ;
#54862=CARTESIAN_POINT ( 'NONE',  ( 15.00000000000000000, -10.45096189432314127, 21.10159698893440350 ) ) ;
#54872=CARTESIAN_POINT ( 'NONE',  ( 11.99999999999999822, -16.65972982744876774, -80.28980883073775487 ) ) ;
#54873=DIRECTION ( 'NONE',  ( 0.000000000000000000, 0.000000000000000000, 1.000000000000000000 ) ) ;
#54874=CARTESIAN_POINT ( 'NONE',  ( -10.00000000000000000, 0.000000000000000000, 0.000000000000000000 ) ) ;
#54880=CARTESIAN_POINT ( 'NONE',  ( 15.00000000000000000, 22.07842321921480888, -8.187992925817425771 ) ) ;
#54881=CYLINDRICAL_SURFACE ( 'NONE', #39451, 31.99999999999998579 ) ;
#54882=CARTESIAN_POINT ( 'NONE',  ( 0.000000000000000000, -28.89263327155693517, -71.91182617369219088 ) ) ;
#54884=CARTESIAN_POINT ( 'NONE',  ( 15.00000000000000000, -22.67460108101782978, -6.353146135317906840 ) ) ;
#54886=CIRCLE ( 'NONE', #69280, 82.00000000000000000 ) ;
#54899=CARTESIAN_POINT ( 'NONE',  ( 0.000000000000000000, -74.65491531819124305, 8.830959090342128448 ) ) ;
#54915=DIRECTION ( 'NONE',  ( 0.000000000000000000, 0.000000000000000000, 1.000000000000000000 ) ) ;
#54919=DIRECTION ( 'NONE',  ( 0.000000000000000000, 0.5224985647159500202, -0.8526401643540915121 ) ) ;
#54923=ORIENTED_EDGE ( 'NONE', *, *, #69676, .F. ) ;
#54935=VECTOR ( 'NONE', #15239, 1000.000000000000000 ) ;
#54937=ORIENTED_EDGE ( 'NONE', *, *, #26485, .T. ) ;
#54966=CARTESIAN_POINT ( 'NONE',  ( 11.99999999999999822, -5.256550761632340141, -77.32052557432847095 ) ) ;
#54969=AXIS2_PLACEMENT_3D ( 'NONE', #18614, #24272, #64489 ) ;
#54974=DIRECTION ( 'NONE',  ( -1.000000000000000000, -0.000000000000000000, -0.000000000000000000 ) ) ;
#54975=EDGE_CURVE ( 'NONE', #27662, #55952, #21814, .T. ) ;
#54980=DIRECTION ( 'NONE',  ( -1.000000000000000000, 0.000000000000000000, -0.000000000000000000 ) ) ;
#54981=DIRECTION ( 'NONE',  ( -1.000000000000000000, -0.000000000000000000, 0.000000000000000000 ) ) ;
#54982=AXIS2_PLACEMENT_3D ( 'NONE', #26150, #48719, #60390 ) ;
#54983=ADVANCED_FACE ( 'NONE', ( #55865 ), #11477, .T. ) ;
#54992=EDGE_CURVE ( 'NONE', #7579, #50776, #65086, .T. ) ;
#54996=ORIENTED_EDGE ( 'NONE', *, *, #22326, .F. ) ;
#55002=CARTESIAN_POINT ( 'NONE',  ( 11.99999999999999822, 0.000000000000000000, 0.000000000000000000 ) ) ;
#55011=ORIENTED_EDGE ( 'NONE', *, *, #25911, .F. ) ;
#55012=CIRCLE ( 'NONE', #56267, 31.99999999999998224 ) ;
#55013=ORIENTED_EDGE ( 'NONE', *, *, #19628, .F. ) ;
#55021=DIRECTION ( 'NONE',  ( -1.000000000000000000, 0.000000000000000000, 0.000000000000000000 ) ) ;
#55036=DIRECTION ( 'NONE',  ( 0.000000000000000000, -0.4067366430757989315, -0.9135454576426015327 ) ) ;
#55049=DIRECTION ( 'NONE',  ( -1.000000000000000000, 0.000000000000000000, -0.000000000000000000 ) ) ;
#55051=CARTESIAN_POINT ( 'NONE',  ( 0.000000000000000000, 0.000000000000000000, 0.000000000000000000 ) ) ;
#55064=EDGE_CURVE ( 'NONE', #20436, #69158, #57894, .T. ) ;
#55070=AXIS2_PLACEMENT_3D ( 'NONE', #29267, #22919, #40559 ) ;
#55085=VERTEX_POINT ( 'NONE', #42290 ) ;
#55090=AXIS2_PLACEMENT_3D ( 'NONE', #60639, #54974, #56845 ) ;
#55093=DIRECTION ( 'NONE',  ( -1.000000000000000000, -0.000000000000000000, -0.000000000000000000 ) ) ;
#55094=EDGE_CURVE ( 'NONE', #719, #24118, #64109, .T. ) ;
#55095=DIRECTION ( 'NONE',  ( 0.000000000000000000, 0.000000000000000000, 1.000000000000000000 ) ) ;
#55102=ORIENTED_EDGE ( 'NONE', *, *, #6167, .T. ) ;
#55114=CIRCLE ( 'NONE', #67139, 82.00000000000000000 ) ;
#55121=VERTEX_POINT ( 'NONE', #12945 ) ;
#55127=LINE ( 'NONE', #49116, #11416 ) ;
#55128=VECTOR ( 'NONE', #23605, 1000.000000000000000 ) ;
#55132=LINE ( 'NONE', #9645, #26323 ) ;
#55138=DIRECTION ( 'NONE',  ( -1.000000000000000000, 0.000000000000000000, -0.000000000000000000 ) ) ;
#55139=CARTESIAN_POINT ( 'NONE',  ( 15.00000000000000000, 5.835314593368470248, -22.81335362449854642 ) ) ;
#55152=CYLINDRICAL_SURFACE ( 'NONE', #67267, 31.99999999999998579 ) ;
#55157=AXIS2_PLACEMENT_3D ( 'NONE', #16522, #46216, #44741 ) ;
#55159=EDGE_CURVE ( 'NONE', #9042, #5291, #70451, .T. ) ;
#55166=EDGE_CURVE ( 'NONE', #69920, #3672, #18594, .T. ) ;
#55168=DIRECTION ( 'NONE',  ( 0.000000000000000000, 0.000000000000000000, 1.000000000000000000 ) ) ;
#55169=DIRECTION ( 'NONE',  ( 0.000000000000000000, 0.000000000000000000, 1.000000000000000000 ) ) ;
#55171=CIRCLE ( 'NONE', #4814, 31.99999999999998579 ) ;
#55177=AXIS2_PLACEMENT_3D ( 'NONE', #1283, #48573, #58748 ) ;
#55188=LINE ( 'NONE', #54091, #13573 ) ;
#55189=DIRECTION ( 'NONE',  ( -1.000000000000000000, -0.000000000000000000, 0.000000000000000000 ) ) ;
#55194=VERTEX_POINT ( 'NONE', #987 ) ;
#55213=VERTEX_POINT ( 'NONE', #24255 ) ;
#55220=ORIENTED_EDGE ( 'NONE', *, *, #41522, .F. ) ;
#55228=AXIS2_PLACEMENT_3D ( 'NONE', #28300, #10647, #39603 ) ;
#55232=PLANE ( 'NONE',  #63894 ) ;
#55237=EDGE_CURVE ( 'NONE', #72968, #19406, #17057, .T. ) ;
#55241=CARTESIAN_POINT ( 'NONE',  ( 11.99999999999999822, 0.000000000000000000, 0.000000000000000000 ) ) ;
#55246=DIRECTION ( 'NONE',  ( 0.000000000000000000, -0.7431448254773862505, 0.6691306063588671194 ) ) ;
#55253=CARTESIAN_POINT ( 'NONE',  ( 15.00000000000000000, -20.55727247249748402, -16.78983467731284307 ) ) ;
#55263=CARTESIAN_POINT ( 'NONE',  ( 15.00000000000000000, 20.85821328998756385, 10.92862929874494249 ) ) ;
#55264=EDGE_CURVE ( 'NONE', #45393, #12388, #48276, .T. ) ;
#55272=CARTESIAN_POINT ( 'NONE',  ( 11.99999999999999822, 65.64334221924964652, -41.19522573413665611 ) ) ;
#55273=EDGE_CURVE ( 'NONE', #1863, #60548, #45887, .T. ) ;
#55274=DIRECTION ( 'NONE',  ( -1.000000000000000000, 0.000000000000000000, -0.000000000000000000 ) ) ;
#55284=ORIENTED_EDGE ( 'NONE', *, *, #544, .T. ) ;
#55290=DIRECTION ( 'NONE',  ( 0.000000000000000000, 0.5877852522924742473, -0.8090169943749466741 ) ) ;
#55292=CARTESIAN_POINT ( 'NONE',  ( 11.99999999999999822, 27.74655509720670210, 77.16300072079670258 ) ) ;
#55294=ORIENTED_EDGE ( 'NONE', *, *, #48701, .F. ) ;
#55297=LINE ( 'NONE', #15437, #9648 ) ;
#55303=AXIS2_PLACEMENT_3D ( 'NONE', #34978, #45903, #12037 ) ;
#55308=EDGE_LOOP ( 'NONE', ( #28042, #66956, #28177, #44010 ) ) ;
#55327=EDGE_CURVE ( 'NONE', #19604, #58617, #8736, .T. ) ;
#55328=ORIENTED_EDGE ( 'NONE', *, *, #72883, .F. ) ;
#55330=EDGE_CURVE ( 'NONE', #70942, #33637, #13258, .T. ) ;
#55339=AXIS2_PLACEMENT_3D ( 'NONE', #59204, #71201, #55036 ) ;
#55344=DIRECTION ( 'NONE',  ( -1.000000000000000000, -0.000000000000000000, 0.000000000000000000 ) ) ;
#55348=EDGE_LOOP ( 'NONE', ( #64643, #46046, #37444, #33579 ) ) ;
#55351=CARTESIAN_POINT ( 'NONE',  ( 6.000000000000000000, -44.99326035066007279, -68.55367621811190304 ) ) ;
#55358=EDGE_CURVE ( 'NONE', #16056, #7244, #19632, .T. ) ;
#55361=VECTOR ( 'NONE', #749, 999.9999999999998863 ) ;
#55370=DIRECTION ( 'NONE',  ( -1.000000000000000000, 0.000000000000000000, 0.000000000000000000 ) ) ;
#55372=FACE_OUTER_BOUND ( 'NONE', #65469, .T. ) ;
#55376=ORIENTED_EDGE ( 'NONE', *, *, #537, .F. ) ;
#55378=ORIENTED_EDGE ( 'NONE', *, *, #49814, .T. ) ;
#55380=ORIENTED_EDGE ( 'NONE', *, *, #56302, .F. ) ;
#55385=FACE_OUTER_BOUND ( 'NONE', #65574, .T. ) ;
#55402=DIRECTION ( 'NONE',  ( 0.000000000000000000, 0.000000000000000000, 1.000000000000000000 ) ) ;
#55409=FACE_OUTER_BOUND ( 'NONE', #51859, .T. ) ;
#55420=ADVANCED_FACE ( 'NONE', ( #38418 ), #71869, .T. ) ;
#55421=ORIENTED_EDGE ( 'NONE', *, *, #70798, .T. ) ;
#55427=CARTESIAN_POINT ( 'NONE',  ( 0.000000000000000000, 30.41916302227114599, 71.27951684758035356 ) ) ;
#55429=CARTESIAN_POINT ( 'NONE',  ( 0.000000000000000000, 55.16347631943042984, 60.67117009219156643 ) ) ;
#55431=EDGE_CURVE ( 'NONE', #27292, #50748, #14733, .T. ) ;
#55432=EDGE_LOOP ( 'NONE', ( #29821, #70681, #6745, #54261 ) ) ;
#55443=EDGE_CURVE ( 'NONE', #67492, #31113, #24348, .T. ) ;
#55450=DIRECTION ( 'NONE',  ( 0.000000000000000000, 0.000000000000000000, -1.000000000000000000 ) ) ;
#55461=DIRECTION ( 'NONE',  ( -1.000000000000000000, 0.000000000000000000, 0.000000000000000000 ) ) ;
#55468=VECTOR ( 'NONE', #64405, 1000.000000000000000 ) ;
#55471=AXIS2_PLACEMENT_3D ( 'NONE', #52390, #47138, #64064 ) ;
#55473=CARTESIAN_POINT ( 'NONE',  ( 11.99999999999999822, 0.000000000000000000, 77.49899999999999523 ) ) ;
#55474=DIRECTION ( 'NONE',  ( -1.000000000000000000, -0.000000000000000000, -0.000000000000000000 ) ) ;
#55475=DIRECTION ( 'NONE',  ( 0.000000000000000000, -0.4067366430757908269, 0.9135454576426049744 ) ) ;
#55480=ORIENTED_EDGE ( 'NONE', *, *, #66105, .F. ) ;
#55482=ORIENTED_EDGE ( 'NONE', *, *, #11865, .F. ) ;
#55485=CARTESIAN_POINT ( 'NONE',  ( 15.00000000000000000, -18.13022148937263012, -15.02647892043543898 ) ) ;
#55489=DIRECTION ( 'NONE',  ( -1.000000000000000000, 0.000000000000000000, 0.000000000000000000 ) ) ;
#55492=ORIENTED_EDGE ( 'NONE', *, *, #8737, .F. ) ;
#55499=ORIENTED_EDGE ( 'NONE', *, *, #61567, .T. ) ;
#55502=CARTESIAN_POINT ( 'NONE',  ( 6.000000000000000000, 81.50828551894227303, 8.966570791700986476 ) ) ;
#55504=DIRECTION ( 'NONE',  ( 0.000000000000000000, 0.9238795325112878487, -0.3826834323650874503 ) ) ;
#55508=FACE_OUTER_BOUND ( 'NONE', #5461, .T. ) ;
#55511=CARTESIAN_POINT ( 'NONE',  ( 15.00000000000000000, -25.60904388321925040, -6.976881207771165272 ) ) ;
#55516=DIRECTION ( 'NONE',  ( -1.000000000000000000, -0.000000000000000000, 0.000000000000000000 ) ) ;
#55518=LINE ( 'NONE', #43141, #53337 ) ;
#55521=VERTEX_POINT ( 'NONE', #60617 ) ;
#55524=VERTEX_POINT ( 'NONE', #52283 ) ;
#55525=CYLINDRICAL_SURFACE ( 'NONE', #31888, 82.00000000000000000 ) ;
#55526=CIRCLE ( 'NONE', #21868, 82.00000000000000000 ) ;
#55527=CIRCLE ( 'NONE', #23123, 31.99999999999998579 ) ;
#55529=DIRECTION ( 'NONE',  ( 0.000000000000000000, 0.8090169943749445647, 0.5877852522924770229 ) ) ;
#55531=CYLINDRICAL_SURFACE ( 'NONE', #47255, 77.49899999999999523 ) ;
#55532=CARTESIAN_POINT ( 'NONE',  ( 11.99999999999999822, 76.41127070299290835, -12.93880638057234123 ) ) ;
#55535=CARTESIAN_POINT ( 'NONE',  ( 6.000000000000000000, 34.94270380257741238, -74.18225833017852722 ) ) ;
#55544=LINE ( 'NONE', #44649, #8328 ) ;
#55549=DIRECTION ( 'NONE',  ( -1.000000000000000000, 0.000000000000000000, -0.000000000000000000 ) ) ;
#55550=CARTESIAN_POINT ( 'NONE',  ( 11.99999999999999822, -70.53064760720336324, 26.01480285779810231 ) ) ;
#55555=EDGE_CURVE ( 'NONE', #30315, #30862, #5701, .T. ) ;
#55557=DIRECTION ( 'NONE',  ( -1.000000000000000000, 0.000000000000000000, 0.000000000000000000 ) ) ;
#55563=ORIENTED_EDGE ( 'NONE', *, *, #22162, .F. ) ;
#55568=CARTESIAN_POINT ( 'NONE',  ( 6.000000000000000000, -68.55367621811173251, 44.99326035066031437 ) ) ;
#55570=DIRECTION ( 'NONE',  ( -1.000000000000000000, -0.000000000000000000, 0.000000000000000000 ) ) ;
#55593=ORIENTED_EDGE ( 'NONE', *, *, #57404, .F. ) ;
#55594=ORIENTED_EDGE ( 'NONE', *, *, #18350, .T. ) ;
#55605=EDGE_CURVE ( 'NONE', #42829, #12604, #68098, .T. ) ;
#55608=DIRECTION ( 'NONE',  ( 0.000000000000000000, 0.1564344650402311743, -0.9876883405951376593 ) ) ;
#55610=DIRECTION ( 'NONE',  ( 0.000000000000000000, 0.000000000000000000, 1.000000000000000000 ) ) ;
#55623=CIRCLE ( 'NONE', #20782, 82.00000000000000000 ) ;
#55628=AXIS2_PLACEMENT_3D ( 'NONE', #49321, #60262, #14739 ) ;
#55630=LINE ( 'NONE', #22539, #31074 ) ;
#55634=CARTESIAN_POINT ( 'NONE',  ( 11.99999999999999822, -74.65491531819111515, -8.830959090343204920 ) ) ;
#55642=VERTEX_POINT ( 'NONE', #17701 ) ;
#55654=VECTOR ( 'NONE', #37073, 999.9999999999998863 ) ;
#55661=CARTESIAN_POINT ( 'NONE',  ( 0.000000000000000000, 0.000000000000000000, 0.000000000000000000 ) ) ;
#55664=DIRECTION ( 'NONE',  ( 1.000000000000000000, 0.000000000000000000, 0.000000000000000000 ) ) ;
#55665=AXIS2_PLACEMENT_3D ( 'NONE', #44385, #49273, #55290 ) ;
#55667=DIRECTION ( 'NONE',  ( -1.000000000000000000, 0.000000000000000000, 0.000000000000000000 ) ) ;
#55668=AXIS2_PLACEMENT_3D ( 'NONE', #30290, #52117, #52480 ) ;
#55672=VECTOR ( 'NONE', #73920, 1000.000000000000000 ) ;
#55677=DIRECTION ( 'NONE',  ( -1.000000000000000000, 0.000000000000000000, 0.000000000000000000 ) ) ;
#55679=EDGE_LOOP ( 'NONE', ( #24861, #12013, #38662, #71355 ) ) ;
#55684=VERTEX_POINT ( 'NONE', #22609 ) ;
#55692=EDGE_CURVE ( 'NONE', #37007, #73707, #39965, .T. ) ;
#55693=DIRECTION ( 'NONE',  ( -1.000000000000000000, 0.000000000000000000, -0.000000000000000000 ) ) ;
#55699=ADVANCED_FACE ( 'NONE', ( #71407 ), #59047, .T. ) ;
#55702=ORIENTED_EDGE ( 'NONE', *, *, #6720, .F. ) ;
#55703=LINE ( 'NONE', #15853, #34858 ) ;
#55710=VERTEX_POINT ( 'NONE', #65790 ) ;
#55727=CARTESIAN_POINT ( 'NONE',  ( 0.000000000000000000, -26.01480285779785362, -70.53064760720343429 ) ) ;
#55735=ORIENTED_EDGE ( 'NONE', *, *, #16538, .T. ) ;
#55742=DIRECTION ( 'NONE',  ( 0.000000000000000000, 0.000000000000000000, 1.000000000000000000 ) ) ;
#55746=EDGE_CURVE ( 'NONE', #5309, #65173, #59132, .T. ) ;
#55754=AXIS2_PLACEMENT_3D ( 'NONE', #11140, #45744, #50987 ) ;
#55755=VERTEX_POINT ( 'NONE', #36464 ) ;
#55759=DIRECTION ( 'NONE',  ( 0.000000000000000000, 0.000000000000000000, 1.000000000000000000 ) ) ;
#55760=EDGE_LOOP ( 'NONE', ( #15331, #21646, #49359, #59742 ) ) ;
#55761=VERTEX_POINT ( 'NONE', #64680 ) ;
#55763=VERTEX_POINT ( 'NONE', #31194 ) ;
#55770=CARTESIAN_POINT ( 'NONE',  ( 11.99999999999999822, 11.30684508768339569, 76.66974797899841576 ) ) ;
#55771=DIRECTION ( 'NONE',  ( 0.000000000000000000, -0.9781476007338067991, -0.2079116908177533196 ) ) ;
#55790=EDGE_CURVE ( 'NONE', #57242, #51571, #55527, .T. ) ;
#55795=VECTOR ( 'NONE', #53405, 1000.000000000000000 ) ;
#55798=EDGE_CURVE ( 'NONE', #68814, #27944, #12318, .T. ) ;
#55799=DIRECTION ( 'NONE',  ( -1.000000000000000000, 0.000000000000000000, -0.000000000000000000 ) ) ;
#55801=AXIS2_PLACEMENT_3D ( 'NONE', #14963, #37538, #54445 ) ;
#55810=FACE_OUTER_BOUND ( 'NONE', #47846, .T. ) ;
#55813=CARTESIAN_POINT ( 'NONE',  ( 11.99999999999999822, -46.53671651293991118, 59.03961581697383565 ) ) ;
#55834=CIRCLE ( 'NONE', #20999, 31.99999999999998224 ) ;
#55845=DIRECTION ( 'NONE',  ( 0.000000000000000000, 0.4539904997395478037, -0.8910065241883673437 ) ) ;
#55857=DIRECTION ( 'NONE',  ( 0.000000000000000000, 0.000000000000000000, 1.000000000000000000 ) ) ;
#55862=VERTEX_POINT ( 'NONE', #66892 ) ;
#55865=FACE_OUTER_BOUND ( 'NONE', #2208, .T. ) ;
#55866=EDGE_LOOP ( 'NONE', ( #16989, #46876, #27014, #35958 ) ) ;
#55880=EDGE_CURVE ( 'NONE', #63637, #73028, #67643, .T. ) ;
#55887=LINE ( 'NONE', #61907, #6505 ) ;
#55895=DIRECTION ( 'NONE',  ( 0.000000000000000000, 0.000000000000000000, -1.000000000000000000 ) ) ;
#55899=DIRECTION ( 'NONE',  ( 1.000000000000000000, 0.000000000000000000, 0.000000000000000000 ) ) ;
#55903=CARTESIAN_POINT ( 'NONE',  ( 11.99999999999999822, -26.01480285779885904, 70.53064760720306481 ) ) ;
#55909=ORIENTED_EDGE ( 'NONE', *, *, #70927, .F. ) ;
#55911=DIRECTION ( 'NONE',  ( 1.000000000000000000, -0.000000000000000000, -0.000000000000000000 ) ) ;
#55925=EDGE_CURVE ( 'NONE', #40890, #51530, #4505, .T. ) ;
#55926=CARTESIAN_POINT ( 'NONE',  ( 15.00000000000000000, 8.688484142253932063, -21.88630264137371029 ) ) ;
#55927=DIRECTION ( 'NONE',  ( -1.000000000000000000, -0.000000000000000000, 0.000000000000000000 ) ) ;
#55929=CARTESIAN_POINT ( 'NONE',  ( 11.99999999999999822, -59.03961581697432592, 46.53671651293927880 ) ) ;
#55935=CARTESIAN_POINT ( 'NONE',  ( 0.000000000000000000, -78.73519480814938731, -22.90783923731713045 ) ) ;
#55936=ORIENTED_EDGE ( 'NONE', *, *, #9099, .F. ) ;
#55952=VERTEX_POINT ( 'NONE', #37593 ) ;
#55964=VERTEX_POINT ( 'NONE', #54872 ) ;
#55986=LINE ( 'NONE', #33413, #22739 ) ;
#55997=EDGE_CURVE ( 'NONE', #41513, #45152, #65192, .T. ) ;
#56001=CIRCLE ( 'NONE', #51172, 82.00000000000000000 ) ;
#56005=DIRECTION ( 'NONE',  ( -1.000000000000000000, -0.000000000000000000, 0.000000000000000000 ) ) ;
#56025=VERTEX_POINT ( 'NONE', #17620 ) ;
#56031=ORIENTED_EDGE ( 'NONE', *, *, #11280, .F. ) ;
#56032=DIRECTION ( 'NONE',  ( -1.000000000000000000, -0.000000000000000000, -0.000000000000000000 ) ) ;
#56034=ORIENTED_EDGE ( 'NONE', *, *, #20866, .T. ) ;
#56037=EDGE_CURVE ( 'NONE', #19406, #588, #40024, .T. ) ;
#56038=AXIS2_PLACEMENT_3D ( 'NONE', #33397, #49216, #72145 ) ;
#56039=ORIENTED_EDGE ( 'NONE', *, *, #25412, .T. ) ;
#56048=AXIS2_PLACEMENT_3D ( 'NONE', #30163, #64764, #30527 ) ;
#56050=VECTOR ( 'NONE', #6617, 1000.000000000000000 ) ;
#56064=VECTOR ( 'NONE', #47678, 1000.000000000000000 ) ;
#56080=ORIENTED_EDGE ( 'NONE', *, *, #73676, .T. ) ;
#56087=DIRECTION ( 'NONE',  ( 0.000000000000000000, 0.000000000000000000, 1.000000000000000000 ) ) ;
#56095=LINE ( 'NONE', #72992, #41905 ) ;
#56113=ORIENTED_EDGE ( 'NONE', *, *, #16528, .T. ) ;
#56120=ORIENTED_EDGE ( 'NONE', *, *, #22848, .T. ) ;
#56125=EDGE_LOOP ( 'NONE', ( #52328, #8959, #6319, #17012, #10180, #3875, #18857, #17241, #47085, #31150, #26099, #46464, #26058, #46071, #34363, #20227, #72035, #13716, #37800, #73725, #14127, #7799, #25421, #23321, #24506, #6757, #10107, #42919, #70425, #67410, #27355, #12192, #67453, #35422, #36605, #29853, #7134, #65970, #69896, #39773, #39414, #71109, #66596, #50473, #73970, #34146, #24896, #62353, #3831, #39751, #18331, #6391, #12921, #19390, #17275, #2972, #34571, #29960, #47183, #2255, #23786, #40063, #1446, #14988, #30775, #73883, #68168, #36510, #2713, #31535, #2254, #15307, #28364, #57729, #8975, #39212, #37856, #64899, #2876, #12470, #8198, #43830, #73529, #19975, #63060, #11296, #63635, #28984, #65833, #70058, #27838, #43306, #14863, #66243, #61607, #53892, #61482, #34028, #24320, #42518, #39194, #42551, #5940, #51574, #68719, #32772, #69717, #14778, #33480, #11334, #46972, #33633, #17113, #60392, #69474, #39100, #57141, #49310, #47777, #52533, #40316, #8070, #35535, #3719, #52549, #32808, #41720, #40353, #4955, #48100, #16735, #59474, #7106, #70438, #25054, #2109, #53430, #26783, #71393, #6824, #53372, #5556, #39620, #69115, #15830, #69700, #55220, #23987, #44834, #71298, #6827, #57332, #10995, #54739, #43510, #39433, #28784, #40294, #69708, #4031, #65828, #31138, #43925, #29957, #39744, #25248, #4712, #59575, #43671, #52978, #7383, #29392, #5022, #59833, #32634, #13585, #29964, #55480, #34206, #154, #1531, #10626, #35309, #25514, #58947, #49478, #41857, #39052, #36453, #56943, #40983, #8482, #2846, #12577, #10280, #10163, #73514, #20791, #31092, #69709, #74291, #32487, #66111, #34901, #45317, #36712, #15040, #35154, #46555, #51255, #24297, #11185, #54201, #67694, #48310, #42216, #60298, #70814, #66474, #38752, #69544, #60224, #21527, #28457, #9439, #17825, #58282, #65195, #61594, #26556, #33924, #42530, #19389, #31623, #57962, #173, #54996, #1545, #70613, #18933, #52253, #1641, #71948, #58448, #38640, #39141, #69885, #45738, #73694, #15612, #39572, #35403, #13789, #21989, #31532, #54358, #69112, #17940, #65186, #63445, #44583, #39320, #18673, #17421, #36066, #9416, #7380, #42560, #48971, #43733, #69157, #15836, #62811, #59296, #72832, #71646, #68074, #3208, #48979, #47508, #68383, #8140, #45401, #22854, #35534, #21608, #29686, #36816, #66869, #13304, #8994, #38364, #66349, #1511, #53787, #71238, #22370, #52231, #25253, #27690, #50939, #4276, #30871, #16400, #57880, #13257, #60670, #63893, #28752, #4993, #998, #36366, #32565, #35361, #59941, #33933, #19419, #417, #31546, #44571, #47699, #43185, #59176, #46302, #47157 ) ) ;
#56130=CYLINDRICAL_SURFACE ( 'NONE', #14095, 82.00000000000000000 ) ;
#56149=ORIENTED_EDGE ( 'NONE', *, *, #46944, .T. ) ;
#56154=DIRECTION ( 'NONE',  ( 0.000000000000000000, 0.000000000000000000, 1.000000000000000000 ) ) ;
#56158=DIRECTION ( 'NONE',  ( 0.000000000000000000, -0.07845909572785224328, 0.9969173337331274087 ) ) ;
#56159=CARTESIAN_POINT ( 'NONE',  ( 11.99999999999999822, -0.8261519478436571973, 77.49459641780886443 ) ) ;
#56161=ORIENTED_EDGE ( 'NONE', *, *, #21748, .F. ) ;
#56167=CYLINDRICAL_SURFACE ( 'NONE', #41139, 77.49899999999999523 ) ;
#56183=( NAMED_UNIT ( * ) SI_UNIT ( $, .STERADIAN. ) SOLID_ANGLE_UNIT ( ) );
#56184=ADVANCED_FACE ( 'NONE', ( #35633 ), #65340, .T. ) ;
#56192=EDGE_CURVE ( 'NONE', #27433, #68051, #58208, .T. ) ;
#56194=DIRECTION ( 'NONE',  ( -1.000000000000000000, 0.000000000000000000, 0.000000000000000000 ) ) ;
#56200=ADVANCED_FACE ( 'NONE', ( #2217 ), #7450, .F. ) ;
#56223=ORIENTED_EDGE ( 'NONE', *, *, #35648, .F. ) ;
#56229=DIRECTION ( 'NONE',  ( 0.000000000000000000, 0.1564344650402311743, -0.9876883405951376593 ) ) ;
#56231=CIRCLE ( 'NONE', #65835, 31.99999999999998934 ) ;
#56248=DIRECTION ( 'NONE',  ( -1.000000000000000000, 0.000000000000000000, 0.000000000000000000 ) ) ;
#56249=CARTESIAN_POINT ( 'NONE',  ( 11.99999999999999822, 0.000000000000000000, 0.000000000000000000 ) ) ;
#56250=DIRECTION ( 'NONE',  ( 0.000000000000000000, 0.9238795325112877377, -0.3826834323650873948 ) ) ;
#56257=ORIENTED_EDGE ( 'NONE', *, *, #38136, .T. ) ;
#56263=EDGE_LOOP ( 'NONE', ( #7941, #49207, #5748, #53724 ) ) ;
#56264=DIRECTION ( 'NONE',  ( 0.000000000000000000, 0.000000000000000000, 1.000000000000000000 ) ) ;
#56266=VECTOR ( 'NONE', #1306, 1000.000000000000000 ) ;
#56267=AXIS2_PLACEMENT_3D ( 'NONE', #51179, #68110, #67741 ) ;
#56268=EDGE_CURVE ( 'NONE', #40273, #8991, #46937, .T. ) ;
#56283=DIRECTION ( 'NONE',  ( 0.000000000000000000, 0.6691306063588579045, -0.7431448254773945772 ) ) ;
#56286=DIRECTION ( 'NONE',  ( 0.000000000000000000, 0.000000000000000000, 1.000000000000000000 ) ) ;
#56291=AXIS2_PLACEMENT_3D ( 'NONE', #37990, #32703, #15052 ) ;
#56293=CIRCLE ( 'NONE', #2284, 77.49899999999999523 ) ;
#56298=DIRECTION ( 'NONE',  ( 0.000000000000000000, -0.6691306063588579045, 0.7431448254773945772 ) ) ;
#56299=CARTESIAN_POINT ( 'NONE',  ( 11.99999999999999822, 0.000000000000000000, 0.000000000000000000 ) ) ;
#56302=EDGE_CURVE ( 'NONE', #49934, #16205, #73590, .T. ) ;
#56306=VECTOR ( 'NONE', #38763, 1000.000000000000000 ) ;
#56307=FACE_OUTER_BOUND ( 'NONE', #56408, .T. ) ;
#56310=DIRECTION ( 'NONE',  ( -1.000000000000000000, 0.000000000000000000, 0.000000000000000000 ) ) ;
#56314=AXIS2_PLACEMENT_3D ( 'NONE', #24587, #17834, #24233 ) ;
#56315=AXIS2_PLACEMENT_3D ( 'NONE', #8661, #37609, #42141 ) ;
#56320=DIRECTION ( 'NONE',  ( 1.000000000000000000, 0.000000000000000000, -0.000000000000000000 ) ) ;
#56329=CARTESIAN_POINT ( 'NONE',  ( 5.999999999999999112, 51.29473840253223216, 63.97538442413444670 ) ) ;
#56336=ORIENTED_EDGE ( 'NONE', *, *, #44243, .F. ) ;
#56338=CIRCLE ( 'NONE', #52737, 77.49900000000002365 ) ;
#56345=AXIS2_PLACEMENT_3D ( 'NONE', #25957, #15795, #60912 ) ;
#56352=CIRCLE ( 'NONE', #19139, 82.00000000000000000 ) ;
#56356=CARTESIAN_POINT ( 'NONE',  ( 0.000000000000000000, 0.000000000000000000, 0.000000000000000000 ) ) ;
#56361=DIRECTION ( 'NONE',  ( -1.000000000000000000, -0.000000000000000000, -0.000000000000000000 ) ) ;
#56374=DIRECTION ( 'NONE',  ( 0.000000000000000000, 0.000000000000000000, -1.000000000000000000 ) ) ;
#56382=DIRECTION ( 'NONE',  ( -1.000000000000000000, -0.000000000000000000, 0.000000000000000000 ) ) ;
#56387=ADVANCED_FACE ( 'NONE', ( #14560 ), #38236, .T. ) ;
#56390=FACE_OUTER_BOUND ( 'NONE', #24893, .T. ) ;
#56394=VECTOR ( 'NONE', #62758, 1000.000000000000000 ) ;
#56395=CIRCLE ( 'NONE', #15541, 31.99999999999998224 ) ;
#56400=ORIENTED_EDGE ( 'NONE', *, *, #67826, .F. ) ;
#56401=VECTOR ( 'NONE', #43753, 1000.000000000000000 ) ;
#56402=ORIENTED_EDGE ( 'NONE', *, *, #72110, .F. ) ;
#56408=EDGE_LOOP ( 'NONE', ( #46510, #23837, #21633, #8632 ) ) ;
#56410=ORIENTED_EDGE ( 'NONE', *, *, #23770, .T. ) ;
#56412=ORIENTED_EDGE ( 'NONE', *, *, #34555, .T. ) ;
#56414=CARTESIAN_POINT ( 'NONE',  ( 15.00000000000000000, 23.49999999999999645, -1.500000000000003997 ) ) ;
#56415=ORIENTED_EDGE ( 'NONE', *, *, #16144, .T. ) ;
#56433=EDGE_CURVE ( 'NONE', #12910, #7033, #16023, .T. ) ;
#56435=DIRECTION ( 'NONE',  ( -1.000000000000000000, 0.000000000000000000, -0.000000000000000000 ) ) ;
#56438=VERTEX_POINT ( 'NONE', #45003 ) ;
#56439=CARTESIAN_POINT ( 'NONE',  ( 15.00000000000000000, 0.000000000000000000, 0.000000000000000000 ) ) ;
#56442=CARTESIAN_POINT ( 'NONE',  ( 11.99999999999999822, -60.67117009219096957, -55.16347631943106933 ) ) ;
#56447=CARTESIAN_POINT ( 'NONE',  ( 6.000000000000000000, 76.69515212746057387, -29.01471420065479379 ) ) ;
#56452=CARTESIAN_POINT ( 'NONE',  ( 11.99999999999999822, 0.000000000000000000, 0.000000000000000000 ) ) ;
#56453=DIRECTION ( 'NONE',  ( 1.000000000000000000, 0.000000000000000000, -0.000000000000000000 ) ) ;
#56455=CARTESIAN_POINT ( 'NONE',  ( 11.99999999999999822, 0.000000000000000000, 0.000000000000000000 ) ) ;
#56456=AXIS2_PLACEMENT_3D ( 'NONE', #5766, #34318, #28672 ) ;
#56461=AXIS2_PLACEMENT_3D ( 'NONE', #69263, #64736, #59098 ) ;
#56478=LINE ( 'NONE', #68497, #41667 ) ;
#56485=AXIS2_PLACEMENT_3D ( 'NONE', #56749, #68397, #39823 ) ;
#56486=DIRECTION ( 'NONE',  ( 0.000000000000000000, 0.6494480483301793283, 0.7604059656000345946 ) ) ;
#56488=AXIS2_PLACEMENT_3D ( 'NONE', #33680, #39710, #61897 ) ;
#56507=AXIS2_PLACEMENT_3D ( 'NONE', #59161, #65180, #7652 ) ;
#56516=VERTEX_POINT ( 'NONE', #56662 ) ;
#56517=ORIENTED_EDGE ( 'NONE', *, *, #69987, .T. ) ;
#56527=EDGE_CURVE ( 'NONE', #28695, #22274, #17528, .T. ) ;
#56531=ADVANCED_FACE ( 'NONE', ( #51743 ), #50246, .T. ) ;
#56538=CARTESIAN_POINT ( 'NONE',  ( 11.99999999999999822, -26.02418014898260878, -70.52718814184285634 ) ) ;
#56545=VECTOR ( 'NONE', #7728, 1000.000000000000000 ) ;
#56566=VECTOR ( 'NONE', #10381, 999.9999999999998863 ) ;
#56570=CARTESIAN_POINT ( 'NONE',  ( 0.000000000000000000, 0.000000000000000000, 0.000000000000000000 ) ) ;
#56594=CIRCLE ( 'NONE', #17147, 77.49899999999999523 ) ;
#56599=EDGE_LOOP ( 'NONE', ( #28554, #55936, #774, #52923 ) ) ;
#56611=ADVANCED_FACE ( 'NONE', ( #29166 ), #69767, .T. ) ;
#56613=DIRECTION ( 'NONE',  ( -1.000000000000000000, 0.000000000000000000, 0.000000000000000000 ) ) ;
#56620=ORIENTED_EDGE ( 'NONE', *, *, #48873, .F. ) ;
#56634=ADVANCED_FACE ( 'NONE', ( #12618 ), #17896, .T. ) ;
#56641=ORIENTED_EDGE ( 'NONE', *, *, #68620, .T. ) ;
#56642=PRODUCT_DEFINITION_SHAPE ( 'NONE', 'NONE',  #29261 ) ;
#56646=LINE ( 'NONE', #62279, #36535 ) ;
#56648=VERTEX_POINT ( 'NONE', #41948 ) ;
#56656=AXIS2_PLACEMENT_3D ( 'NONE', #22993, #40642, #40271 ) ;
#56657=CARTESIAN_POINT ( 'NONE',  ( 12.00000000000000000, 24.81905959214260804, -9.408202855044828894 ) ) ;
#56662=CARTESIAN_POINT ( 'NONE',  ( 0.000000000000000000, 22.90783923731740401, -78.73519480814930205 ) ) ;
#56687=CYLINDRICAL_SURFACE ( 'NONE', #54293, 82.00000000000000000 ) ;
#56690=EDGE_CURVE ( 'NONE', #6124, #56906, #25619, .T. ) ;
#56695=DIRECTION ( 'NONE',  ( 0.000000000000000000, 0.000000000000000000, 1.000000000000000000 ) ) ;
#56700=VECTOR ( 'NONE', #5255, 1000.000000000000000 ) ;
#56710=CIRCLE ( 'NONE', #21861, 31.99999999999999289 ) ;
#56715=VECTOR ( 'NONE', #12316, 1000.000000000000000 ) ;
#56720=ORIENTED_EDGE ( 'NONE', *, *, #31137, .T. ) ;
#56732=DIRECTION ( 'NONE',  ( 0.000000000000000000, 0.000000000000000000, 1.000000000000000000 ) ) ;
#56738=ORIENTED_EDGE ( 'NONE', *, *, #68358, .T. ) ;
#56749=CARTESIAN_POINT ( 'NONE',  ( 0.000000000000000000, 0.000000000000000000, 0.000000000000000000 ) ) ;
#56759=DIRECTION ( 'NONE',  ( -1.000000000000000000, -0.000000000000000000, 0.000000000000000000 ) ) ;
#56760=AXIS2_PLACEMENT_3D ( 'NONE', #31347, #49005, #19326 ) ;
#56762=VECTOR ( 'NONE', #37777, 1000.000000000000227 ) ;
#56764=AXIS2_PLACEMENT_3D ( 'NONE', #50275, #23212, #51392 ) ;
#56765=FACE_OUTER_BOUND ( 'NONE', #48581, .T. ) ;
#56767=CYLINDRICAL_SURFACE ( 'NONE', #7800, 82.00000000000000000 ) ;
#56769=AXIS2_PLACEMENT_3D ( 'NONE', #44058, #10204, #9464 ) ;
#56771=ORIENTED_EDGE ( 'NONE', *, *, #59924, .F. ) ;
#56790=ORIENTED_EDGE ( 'NONE', *, *, #46094, .T. ) ;
#56792=VERTEX_POINT ( 'NONE', #54966 ) ;
#56795=EDGE_LOOP ( 'NONE', ( #63631, #56790, #36339, #3337 ) ) ;
#56802=CIRCLE ( 'NONE', #33985, 77.49900000000000944 ) ;
#56803=EDGE_LOOP ( 'NONE', ( #48700, #24065, #64629, #7297 ) ) ;
#56812=AXIS2_PLACEMENT_3D ( 'NONE', #3985, #73865, #27251 ) ;
#56814=DIRECTION ( 'NONE',  ( 0.000000000000000000, 0.000000000000000000, 1.000000000000000000 ) ) ;
#56823=CARTESIAN_POINT ( 'NONE',  ( 0.000000000000000000, -63.97538442413463855, 51.29473840253199057 ) ) ;
#56825=EDGE_CURVE ( 'NONE', #39476, #28106, #22246, .T. ) ;
#56827=EDGE_CURVE ( 'NONE', #70501, #62894, #25679, .T. ) ;
#56828=DIRECTION ( 'NONE',  ( 0.000000000000000000, 0.000000000000000000, 1.000000000000000000 ) ) ;
#56832=CARTESIAN_POINT ( 'NONE',  ( 11.99999999999999822, 0.000000000000000000, 0.000000000000000000 ) ) ;
#56835=CARTESIAN_POINT ( 'NONE',  ( 11.99999999999999822, -49.70050353004932475, 59.46389618801947563 ) ) ;
#56839=DIRECTION ( 'NONE',  ( 0.000000000000000000, 0.000000000000000000, 1.000000000000000000 ) ) ;
#56845=DIRECTION ( 'NONE',  ( 0.000000000000000000, 0.000000000000000000, 1.000000000000000000 ) ) ;
#56853=VERTEX_POINT ( 'NONE', #61732 ) ;
#56858=CIRCLE ( 'NONE', #36448, 31.99999999999997868 ) ;
#56860=LINE ( 'NONE', #45591, #63465 ) ;
#56862=EDGE_LOOP ( 'NONE', ( #5220, #42178, #10041, #66615 ) ) ;
#56865=FACE_OUTER_BOUND ( 'NONE', #39960, .T. ) ;
#56882=EDGE_CURVE ( 'NONE', #61291, #66432, #38890, .T. ) ;
#56885=AXIS2_PLACEMENT_3D ( 'NONE', #63111, #4475, #28871 ) ;
#56897=DIRECTION ( 'NONE',  ( 0.000000000000000000, 0.000000000000000000, 1.000000000000000000 ) ) ;
#56899=EDGE_CURVE ( 'NONE', #36914, #3905, #2904, .T. ) ;
#56906=VERTEX_POINT ( 'NONE', #52293 ) ;
#56907=CARTESIAN_POINT ( 'NONE',  ( 11.99999999999999822, -76.69515212746036070, 29.01471420065536932 ) ) ;
#56909=CARTESIAN_POINT ( 'NONE',  ( 11.99999999999999822, 62.50329211542435104, 41.76937507738811917 ) ) ;
#56927=CARTESIAN_POINT ( 'NONE',  ( 11.99999999999999822, 0.000000000000000000, 0.000000000000000000 ) ) ;
#56933=AXIS2_PLACEMENT_3D ( 'NONE', #15111, #38050, #3861 ) ;
#56936=CARTESIAN_POINT ( 'NONE',  ( 11.99999999999999822, -2.956366410620109519, -75.11725578898472122 ) ) ;
#56943=ORIENTED_EDGE ( 'NONE', *, *, #42262, .F. ) ;
#56944=CARTESIAN_POINT ( 'NONE',  ( 0.000000000000000000, 41.76106447765580043, -62.50884508063379741 ) ) ;
#56951=EDGE_CURVE ( 'NONE', #70850, #29463, #71273, .T. ) ;
#56953=DIRECTION ( 'NONE',  ( -1.000000000000000000, -0.000000000000000000, 0.000000000000000000 ) ) ;
#56976=VERTEX_POINT ( 'NONE', #34258 ) ;
#56989=CARTESIAN_POINT ( 'NONE',  ( 11.99999999999999822, 41.76937507738875155, -62.50329211542393892 ) ) ;
#56999=AXIS2_PLACEMENT_3D ( 'NONE', #36721, #70182, #2567 ) ;
#57000=DIRECTION ( 'NONE',  ( -1.000000000000000000, 0.000000000000000000, 0.000000000000000000 ) ) ;
#57007=ORIENTED_EDGE ( 'NONE', *, *, #28444, .F. ) ;
#57014=ORIENTED_EDGE ( 'NONE', *, *, #42369, .T. ) ;
#57027=AXIS2_PLACEMENT_3D ( 'NONE', #58733, #47812, #53091 ) ;
#57030=LINE ( 'NONE', #28439, #18181 ) ;
#57035=VECTOR ( 'NONE', #4618, 1000.000000000000000 ) ;
#57040=CARTESIAN_POINT ( 'NONE',  ( 15.00000000000000000, 9.615535125378766423, -24.73947219025917121 ) ) ;
#57041=DIRECTION ( 'NONE',  ( -0.000000000000000000, 0.7431448254773945772, 0.6691306063588579045 ) ) ;
#57042=DIRECTION ( 'NONE',  ( -1.000000000000000000, 0.000000000000000000, 0.000000000000000000 ) ) ;
#57043=CIRCLE ( 'NONE', #72621, 31.99999999999998579 ) ;
#57047=VECTOR ( 'NONE', #28334, 1000.000000000000000 ) ;
#57058=LINE ( 'NONE', #29561, #36960 ) ;
#57064=VERTEX_POINT ( 'NONE', #31571 ) ;
#57069=DIRECTION ( 'NONE',  ( -1.000000000000000000, 0.000000000000000000, 0.000000000000000000 ) ) ;
#57082=VECTOR ( 'NONE', #11650, 1000.000000000000000 ) ;
#57083=ORIENTED_EDGE ( 'NONE', *, *, #20042, .T. ) ;
#57088=ORIENTED_EDGE ( 'NONE', *, *, #32652, .T. ) ;
#57089=DIRECTION ( 'NONE',  ( -1.000000000000000000, 0.000000000000000000, -0.000000000000000000 ) ) ;
#57092=ORIENTED_EDGE ( 'NONE', *, *, #27075, .F. ) ;
#57093=VERTEX_POINT ( 'NONE', #25568 ) ;
#57098=APPLICATION_CONTEXT ( 'automotive_design' ) ;
#57099=DIRECTION ( 'NONE',  ( -1.000000000000000000, -0.000000000000000000, -0.000000000000000000 ) ) ;
#57104=DIRECTION ( 'NONE',  ( -1.000000000000000000, 0.000000000000000000, 0.000000000000000000 ) ) ;
#57108=DIRECTION ( 'NONE',  ( -1.000000000000000000, 0.000000000000000000, 0.000000000000000000 ) ) ;
#57122=CYLINDRICAL_SURFACE ( 'NONE', #18537, 82.00000000000000000 ) ;
#57124=ADVANCED_FACE ( 'NONE', ( #53040 ), #2687, .T. ) ;
#57134=EDGE_CURVE ( 'NONE', #45883, #719, #17307, .T. ) ;
#57141=ORIENTED_EDGE ( 'NONE', *, *, #28336, .F. ) ;
#57145=VECTOR ( 'NONE', #52364, 1000.000000000000000 ) ;
#57151=VERTEX_POINT ( 'NONE', #64690 ) ;
#57156=EDGE_LOOP ( 'NONE', ( #70280, #59536, #35945, #20324 ) ) ;
#57160=DIRECTION ( 'NONE',  ( 0.000000000000000000, 0.8526401643540936215, -0.5224985647159469115 ) ) ;
#57171=DIRECTION ( 'NONE',  ( -1.000000000000000000, -0.000000000000000000, -0.000000000000000000 ) ) ;
#57176=CARTESIAN_POINT ( 'NONE',  ( 11.99999999999999822, 0.000000000000000000, 0.000000000000000000 ) ) ;
#57189=DIRECTION ( 'NONE',  ( 0.000000000000000000, 0.3090169943749572767, 0.9510565162951503115 ) ) ;
#57191=VECTOR ( 'NONE', #59476, 1000.000000000000000 ) ;
#57202=DIRECTION ( 'NONE',  ( -1.000000000000000000, -0.000000000000000000, -0.000000000000000000 ) ) ;
#57207=ADVANCED_FACE ( 'NONE', ( #27413 ), #3404, .F. ) ;
#57209=CIRCLE ( 'NONE', #4409, 31.99999999999998579 ) ;
#57212=EDGE_CURVE ( 'NONE', #6635, #67063, #27796, .T. ) ;
#57214=CARTESIAN_POINT ( 'NONE',  ( 11.99999999999999822, 46.53671651293948486, 59.03961581697416250 ) ) ;
#57216=CARTESIAN_POINT ( 'NONE',  ( 0.000000000000000000, 0.000000000000000000, 0.000000000000000000 ) ) ;
#57219=CARTESIAN_POINT ( 'NONE',  ( 5.999999999999999112, 50.23322058963348979, 64.81221759200361987 ) ) ;
#57234=EDGE_LOOP ( 'NONE', ( #36045, #68729, #60155, #50598 ) ) ;
#57242=VERTEX_POINT ( 'NONE', #66180 ) ;
#57262=CARTESIAN_POINT ( 'NONE',  ( 15.00000000000000000, 23.59884966291521380, -12.14883922797262805 ) ) ;
#57268=VERTEX_POINT ( 'NONE', #37606 ) ;
#57283=FACE_OUTER_BOUND ( 'NONE', #19479, .T. ) ;
#57286=CIRCLE ( 'NONE', #29622, 82.00000000000000000 ) ;
#57291=ADVANCED_FACE ( 'NONE', ( #15022 ), #62020, .F. ) ;
#57292=CARTESIAN_POINT ( 'NONE',  ( 11.99999999999999822, 65.59268652807263322, -36.72794159290169347 ) ) ;
#57293=FACE_OUTER_BOUND ( 'NONE', #65771, .T. ) ;
#57296=CARTESIAN_POINT ( 'NONE',  ( 11.99999999999999822, 41.76937507738875155, -62.50329211542393892 ) ) ;
#57297=CARTESIAN_POINT ( 'NONE',  ( 0.000000000000000000, -68.67312586194971402, -35.91791733033549860 ) ) ;
#57301=ADVANCED_FACE ( 'NONE', ( #32308 ), #15393, .F. ) ;
#57305=DIRECTION ( 'NONE',  ( 0.000000000000000000, 0.000000000000000000, 1.000000000000000000 ) ) ;
#57310=CARTESIAN_POINT ( 'NONE',  ( 0.000000000000000000, -46.11716303203233736, 67.80270845531873647 ) ) ;
#57312=ADVANCED_FACE ( 'NONE', ( #23640 ), #57122, .T. ) ;
#57332=ORIENTED_EDGE ( 'NONE', *, *, #70345, .F. ) ;
#57340=DIRECTION ( 'NONE',  ( 0.000000000000000000, 0.000000000000000000, -1.000000000000000000 ) ) ;
#57341=DIRECTION ( 'NONE',  ( 0.000000000000000000, 0.000000000000000000, 1.000000000000000000 ) ) ;
#57342=AXIS2_PLACEMENT_3D ( 'NONE', #56570, #73830, #50905 ) ;
#57348=ORIENTED_EDGE ( 'NONE', *, *, #68945, .F. ) ;
#57359=DIRECTION ( 'NONE',  ( -1.000000000000000000, -0.000000000000000000, -0.000000000000000000 ) ) ;
#57361=ORIENTED_EDGE ( 'NONE', *, *, #67234, .T. ) ;
#57364=DIRECTION ( 'NONE',  ( 0.000000000000000000, 0.000000000000000000, 1.000000000000000000 ) ) ;
#57370=ADVANCED_FACE ( 'NONE', ( #62783 ), #52206, .F. ) ;
#57372=ADVANCED_FACE ( 'NONE', ( #40558 ), #51098, .T. ) ;
#57373=DIRECTION ( 'NONE',  ( 1.000000000000000000, -0.000000000000000000, 0.000000000000000000 ) ) ;
#57383=DIRECTION ( 'NONE',  ( 1.000000000000000000, 0.000000000000000000, 0.000000000000000000 ) ) ;
#57385=LINE ( 'NONE', #22817, #61361 ) ;
#57388=CARTESIAN_POINT ( 'NONE',  ( 11.99999999999999822, -55.19960302592029677, -51.03279382321147750 ) ) ;
#57404=EDGE_CURVE ( 'NONE', #37858, #71422, #11339, .T. ) ;
#57407=DIRECTION ( 'NONE',  ( 0.000000000000000000, -0.5877852522924625900, -0.8090169943749551118 ) ) ;
#57409=CIRCLE ( 'NONE', #2171, 31.99999999999998579 ) ;
#57413=AXIS2_PLACEMENT_3D ( 'NONE', #57699, #30217, #52793 ) ;
#57416=DIRECTION ( 'NONE',  ( 0.000000000000000000, 0.000000000000000000, 1.000000000000000000 ) ) ;
#57420=CARTESIAN_POINT ( 'NONE',  ( 15.00000000000000000, -0.9646360437375368635, -23.52805723605589705 ) ) ;
#57426=ORIENTED_EDGE ( 'NONE', *, *, #62508, .F. ) ;
#57435=CARTESIAN_POINT ( 'NONE',  ( 12.00000000000000000, -11.95096189432345923, -23.69967320028757030 ) ) ;
#57439=ORIENTED_EDGE ( 'NONE', *, *, #1576, .T. ) ;
#57444=EDGE_LOOP ( 'NONE', ( #46727, #11681, #36683, #15556 ) ) ;
#57449=DIRECTION ( 'NONE',  ( 0.000000000000000000, 0.9876883405951371042, 0.1564344650402347547 ) ) ;
#57451=ORIENTED_EDGE ( 'NONE', *, *, #47053, .T. ) ;
#57452=LINE ( 'NONE', #5968, #61536 ) ;
#57454=ORIENTED_EDGE ( 'NONE', *, *, #72291, .T. ) ;
#57458=FACE_BOUND ( 'NONE', #73138, .T. ) ;
#57468=CARTESIAN_POINT ( 'NONE',  ( 0.000000000000000000, 62.50329211542494789, -41.76937507738723099 ) ) ;
#57473=DIRECTION ( 'NONE',  ( 0.000000000000000000, 0.000000000000000000, -1.000000000000000000 ) ) ;
#57484=CIRCLE ( 'NONE', #31006, 77.49900000000000944 ) ;
#57486=FACE_OUTER_BOUND ( 'NONE', #21063, .T. ) ;
#57487=LINE ( 'NONE', #29625, #50538 ) ;
#57495=AXIS2_PLACEMENT_3D ( 'NONE', #42278, #14044, #65206 ) ;
#57499=( LENGTH_UNIT ( ) NAMED_UNIT ( * ) SI_UNIT ( .MILLI., .METRE. ) );
#57505=VECTOR ( 'NONE', #59698, 1000.000000000000000 ) ;
#57513=VERTEX_POINT ( 'NONE', #66010 ) ;
#57523=CARTESIAN_POINT ( 'NONE',  ( 11.99999999999999822, -18.89407956138310496, 75.16055320797023853 ) ) ;
#57524=CIRCLE ( 'NONE', #40731, 31.99999999999998934 ) ;
#57526=DIRECTION ( 'NONE',  ( -1.000000000000000000, 0.000000000000000000, 0.000000000000000000 ) ) ;
#57531=EDGE_CURVE ( 'NONE', #6316, #42183, #22145, .T. ) ;
#57533=AXIS2_PLACEMENT_3D ( 'NONE', #6555, #44933, #11083 ) ;
#57537=ORIENTED_EDGE ( 'NONE', *, *, #64333, .T. ) ;
#57539=FACE_OUTER_BOUND ( 'NONE', #72221, .T. ) ;
#57542=EDGE_CURVE ( 'NONE', #11201, #47808, #4173, .T. ) ;
#57551=PLANE ( 'NONE',  #33506 ) ;
#57566=DIRECTION ( 'NONE',  ( -1.000000000000000000, -0.000000000000000000, -0.000000000000000000 ) ) ;
#57568=CARTESIAN_POINT ( 'NONE',  ( 5.999999999999999112, -64.81221759200379040, 50.23322058963324110 ) ) ;
#57573=CARTESIAN_POINT ( 'NONE',  ( 11.99999999999999822, -74.65491531819111515, -8.830959090343204920 ) ) ;
#57576=EDGE_CURVE ( 'NONE', #62322, #6316, #28727, .T. ) ;
#57582=DIRECTION ( 'NONE',  ( -1.000000000000000000, -0.000000000000000000, -0.000000000000000000 ) ) ;
#57584=CARTESIAN_POINT ( 'NONE',  ( 11.99999999999999822, 0.000000000000000000, 0.000000000000000000 ) ) ;
#57598=DIRECTION ( 'NONE',  ( -1.000000000000000000, 0.000000000000000000, 0.000000000000000000 ) ) ;
#57600=ORIENTED_EDGE ( 'NONE', *, *, #12544, .T. ) ;
#57602=FACE_OUTER_BOUND ( 'NONE', #33927, .T. ) ;
#57611=ORIENTED_EDGE ( 'NONE', *, *, #25974, .T. ) ;
#57615=ORIENTED_EDGE ( 'NONE', *, *, #51808, .F. ) ;
#57616=CARTESIAN_POINT ( 'NONE',  ( 11.99999999999999822, -17.28742895386031719, -75.54627589209962935 ) ) ;
#57625=EDGE_CURVE ( 'NONE', #3632, #57151, #37767, .T. ) ;
#57632=AXIS2_PLACEMENT_3D ( 'NONE', #65232, #41548, #24625 ) ;
#57634=CYLINDRICAL_SURFACE ( 'NONE', #73801, 31.99999999999998579 ) ;
#57658=VERTEX_POINT ( 'NONE', #68601 ) ;
#57664=CARTESIAN_POINT ( 'NONE',  ( 15.00000000000000000, 6.762365576493310826, -25.66652317338401090 ) ) ;
#57669=CIRCLE ( 'NONE', #45659, 77.49899999999999523 ) ;
#57670=DIRECTION ( 'NONE',  ( 0.000000000000000000, 2.312964634635746211E-15, -1.000000000000000000 ) ) ;
#57671=VECTOR ( 'NONE', #58120, 1000.000000000000227 ) ;
#57680=EDGE_CURVE ( 'NONE', #63817, #22572, #24573, .T. ) ;
#57689=CIRCLE ( 'NONE', #64925, 31.99999999999999289 ) ;
#57690=AXIS2_PLACEMENT_3D ( 'NONE', #11642, #51885, #69902 ) ;
#57691=VECTOR ( 'NONE', #19665, 1000.000000000000000 ) ;
#57699=CARTESIAN_POINT ( 'NONE',  ( 11.99999999999999822, 0.000000000000000000, 0.000000000000000000 ) ) ;
#57715=AXIS2_PLACEMENT_3D ( 'NONE', #54325, #2851, #26849 ) ;
#57722=FACE_OUTER_BOUND ( 'NONE', #5433, .T. ) ;
#57729=ORIENTED_EDGE ( 'NONE', *, *, #52108, .F. ) ;
#57743=EDGE_LOOP ( 'NONE', ( #18561, #64639, #64301, #25900 ) ) ;
#57757=CARTESIAN_POINT ( 'NONE',  ( 0.000000000000000000, 24.73286445877704764, 73.44644590900067271 ) ) ;
#57763=DIRECTION ( 'NONE',  ( 0.000000000000000000, 0.000000000000000000, 1.000000000000000000 ) ) ;
#57764=DIRECTION ( 'NONE',  ( -1.000000000000000000, 0.000000000000000000, 0.000000000000000000 ) ) ;
#57768=ORIENTED_EDGE ( 'NONE', *, *, #63252, .F. ) ;
#57771=CIRCLE ( 'NONE', #26571, 77.49900000000000944 ) ;
#57773=CIRCLE ( 'NONE', #9728, 31.99999999999998579 ) ;
#57775=ORIENTED_EDGE ( 'NONE', *, *, #13913, .T. ) ;
#57778=CARTESIAN_POINT ( 'NONE',  ( 0.000000000000000000, 74.18225833017937987, -34.94270380257559339 ) ) ;
#57779=CIRCLE ( 'NONE', #28950, 82.00000000000000000 ) ;
#57789=DIRECTION ( 'NONE',  ( -1.000000000000000000, -0.000000000000000000, -0.000000000000000000 ) ) ;
#57800=ORIENTED_EDGE ( 'NONE', *, *, #69019, .F. ) ;
#57801=ORIENTED_EDGE ( 'NONE', *, *, #65110, .T. ) ;
#57809=VERTEX_POINT ( 'NONE', #37344 ) ;
#57823=CIRCLE ( 'NONE', #16979, 82.00000000000000000 ) ;
#57830=AXIS2_PLACEMENT_3D ( 'NONE', #69300, #6884, #1662 ) ;
#57839=EDGE_LOOP ( 'NONE', ( #19718, #64271, #2748, #48630 ) ) ;
#57852=CARTESIAN_POINT ( 'NONE',  ( 11.99999999999999822, 69.42325613327440692, 34.44570377933622041 ) ) ;
#57859=CARTESIAN_POINT ( 'NONE',  ( 12.00000000000000000, -22.32062822937469093, 14.36278369418830181 ) ) ;
#57865=DIRECTION ( 'NONE',  ( 0.000000000000000000, -0.2334453638558922350, -0.9723699203976797767 ) ) ;
#57867=CARTESIAN_POINT ( 'NONE',  ( 12.00000000000000000, 6.762365576493310826, -25.66652317338400735 ) ) ;
#57870=CIRCLE ( 'NONE', #51852, 31.99999999999998934 ) ;
#57874=ORIENTED_EDGE ( 'NONE', *, *, #53622, .T. ) ;
#57878=VECTOR ( 'NONE', #67808, 1000.000000000000000 ) ;
#57880=ORIENTED_EDGE ( 'NONE', *, *, #73220, .F. ) ;
#57882=AXIS2_PLACEMENT_3D ( 'NONE', #60401, #2907, #43109 ) ;
#57886=ADVANCED_FACE ( 'NONE', ( #26038 ), #25317, .T. ) ;
#57887=EDGE_CURVE ( 'NONE', #51530, #33478, #71897, .T. ) ;
#57888=VERTEX_POINT ( 'NONE', #43364 ) ;
#57890=ORIENTED_EDGE ( 'NONE', *, *, #43055, .T. ) ;
#57894=CIRCLE ( 'NONE', #11088, 82.00000000000000000 ) ;
#57897=VERTEX_POINT ( 'NONE', #72627 ) ;
#57904=ADVANCED_FACE ( 'NONE', ( #3879 ), #42607, .T. ) ;
#57905=ORIENTED_EDGE ( 'NONE', *, *, #8821, .T. ) ;
#57909=CARTESIAN_POINT ( 'NONE',  ( 0.000000000000000000, 0.000000000000000000, 0.000000000000000000 ) ) ;
#57910=CYLINDRICAL_SURFACE ( 'NONE', #42632, 82.00000000000000000 ) ;
#57914=CARTESIAN_POINT ( 'NONE',  ( 0.000000000000000000, 51.02545421589324803, 55.20638768913779870 ) ) ;
#57917=EDGE_CURVE ( 'NONE', #51812, #66208, #72609, .T. ) ;
#57931=AXIS2_PLACEMENT_3D ( 'NONE', #40048, #58440, #57340 ) ;
#57939=AXIS2_PLACEMENT_3D ( 'NONE', #65319, #13427, #29972 ) ;
#57940=ORIENTED_EDGE ( 'NONE', *, *, #33896, .T. ) ;
#57955=EDGE_CURVE ( 'NONE', #55521, #51812, #71526, .T. ) ;
#57960=EDGE_CURVE ( 'NONE', #64440, #22274, #37816, .T. ) ;
#57962=ORIENTED_EDGE ( 'NONE', *, *, #34809, .F. ) ;
#57975=ORIENTED_EDGE ( 'NONE', *, *, #33725, .F. ) ;
#57983=ADVANCED_FACE ( 'NONE', ( #41307 ), #6724, .T. ) ;
#57990=VECTOR ( 'NONE', #63870, 1000.000000000000000 ) ;
#57996=DIRECTION ( 'NONE',  ( -1.000000000000000000, -0.000000000000000000, -0.000000000000000000 ) ) ;
#58000=EDGE_CURVE ( 'NONE', #70160, #62821, #67375, .T. ) ;
#58005=DIRECTION ( 'NONE',  ( 0.000000000000000000, 0.000000000000000000, 1.000000000000000000 ) ) ;
#58006=CARTESIAN_POINT ( 'NONE',  ( 11.99999999999999822, 59.75363087400153006, -56.15606465354896670 ) ) ;
#58013=VERTEX_POINT ( 'NONE', #69866 ) ;
#58014=ORIENTED_EDGE ( 'NONE', *, *, #17134, .F. ) ;
#58019=DIRECTION ( 'NONE',  ( -1.000000000000000000, 0.000000000000000000, 0.000000000000000000 ) ) ;
#58020=CIRCLE ( 'NONE', #67623, 77.49899999999999523 ) ;
#58024=ORIENTED_EDGE ( 'NONE', *, *, #55431, .F. ) ;
#58041=DIRECTION ( 'NONE',  ( 0.000000000000000000, -0.4539904997395541875, 0.8910065241883641241 ) ) ;
#58044=AXIS2_PLACEMENT_3D ( 'NONE', #6351, #24733, #24005 ) ;
#58048=ADVANCED_FACE ( 'NONE', ( #9863 ), #62117, .T. ) ;
#58049=EDGE_CURVE ( 'NONE', #38445, #72240, #19760, .T. ) ;
#58057=ORIENTED_EDGE ( 'NONE', *, *, #39970, .T. ) ;
#58058=EDGE_CURVE ( 'NONE', #25980, #21350, #55834, .T. ) ;
#58068=EDGE_CURVE ( 'NONE', #68327, #64494, #18583, .T. ) ;
#58081=DIRECTION ( 'NONE',  ( -1.000000000000000000, -0.000000000000000000, 0.000000000000000000 ) ) ;
#58095=AXIS2_PLACEMENT_3D ( 'NONE', #26344, #72922, #54915 ) ;
#58100=CYLINDRICAL_SURFACE ( 'NONE', #9084, 31.99999999999998579 ) ;
#58101=DIRECTION ( 'NONE',  ( -1.000000000000000000, -0.000000000000000000, -0.000000000000000000 ) ) ;
#58102=LINE ( 'NONE', #47925, #37826 ) ;
#58104=CIRCLE ( 'NONE', #59275, 82.00000000000000000 ) ;
#58108=ORIENTED_EDGE ( 'NONE', *, *, #18162, .F. ) ;
#58109=VERTEX_POINT ( 'NONE', #48421 ) ;
#58120=DIRECTION ( 'NONE',  ( -0.000000000000000000, -0.3090169943749572767, -0.9510565162951503115 ) ) ;
#58121=CARTESIAN_POINT ( 'NONE',  ( 11.99999999999999822, 74.65491531819118620, -8.830959090342659579 ) ) ;
#58131=EDGE_CURVE ( 'NONE', #34691, #45762, #9032, .T. ) ;
#58133=AXIS2_PLACEMENT_3D ( 'NONE', #12474, #70339, #7942 ) ;
#58139=CIRCLE ( 'NONE', #36493, 31.99999999999998579 ) ;
#58157=CIRCLE ( 'NONE', #34113, 77.49900000000000944 ) ;
#58158=ORIENTED_EDGE ( 'NONE', *, *, #47954, .T. ) ;
#58163=EDGE_CURVE ( 'NONE', #51303, #72289, #59714, .T. ) ;
#58166=CYLINDRICAL_SURFACE ( 'NONE', #11333, 31.99999999999998579 ) ;
#58187=ORIENTED_EDGE ( 'NONE', *, *, #54552, .T. ) ;
#58195=AXIS2_PLACEMENT_3D ( 'NONE', #53420, #31222, #71799 ) ;
#58199=ORIENTED_EDGE ( 'NONE', *, *, #42173, .T. ) ;
#58200=ORIENTED_EDGE ( 'NONE', *, *, #61614, .T. ) ;
#58208=LINE ( 'NONE', #30730, #18369 ) ;
#58209=DIRECTION ( 'NONE',  ( -1.000000000000000000, -0.000000000000000000, 0.000000000000000000 ) ) ;
#58221=LINE ( 'NONE', #36389, #49253 ) ;
#58222=AXIS2_PLACEMENT_3D ( 'NONE', #25487, #14573, #48418 ) ;
#58228=LINE ( 'NONE', #19475, #64749 ) ;
#58237=EDGE_CURVE ( 'NONE', #2536, #68158, #42639, .T. ) ;
#58238=CARTESIAN_POINT ( 'NONE',  ( 11.99999999999999822, 0.000000000000000000, 0.000000000000000000 ) ) ;
#58242=CIRCLE ( 'NONE', #41451, 31.99999999999998579 ) ;
#58243=ORIENTED_EDGE ( 'NONE', *, *, #55094, .T. ) ;
#58250=VERTEX_POINT ( 'NONE', #19107 ) ;
#58252=ADVANCED_FACE ( 'NONE', ( #18729 ), #42056, .F. ) ;
#58253=CARTESIAN_POINT ( 'NONE',  ( 11.99999999999999822, 0.000000000000000000, 0.000000000000000000 ) ) ;
#58254=AXIS2_PLACEMENT_3D ( 'NONE', #46930, #34909, #7442 ) ;
#58259=ORIENTED_EDGE ( 'NONE', *, *, #70782, .T. ) ;
#58262=CARTESIAN_POINT ( 'NONE',  ( 11.99999999999999822, 0.000000000000000000, 0.000000000000000000 ) ) ;
#58271=CARTESIAN_POINT ( 'NONE',  ( 0.000000000000000000, 81.50828551894227303, 8.966570791700986476 ) ) ;
#58276=DIRECTION ( 'NONE',  ( 0.000000000000000000, 0.8090169943749445647, 0.5877852522924770229 ) ) ;
#58277=CARTESIAN_POINT ( 'NONE',  ( 11.99999999999999822, -55.19960302592104284, 51.03279382321070301 ) ) ;
#58282=ORIENTED_EDGE ( 'NONE', *, *, #23857, .F. ) ;
#58291=CARTESIAN_POINT ( 'NONE',  ( 0.000000000000000000, 0.000000000000000000, 0.000000000000000000 ) ) ;
#58293=LINE ( 'NONE', #39908, #54138 ) ;
#58302=EDGE_LOOP ( 'NONE', ( #24599, #3710, #68243, #44172 ) ) ;
#58306=CIRCLE ( 'NONE', #18689, 77.49899999999999523 ) ;
#58314=AXIS2_PLACEMENT_3D ( 'NONE', #72688, #22710, #51258 ) ;
#58315=AXIS2_PLACEMENT_3D ( 'NONE', #45646, #50512, #21946 ) ;
#58316=EDGE_LOOP ( 'NONE', ( #38063, #64452, #62594, #14941 ) ) ;
#58318=DIRECTION ( 'NONE',  ( 0.000000000000000000, 0.000000000000000000, 1.000000000000000000 ) ) ;
#58321=DIRECTION ( 'NONE',  ( -1.000000000000000000, -0.000000000000000000, 0.000000000000000000 ) ) ;
#58324=EDGE_CURVE ( 'NONE', #43683, #15633, #10214, .T. ) ;
#58325=CARTESIAN_POINT ( 'NONE',  ( 0.000000000000000000, 44.88180994100376608, 63.18004540533043922 ) ) ;
#58336=ORIENTED_EDGE ( 'NONE', *, *, #43564, .F. ) ;
#58344=ORIENTED_EDGE ( 'NONE', *, *, #12629, .F. ) ;
#58351=ORIENTED_EDGE ( 'NONE', *, *, #1426, .F. ) ;
#58355=AXIS2_PLACEMENT_3D ( 'NONE', #39934, #68875, #17724 ) ;
#58358=CIRCLE ( 'NONE', #41564, 31.99999999999999289 ) ;
#58359=CARTESIAN_POINT ( 'NONE',  ( 15.00000000000000000, 6.762365576493647445, 25.66652317338391498 ) ) ;
#58366=VECTOR ( 'NONE', #56453, 1000.000000000000000 ) ;
#58374=LINE ( 'NONE', #13252, #23337 ) ;
#58377=LINE ( 'NONE', #12139, #57145 ) ;
#58379=ORIENTED_EDGE ( 'NONE', *, *, #17815, .F. ) ;
#58380=CIRCLE ( 'NONE', #781, 31.99999999999998224 ) ;
#58387=PLANE ( 'NONE',  #57830 ) ;
#58396=DIRECTION ( 'NONE',  ( -1.000000000000000000, 0.000000000000000000, 0.000000000000000000 ) ) ;
#58405=DIRECTION ( 'NONE',  ( -1.000000000000000000, -0.000000000000000000, -0.000000000000000000 ) ) ;
#58410=AXIS2_PLACEMENT_3D ( 'NONE', #63279, #30514, #36529 ) ;
#58416=ADVANCED_FACE ( 'NONE', ( #14952 ), #37894, .T. ) ;
#58417=CIRCLE ( 'NONE', #44042, 82.00000000000000000 ) ;
#58418=CARTESIAN_POINT ( 'NONE',  ( 11.99999999999999822, 51.03279382321088065, 55.19960302592086521 ) ) ;
#58419=ORIENTED_EDGE ( 'NONE', *, *, #2156, .T. ) ;
#58422=CARTESIAN_POINT ( 'NONE',  ( 11.99999999999999822, 49.70050353004889132, 59.46389618801982380 ) ) ;
#58423=AXIS2_PLACEMENT_3D ( 'NONE', #47329, #70233, #46963 ) ;
#58429=EDGE_LOOP ( 'NONE', ( #44560, #53530, #47338, #1332 ) ) ;
#58437=ORIENTED_EDGE ( 'NONE', *, *, #16617, .T. ) ;
#58440=DIRECTION ( 'NONE',  ( 1.000000000000000000, 0.000000000000000000, 0.000000000000000000 ) ) ;
#58442=DIRECTION ( 'NONE',  ( -1.000000000000000000, 0.000000000000000000, 0.000000000000000000 ) ) ;
#58448=ORIENTED_EDGE ( 'NONE', *, *, #51793, .F. ) ;
#58455=AXIS2_PLACEMENT_3D ( 'NONE', #19532, #53025, #48846 ) ;
#58467=ORIENTED_EDGE ( 'NONE', *, *, #13212, .T. ) ;
#58468=ADVANCED_FACE ( 'NONE', ( #16815 ), #28825, .F. ) ;
#58477=CIRCLE ( 'NONE', #21214, 82.00000000000000000 ) ;
#58487=AXIS2_PLACEMENT_3D ( 'NONE', #6473, #69244, #34659 ) ;
#58489=EDGE_CURVE ( 'NONE', #71472, #43291, #60675, .T. ) ;
#58500=ORIENTED_EDGE ( 'NONE', *, *, #43706, .T. ) ;
#58501=EDGE_CURVE ( 'NONE', #63724, #42793, #3058, .T. ) ;
#58507=ADVANCED_FACE ( 'NONE', ( #17181 ), #34095, .F. ) ;
#58518=DIRECTION ( 'NONE',  ( -1.000000000000000000, -0.000000000000000000, -0.000000000000000000 ) ) ;
#58524=VERTEX_POINT ( 'NONE', #40113 ) ;
#58534=ORIENTED_EDGE ( 'NONE', *, *, #23597, .T. ) ;
#58541=VERTEX_POINT ( 'NONE', #33727 ) ;
#58542=DIRECTION ( 'NONE',  ( -1.000000000000000000, 0.000000000000000000, -0.000000000000000000 ) ) ;
#58554=ADVANCED_FACE ( 'NONE', ( #21249 ), #38189, .F. ) ;
#58555=EDGE_CURVE ( 'NONE', #50077, #30232, #70245, .T. ) ;
#58556=DIRECTION ( 'NONE',  ( 0.000000000000000000, 0.000000000000000000, 1.000000000000000000 ) ) ;
#58561=CIRCLE ( 'NONE', #51368, 77.49899999999999523 ) ;
#58564=CIRCLE ( 'NONE', #40540, 31.99999999999999289 ) ;
#58573=LINE ( 'NONE', #1845, #2586 ) ;
#58576=ADVANCED_FACE ( 'NONE', ( #9623 ), #44956, .T. ) ;
#58591=ORIENTED_EDGE ( 'NONE', *, *, #66488, .T. ) ;
#58607=CIRCLE ( 'NONE', #44184, 31.99999999999998934 ) ;
#58613=CARTESIAN_POINT ( 'NONE',  ( 15.00000000000000000, -0.9646360437375368635, -23.52805723605589705 ) ) ;
#58615=DIRECTION ( 'NONE',  ( -1.000000000000000000, 0.000000000000000000, 0.000000000000000000 ) ) ;
#58617=VERTEX_POINT ( 'NONE', #39314 ) ;
#58621=EDGE_LOOP ( 'NONE', ( #6472, #33296, #41280, #65003 ) ) ;
#58625=ORIENTED_EDGE ( 'NONE', *, *, #17800, .F. ) ;
#58629=CIRCLE ( 'NONE', #23860, 77.49900000000000944 ) ;
#58632=ORIENTED_EDGE ( 'NONE', *, *, #52049, .T. ) ;
#58640=ORIENTED_EDGE ( 'NONE', *, *, #10185, .T. ) ;
#58643=CIRCLE ( 'NONE', #37021, 31.99999999999999645 ) ;
#58648=DIRECTION ( 'NONE',  ( 0.000000000000000000, 0.000000000000000000, 1.000000000000000000 ) ) ;
#58657=LINE ( 'NONE', #40258, #23570 ) ;
#58658=DIRECTION ( 'NONE',  ( 0.000000000000000000, 0.000000000000000000, -1.000000000000000000 ) ) ;
#58659=DIRECTION ( 'NONE',  ( 0.000000000000000000, -0.9781476007338041345, 0.2079116908177663092 ) ) ;
#58662=CARTESIAN_POINT ( 'NONE',  ( 6.000000000000000000, -81.96053171279903893, 2.543863470248107994 ) ) ;
#58666=EDGE_CURVE ( 'NONE', #73333, #69147, #58306, .T. ) ;
#58678=EDGE_CURVE ( 'NONE', #40792, #5889, #6684, .T. ) ;
#58699=ORIENTED_EDGE ( 'NONE', *, *, #52550, .T. ) ;
#58710=EDGE_LOOP ( 'NONE', ( #4636, #29132, #5925, #42088 ) ) ;
#58723=AXIS2_PLACEMENT_3D ( 'NONE', #54280, #47889, #2807 ) ;
#58729=ORIENTED_EDGE ( 'NONE', *, *, #6285, .F. ) ;
#58733=CARTESIAN_POINT ( 'NONE',  ( 0.000000000000000000, 0.000000000000000000, 0.000000000000000000 ) ) ;
#58748=DIRECTION ( 'NONE',  ( 0.000000000000000000, 0.5000000000000028866, 0.8660254037844369313 ) ) ;
#58753=AXIS2_PLACEMENT_3D ( 'NONE', #8730, #26009, #66612 ) ;
#58757=DIRECTION ( 'NONE',  ( 0.000000000000000000, 0.7604059656000322631, -0.6494480483301821039 ) ) ;
#58764=CARTESIAN_POINT ( 'NONE',  ( 12.00000000000000000, -3.948201729842032215, 23.21447184625297666 ) ) ;
#58766=DIRECTION ( 'NONE',  ( 0.000000000000000000, 0.000000000000000000, 1.000000000000000000 ) ) ;
#58771=DIRECTION ( 'NONE',  ( -1.000000000000000000, 0.000000000000000000, 0.000000000000000000 ) ) ;
#58782=LINE ( 'NONE', #54258, #2228 ) ;
#58783=AXIS2_PLACEMENT_3D ( 'NONE', #49155, #31856, #20591 ) ;
#58785=DIRECTION ( 'NONE',  ( -1.000000000000000000, -0.000000000000000000, 0.000000000000000000 ) ) ;
#58786=ORIENTED_EDGE ( 'NONE', *, *, #21613, .T. ) ;
#58787=DIRECTION ( 'NONE',  ( -1.000000000000000000, 0.000000000000000000, 0.000000000000000000 ) ) ;
#58798=CARTESIAN_POINT ( 'NONE',  ( 11.99999999999999822, 75.16055320797057959, -18.89407956138179046 ) ) ;
#58803=VERTEX_POINT ( 'NONE', #69352 ) ;
#58805=EDGE_CURVE ( 'NONE', #34202, #4754, #42696, .T. ) ;
#58809=CARTESIAN_POINT ( 'NONE',  ( 11.99999999999999822, -69.42325613327466272, 34.44570377933573724 ) ) ;
#58816=VERTEX_POINT ( 'NONE', #58824 ) ;
#58819=EDGE_CURVE ( 'NONE', #4632, #61610, #46339, .T. ) ;
#58824=CARTESIAN_POINT ( 'NONE',  ( 0.000000000000000000, -58.39081064771713869, -50.95692526931392052 ) ) ;
#58828=DIRECTION ( 'NONE',  ( 0.000000000000000000, 0.000000000000000000, 1.000000000000000000 ) ) ;
#58838=EDGE_CURVE ( 'NONE', #24230, #64851, #21096, .T. ) ;
#58842=FACE_OUTER_BOUND ( 'NONE', #49202, .T. ) ;
#58843=DIRECTION ( 'NONE',  ( 0.000000000000000000, 0.4999999999999931166, -0.8660254037844427044 ) ) ;
#58845=ADVANCED_BREP_SHAPE_REPRESENTATION ( '', ( #37031, #43395 ), #46970 ) ;
#58851=CIRCLE ( 'NONE', #20415, 31.99999999999998934 ) ;
#58856=DIRECTION ( 'NONE',  ( -1.000000000000000000, -0.000000000000000000, 0.000000000000000000 ) ) ;
#58864=AXIS2_PLACEMENT_3D ( 'NONE', #22321, #38870, #44892 ) ;
#58866=CARTESIAN_POINT ( 'NONE',  ( 11.99999999999999822, 63.97538442413500093, -51.29473840253155714 ) ) ;
#58870=FACE_OUTER_BOUND ( 'NONE', #25897, .T. ) ;
#58875=PLANE ( 'NONE',  #67031 ) ;
#58885=ORIENTED_EDGE ( 'NONE', *, *, #1852, .T. ) ;
#58888=ORIENTED_EDGE ( 'NONE', *, *, #70742, .F. ) ;
#58889=VECTOR ( 'NONE', #25296, 1000.000000000000000 ) ;
#58891=CIRCLE ( 'NONE', #72081, 77.49899999999998101 ) ;
#58893=LINE ( 'NONE', #5923, #70237 ) ;
#58902=DIRECTION ( 'NONE',  ( 0.000000000000000000, 0.000000000000000000, 1.000000000000000000 ) ) ;
#58919=CARTESIAN_POINT ( 'NONE',  ( 50.00005079999999680, 0.000000000000000000, 0.000000000000000000 ) ) ;
#58925=LINE ( 'NONE', #64939, #8625 ) ;
#58927=ORIENTED_EDGE ( 'NONE', *, *, #5710, .T. ) ;
#58930=EDGE_CURVE ( 'NONE', #12008, #10460, #64839, .T. ) ;
#58932=CARTESIAN_POINT ( 'NONE',  ( 11.99999999999999822, 0.000000000000000000, 0.000000000000000000 ) ) ;
#58933=CARTESIAN_POINT ( 'NONE',  ( 11.99999999999999822, 0.000000000000000000, 0.000000000000000000 ) ) ;
#58938=EDGE_CURVE ( 'NONE', #63634, #21751, #66325, .T. ) ;
#58942=DIRECTION ( 'NONE',  ( -1.000000000000000000, 0.000000000000000000, 0.000000000000000000 ) ) ;
#58947=ORIENTED_EDGE ( 'NONE', *, *, #53632, .F. ) ;
#58952=CIRCLE ( 'NONE', #22942, 82.00000000000000000 ) ;
#58959=CARTESIAN_POINT ( 'NONE',  ( 0.000000000000000000, -72.35160999960831418, 20.41045688087797672 ) ) ;
#58962=DIRECTION ( 'NONE',  ( -1.000000000000000000, 0.000000000000000000, 0.000000000000000000 ) ) ;
#58964=DIRECTION ( 'NONE',  ( 0.000000000000000000, -0.3090169943749350168, -0.9510565162951576390 ) ) ;
#58965=LINE ( 'NONE', #30370, #69636 ) ;
#58974=ORIENTED_EDGE ( 'NONE', *, *, #47359, .T. ) ;
#58980=DIRECTION ( 'NONE',  ( 0.000000000000000000, -0.5877852522924779111, -0.8090169943749440096 ) ) ;
#58982=EDGE_CURVE ( 'NONE', #15793, #46178, #31881, .T. ) ;
#58989=ADVANCED_FACE ( 'NONE', ( #19325 ), #71565, .T. ) ;
#59006=CARTESIAN_POINT ( 'NONE',  ( 12.00000000000000000, 26.49999999999999645, 1.499999999999995781 ) ) ;
#59007=AXIS2_PLACEMENT_3D ( 'NONE', #56249, #67153, #73150 ) ;
#59014=ORIENTED_EDGE ( 'NONE', *, *, #58324, .F. ) ;
#59019=CIRCLE ( 'NONE', #63800, 82.00000000000000000 ) ;
#59020=EDGE_CURVE ( 'NONE', #14313, #15645, #43928, .T. ) ;
#59036=DIRECTION ( 'NONE',  ( 0.000000000000000000, -0.7604059656000227152, -0.6494480483301934282 ) ) ;
#59038=ORIENTED_EDGE ( 'NONE', *, *, #30623, .T. ) ;
#59043=CARTESIAN_POINT ( 'NONE',  ( 6.000000000000000000, -3.894527615417333610, -81.90746397400393164 ) ) ;
#59047=CYLINDRICAL_SURFACE ( 'NONE', #26685, 82.00000000000000000 ) ;
#59062=CARTESIAN_POINT ( 'NONE',  ( 0.000000000000000000, 72.35432306680455383, 20.40083707023012494 ) ) ;
#59069=LINE ( 'NONE', #25225, #12567 ) ;
#59072=EDGE_CURVE ( 'NONE', #15793, #49934, #33193, .T. ) ;
#59079=ADVANCED_FACE ( 'NONE', ( #45240 ), #66681, .T. ) ;
#59088=EDGE_LOOP ( 'NONE', ( #65573, #8685, #67589, #31614 ) ) ;
#59089=ORIENTED_EDGE ( 'NONE', *, *, #35146, .F. ) ;
#59098=DIRECTION ( 'NONE',  ( 0.000000000000000000, 0.2334453638559060851, -0.9723699203976764460 ) ) ;
#59106=EDGE_CURVE ( 'NONE', #15149, #27433, #20994, .T. ) ;
#59107=EDGE_CURVE ( 'NONE', #33770, #47439, #61958, .T. ) ;
#59110=DIRECTION ( 'NONE',  ( 0.000000000000000000, 0.9510565162951510887, -0.3090169943749551673 ) ) ;
#59111=CARTESIAN_POINT ( 'NONE',  ( 11.99999999999999822, 59.03342792756263435, 46.54456581323825048 ) ) ;
#59129=DIRECTION ( 'NONE',  ( 0.000000000000000000, 0.000000000000000000, 1.000000000000000000 ) ) ;
#59132=CIRCLE ( 'NONE', #50733, 31.99999999999999289 ) ;
#59137=LINE ( 'NONE', #36195, #36994 ) ;
#59146=DIRECTION ( 'NONE',  ( 0.000000000000000000, 0.000000000000000000, 1.000000000000000000 ) ) ;
#59150=CARTESIAN_POINT ( 'NONE',  ( 15.00000000000000000, -18.13022148937263012, -15.02647892043543898 ) ) ;
#59154=CYLINDRICAL_SURFACE ( 'NONE', #1480, 31.99999999999998579 ) ;
#59155=ORIENTED_EDGE ( 'NONE', *, *, #879, .T. ) ;
#59161=CARTESIAN_POINT ( 'NONE',  ( 11.99999999999999822, 65.58780272294076497, 36.73666225445916211 ) ) ;
#59170=DIRECTION ( 'NONE',  ( -1.000000000000000000, -0.000000000000000000, -0.000000000000000000 ) ) ;
#59172=CIRCLE ( 'NONE', #50732, 31.99999999999998579 ) ;
#59176=ORIENTED_EDGE ( 'NONE', *, *, #8257, .F. ) ;
#59189=DIRECTION ( 'NONE',  ( -1.000000000000000000, -0.000000000000000000, -0.000000000000000000 ) ) ;
#59192=DIRECTION ( 'NONE',  ( 0.000000000000000000, 0.000000000000000000, 1.000000000000000000 ) ) ;
#59193=CARTESIAN_POINT ( 'NONE',  ( 0.000000000000000000, -30.41916302227061664, -71.27951684758058093 ) ) ;
#59196=CARTESIAN_POINT ( 'NONE',  ( 11.99999999999999822, 64.81221759200417409, -50.23322058963275794 ) ) ;
#59199=CARTESIAN_POINT ( 'NONE',  ( 5.999999999999999112, -59.75363087400035056, -56.15606465355020305 ) ) ;
#59204=CARTESIAN_POINT ( 'NONE',  ( 15.00000000000000000, 24.81905959214260804, -9.408202855044828894 ) ) ;
#59230=LINE ( 'NONE', #70122, #3416 ) ;
#59231=LINE ( 'NONE', #47947, #6835 ) ;
#59235=CARTESIAN_POINT ( 'NONE',  ( 11.99999999999999822, 31.46837873494978055, 68.27212725128286763 ) ) ;
#59252=EDGE_CURVE ( 'NONE', #26000, #24844, #70200, .T. ) ;
#59254=CARTESIAN_POINT ( 'NONE',  ( 0.000000000000000000, 63.18004540533092239, -44.88180994100307686 ) ) ;
#59263=ADVANCED_FACE ( 'NONE', ( #24159 ), #57634, .T. ) ;
#59266=CARTESIAN_POINT ( 'NONE',  ( 12.00000000000000000, -23.29833615347104470, 3.418703333116808629 ) ) ;
#59273=ORIENTED_EDGE ( 'NONE', *, *, #2535, .F. ) ;
#59275=AXIS2_PLACEMENT_3D ( 'NONE', #43532, #49142, #9285 ) ;
#59281=CARTESIAN_POINT ( 'NONE',  ( -10.00000000000000000, 0.000000000000000000, 0.000000000000000000 ) ) ;
#59287=PLANE ( 'NONE',  #45838 ) ;
#59294=DIRECTION ( 'NONE',  ( -1.000000000000000000, 0.000000000000000000, 0.000000000000000000 ) ) ;
#59296=ORIENTED_EDGE ( 'NONE', *, *, #59683, .F. ) ;
#59311=EDGE_LOOP ( 'NONE', ( #12669, #59466, #4929, #37476 ) ) ;
#59315=DIRECTION ( 'NONE',  ( -1.000000000000000000, -0.000000000000000000, -0.000000000000000000 ) ) ;
#59321=DIRECTION ( 'NONE',  ( 0.000000000000000000, -0.1045284632676437703, 0.9945218953682742891 ) ) ;
#59322=CARTESIAN_POINT ( 'NONE',  ( 0.000000000000000000, 72.35160999960817207, 20.41045688087850607 ) ) ;
#59326=CIRCLE ( 'NONE', #8929, 31.99999999999998579 ) ;
#59328=CIRCLE ( 'NONE', #41299, 31.99999999999999289 ) ;
#59330=EDGE_CURVE ( 'NONE', #21721, #15149, #47089, .T. ) ;
#59332=EDGE_LOOP ( 'NONE', ( #25807, #70246, #33450, #44684 ) ) ;
#59335=AXIS2_PLACEMENT_3D ( 'NONE', #1577, #65439, #41747 ) ;
#59337=LINE ( 'NONE', #18361, #56064 ) ;
#59345=AXIS2_PLACEMENT_3D ( 'NONE', #67420, #27562, #21929 ) ;
#59348=VERTEX_POINT ( 'NONE', #888 ) ;
#59355=CARTESIAN_POINT ( 'NONE',  ( 15.00000000000000000, -0.9646360437375368635, -23.52805723605589705 ) ) ;
#59370=ORIENTED_EDGE ( 'NONE', *, *, #30393, .F. ) ;
#59386=ORIENTED_EDGE ( 'NONE', *, *, #29134, .T. ) ;
#59395=CARTESIAN_POINT ( 'NONE',  ( 0.000000000000000000, 55.19960302592066625, 51.03279382321107249 ) ) ;
#59403=DIRECTION ( 'NONE',  ( -0.000000000000000000, 0.2079116908177663092, 0.9781476007338041345 ) ) ;
#59404=CIRCLE ( 'NONE', #12536, 77.49900000000000944 ) ;
#59405=EDGE_CURVE ( 'NONE', #70390, #40964, #36561, .T. ) ;
#59422=DIRECTION ( 'NONE',  ( 1.000000000000000000, 0.000000000000000000, 0.000000000000000000 ) ) ;
#59431=CIRCLE ( 'NONE', #53475, 77.49900000000002365 ) ;
#59435=EDGE_CURVE ( 'NONE', #45705, #40611, #47450, .T. ) ;
#59440=CARTESIAN_POINT ( 'NONE',  ( 6.000000000000000000, -16.65972982744876774, -80.28980883073775487 ) ) ;
#59442=FACE_OUTER_BOUND ( 'NONE', #52694, .T. ) ;
#59443=VERTEX_POINT ( 'NONE', #13232 ) ;
#59451=CARTESIAN_POINT ( 'NONE',  ( 12.00000000000000000, 18.84667830672579569, -18.68964196561269375 ) ) ;
#59454=ORIENTED_EDGE ( 'NONE', *, *, #651, .F. ) ;
#59459=CYLINDRICAL_SURFACE ( 'NONE', #58133, 77.49899999999999523 ) ;
#59466=ORIENTED_EDGE ( 'NONE', *, *, #35721, .T. ) ;
#59467=EDGE_LOOP ( 'NONE', ( #34156, #63067, #8890, #69183 ) ) ;
#59474=ORIENTED_EDGE ( 'NONE', *, *, #71200, .F. ) ;
#59476=DIRECTION ( 'NONE',  ( -1.000000000000000000, -0.000000000000000000, -0.000000000000000000 ) ) ;
#59492=CARTESIAN_POINT ( 'NONE',  ( 0.000000000000000000, 6.903761155837791819, 77.19088730480525840 ) ) ;
#59500=AXIS2_PLACEMENT_3D ( 'NONE', #52099, #46465, #69390 ) ;
#59502=EDGE_CURVE ( 'NONE', #18143, #49623, #6574, .T. ) ;
#59504=DIRECTION ( 'NONE',  ( -1.000000000000000000, -0.000000000000000000, 0.000000000000000000 ) ) ;
#59510=CARTESIAN_POINT ( 'NONE',  ( 12.00000000000000000, -4.261787119644964150, 26.19803753235780164 ) ) ;
#59514=DIRECTION ( 'NONE',  ( 0.000000000000000000, -0.6494480483301904306, 0.7604059656000252687 ) ) ;
#59515=CARTESIAN_POINT ( 'NONE',  ( 6.000000000000000000, -76.69515212745996280, -29.01471420065643869 ) ) ;
#59518=CARTESIAN_POINT ( 'NONE',  ( 0.000000000000000000, -8.966570791701281351, 81.50828551894223040 ) ) ;
#59532=EDGE_CURVE ( 'NONE', #37729, #12399, #15033, .T. ) ;
#59534=DIRECTION ( 'NONE',  ( 0.000000000000000000, 0.000000000000000000, 1.000000000000000000 ) ) ;
#59536=ORIENTED_EDGE ( 'NONE', *, *, #61458, .F. ) ;
#59537=CARTESIAN_POINT ( 'NONE',  ( 12.00000000000000000, -11.95096189432345746, -23.69967320028757030 ) ) ;
#59540=ORIENTED_EDGE ( 'NONE', *, *, #15374, .F. ) ;
#59547=ORIENTED_EDGE ( 'NONE', *, *, #22425, .T. ) ;
#59553=EDGE_LOOP ( 'NONE', ( #1140, #33656, #72238, #13496 ) ) ;
#59562=VERTEX_POINT ( 'NONE', #4192 ) ;
#59569=DIRECTION ( 'NONE',  ( 0.000000000000000000, -0.1564344650402381687, 0.9876883405951365491 ) ) ;
#59570=CARTESIAN_POINT ( 'NONE',  ( 11.99999999999999822, 81.96053171279901051, -2.543863470248673764 ) ) ;
#59575=ORIENTED_EDGE ( 'NONE', *, *, #5179, .F. ) ;
#59577=PLANE ( 'NONE',  #55339 ) ;
#59587=ORIENTED_EDGE ( 'NONE', *, *, #65721, .T. ) ;
#59592=CARTESIAN_POINT ( 'NONE',  ( 0.000000000000000000, -74.65491531819111515, 23.16904090965678265 ) ) ;
#59597=EDGE_CURVE ( 'NONE', #37548, #57064, #4226, .T. ) ;
#59599=ORIENTED_EDGE ( 'NONE', *, *, #21457, .T. ) ;
#59608=AXIS2_PLACEMENT_3D ( 'NONE', #14649, #60535, #62015 ) ;
#59619=FACE_OUTER_BOUND ( 'NONE', #60209, .T. ) ;
#59628=ORIENTED_EDGE ( 'NONE', *, *, #14075, .T. ) ;
#59632=FACE_OUTER_BOUND ( 'NONE', #30594, .T. ) ;
#59635=CARTESIAN_POINT ( 'NONE',  ( 11.99999999999999822, -44.88180994100419952, 63.18004540533013369 ) ) ;
#59641=EDGE_CURVE ( 'NONE', #44992, #68450, #51055, .T. ) ;
#59644=EDGE_LOOP ( 'NONE', ( #20055, #72183, #29792, #6659 ) ) ;
#59653=DIRECTION ( 'NONE',  ( -1.000000000000000000, -0.000000000000000000, -0.000000000000000000 ) ) ;
#59655=ADVANCED_FACE ( 'NONE', ( #61329 ), #9810, .T. ) ;
#59656=ORIENTED_EDGE ( 'NONE', *, *, #69316, .T. ) ;
#59657=DIRECTION ( 'NONE',  ( -1.000000000000000000, -0.000000000000000000, -0.000000000000000000 ) ) ;
#59661=EDGE_CURVE ( 'NONE', #3905, #3810, #40216, .T. ) ;
#59666=ADVANCED_FACE ( 'NONE', ( #16944 ), #431, .T. ) ;
#59668=CARTESIAN_POINT ( 'NONE',  ( 11.99999999999999822, -65.59268652807237743, 36.72794159290217664 ) ) ;
#59670=ORIENTED_EDGE ( 'NONE', *, *, #71088, .T. ) ;
#59677=CARTESIAN_POINT ( 'NONE',  ( 11.99999999999999822, 0.000000000000000000, 0.000000000000000000 ) ) ;
#59679=DIRECTION ( 'NONE',  ( 1.000000000000000000, 0.000000000000000000, 0.000000000000000000 ) ) ;
#59682=EDGE_LOOP ( 'NONE', ( #36439, #30467, #14683, #4360 ) ) ;
#59683=EDGE_CURVE ( 'NONE', #62137, #16267, #71425, .T. ) ;
#59689=CARTESIAN_POINT ( 'NONE',  ( 0.000000000000000000, 0.000000000000000000, 0.000000000000000000 ) ) ;
#59694=CARTESIAN_POINT ( 'NONE',  ( 0.000000000000000000, 70.52718814184260054, 26.02418014898334420 ) ) ;
#59698=DIRECTION ( 'NONE',  ( -1.000000000000000000, 0.000000000000000000, 0.000000000000000000 ) ) ;
#59700=ADVANCED_FACE ( 'NONE', ( #17677 ), #57910, .T. ) ;
#59714=LINE ( 'NONE', #7465, #7850 ) ;
#59718=VECTOR ( 'NONE', #61210, 1000.000000000000114 ) ;
#59720=ORIENTED_EDGE ( 'NONE', *, *, #46373, .T. ) ;
#59721=VECTOR ( 'NONE', #45231, 1000.000000000000114 ) ;
#59725=DIRECTION ( 'NONE',  ( -1.000000000000000000, 0.000000000000000000, 0.000000000000000000 ) ) ;
#59731=LINE ( 'NONE', #8214, #16736 ) ;
#59735=DIRECTION ( 'NONE',  ( -1.000000000000000000, -0.000000000000000000, -0.000000000000000000 ) ) ;
#59736=EDGE_CURVE ( 'NONE', #71078, #12401, #59431, .T. ) ;
#59737=VERTEX_POINT ( 'NONE', #58271 ) ;
#59742=ORIENTED_EDGE ( 'NONE', *, *, #43555, .T. ) ;
#59745=ORIENTED_EDGE ( 'NONE', *, *, #40263, .F. ) ;
#59753=EDGE_CURVE ( 'NONE', #20786, #37729, #18051, .T. ) ;
#59757=ORIENTED_EDGE ( 'NONE', *, *, #10687, .F. ) ;
#59759=VERTEX_POINT ( 'NONE', #11293 ) ;
#59772=DIRECTION ( 'NONE',  ( 1.000000000000000000, 0.000000000000000000, 0.000000000000000000 ) ) ;
#59803=ORIENTED_EDGE ( 'NONE', *, *, #34162, .T. ) ;
#59808=AXIS2_PLACEMENT_3D ( 'NONE', #17889, #1755, #40840 ) ;
#59833=ORIENTED_EDGE ( 'NONE', *, *, #60170, .F. ) ;
#59842=EDGE_CURVE ( 'NONE', #53064, #5982, #60779, .T. ) ;
#59844=ORIENTED_EDGE ( 'NONE', *, *, #58237, .T. ) ;
#59847=DIRECTION ( 'NONE',  ( -1.000000000000000000, 0.000000000000000000, 0.000000000000000000 ) ) ;
#59851=CYLINDRICAL_SURFACE ( 'NONE', #71402, 31.99999999999998579 ) ;
#59853=CARTESIAN_POINT ( 'NONE',  ( -10.00000000000000000, 0.000000000000000000, 0.000000000000000000 ) ) ;
#59865=EDGE_CURVE ( 'NONE', #51720, #45705, #13136, .T. ) ;
#59867=FACE_OUTER_BOUND ( 'NONE', #61431, .T. ) ;
#59871=CARTESIAN_POINT ( 'NONE',  ( 11.99999999999999822, -5.256550761633395297, 77.32052557432841411 ) ) ;
#59879=AXIS2_PLACEMENT_3D ( 'NONE', #65082, #23731, #1589 ) ;
#59881=EDGE_CURVE ( 'NONE', #59737, #43856, #72038, .T. ) ;
#59889=VECTOR ( 'NONE', #18915, 1000.000000000000000 ) ;
#59894=CARTESIAN_POINT ( 'NONE',  ( 0.000000000000000000, 0.000000000000000000, 0.000000000000000000 ) ) ;
#59901=CIRCLE ( 'NONE', #45521, 82.00000000000000000 ) ;
#59910=DIRECTION ( 'NONE',  ( 0.000000000000000000, -6.982962677686266711E-15, 1.000000000000000000 ) ) ;
#59912=ORIENTED_EDGE ( 'NONE', *, *, #63001, .F. ) ;
#59922=CARTESIAN_POINT ( 'NONE',  ( 11.99999999999999822, 17.28742895386189460, -75.54627589209927407 ) ) ;
#59924=EDGE_CURVE ( 'NONE', #18572, #26714, #18773, .T. ) ;
#59927=CIRCLE ( 'NONE', #27493, 31.99999999999998579 ) ;
#59930=CYLINDRICAL_SURFACE ( 'NONE', #58723, 77.49899999999999523 ) ;
#59932=ORIENTED_EDGE ( 'NONE', *, *, #59106, .T. ) ;
#59939=CIRCLE ( 'NONE', #68312, 77.49899999999999523 ) ;
#59941=ORIENTED_EDGE ( 'NONE', *, *, #16144, .F. ) ;
#59960=VECTOR ( 'NONE', #68324, 1000.000000000000000 ) ;
#59965=CARTESIAN_POINT ( 'NONE',  ( 0.000000000000000000, 0.8261519478431255115, 77.49459641780886443 ) ) ;
#59974=ORIENTED_EDGE ( 'NONE', *, *, #73602, .F. ) ;
#59975=CARTESIAN_POINT ( 'NONE',  ( 11.99999999999999822, -65.58780272294048075, -36.73666225445966660 ) ) ;
#59977=DIRECTION ( 'NONE',  ( 0.000000000000000000, 0.8910065241883656784, 0.4539904997395511344 ) ) ;
#59985=AXIS2_PLACEMENT_3D ( 'NONE', #15658, #21269, #22793 ) ;
#59988=CARTESIAN_POINT ( 'NONE',  ( 0.000000000000000000, 44.88180994100466847, -63.18004540532978552 ) ) ;
#59991=CARTESIAN_POINT ( 'NONE',  ( 11.99999999999999822, -39.78640506895559525, -66.50666863322042843 ) ) ;
#59993=CARTESIAN_POINT ( 'NONE',  ( 11.99999999999999822, 68.67312586194995561, 35.91791733033500122 ) ) ;
#60003=CIRCLE ( 'NONE', #21603, 31.99999999999999289 ) ;
#60007=ORIENTED_EDGE ( 'NONE', *, *, #52791, .T. ) ;
#60009=VERTEX_POINT ( 'NONE', #10375 ) ;
#60012=EDGE_CURVE ( 'NONE', #11199, #25600, #44226, .T. ) ;
#60014=ADVANCED_FACE ( 'NONE', ( #21265 ), #10751, .T. ) ;
#60015=ORIENTED_EDGE ( 'NONE', *, *, #55327, .T. ) ;
#60021=CYLINDRICAL_SURFACE ( 'NONE', #42468, 82.00000000000000000 ) ;
#60028=ORIENTED_EDGE ( 'NONE', *, *, #24015, .F. ) ;
#60041=EDGE_CURVE ( 'NONE', #42829, #31594, #40274, .T. ) ;
#60055=CARTESIAN_POINT ( 'NONE',  ( 15.00000000000000000, -13.04903810567675393, -19.60159698893424718 ) ) ;
#60057=ORIENTED_EDGE ( 'NONE', *, *, #41830, .F. ) ;
#60064=CARTESIAN_POINT ( 'NONE',  ( 0.000000000000000000, -56.15606465354916566, -59.75363087400133111 ) ) ;
#60069=VECTOR ( 'NONE', #3151, 1000.000000000000000 ) ;
#60081=CARTESIAN_POINT ( 'NONE',  ( 11.99999999999999822, -36.72794159290288718, 65.59268652807197952 ) ) ;
#60092=CARTESIAN_POINT ( 'NONE',  ( 0.000000000000000000, 8.830959090342393125, 74.65491531819122883 ) ) ;
#60095=EDGE_CURVE ( 'NONE', #26057, #60769, #30700, .T. ) ;
#60108=ORIENTED_EDGE ( 'NONE', *, *, #36307, .F. ) ;
#60122=CARTESIAN_POINT ( 'NONE',  ( 0.000000000000000000, 41.76937507738875155, -62.50329211542393892 ) ) ;
#60123=ORIENTED_EDGE ( 'NONE', *, *, #1512, .T. ) ;
#60144=ORIENTED_EDGE ( 'NONE', *, *, #70410, .F. ) ;
#60145=VERTEX_POINT ( 'NONE', #622 ) ;
#60149=ORIENTED_EDGE ( 'NONE', *, *, #65855, .T. ) ;
#60150=CARTESIAN_POINT ( 'NONE',  ( 0.000000000000000000, -30.41916302227164337, 71.27951684758015460 ) ) ;
#60155=ORIENTED_EDGE ( 'NONE', *, *, #24333, .F. ) ;
#60165=DIRECTION ( 'NONE',  ( 0.000000000000000000, 0.3826834323650904479, -0.9238795325112865164 ) ) ;
#60170=EDGE_CURVE ( 'NONE', #1606, #28741, #41499, .T. ) ;
#60175=UNCERTAINTY_MEASURE_WITH_UNIT (LENGTH_MEASURE( 1.000000000000000082E-05 ), #57499, 'distance_accuracy_value', 'NONE');
#60182=DIRECTION ( 'NONE',  ( -1.000000000000000000, 0.000000000000000000, 0.000000000000000000 ) ) ;
#60184=ADVANCED_FACE ( 'NONE', ( #29879 ), #24618, .T. ) ;
#60187=ORIENTED_EDGE ( 'NONE', *, *, #45607, .F. ) ;
#60195=DIRECTION ( 'NONE',  ( 0.000000000000000000, 0.000000000000000000, -1.000000000000000000 ) ) ;
#60196=VERTEX_POINT ( 'NONE', #70459 ) ;
#60203=CARTESIAN_POINT ( 'NONE',  ( 0.000000000000000000, 0.000000000000000000, 0.000000000000000000 ) ) ;
#60204=ORIENTED_EDGE ( 'NONE', *, *, #49496, .T. ) ;
#60209=EDGE_LOOP ( 'NONE', ( #71595, #66845, #22513, #22853 ) ) ;
#60211=AXIS2_PLACEMENT_3D ( 'NONE', #69404, #10792, #11883 ) ;
#60217=DIRECTION ( 'NONE',  ( -1.000000000000000000, 0.000000000000000000, 0.000000000000000000 ) ) ;
#60222=ADVANCED_FACE ( 'NONE', ( #35162 ), #58100, .T. ) ;
#60224=ORIENTED_EDGE ( 'NONE', *, *, #67240, .F. ) ;
#60231=DIRECTION ( 'NONE',  ( 0.000000000000000000, 0.7071067811865439090, 0.7071067811865512365 ) ) ;
#60234=CARTESIAN_POINT ( 'NONE',  ( 5.999999999999999112, 40.65526001592713357, -71.21200624218752750 ) ) ;
#60240=VERTEX_POINT ( 'NONE', #23890 ) ;
#60243=CARTESIAN_POINT ( 'NONE',  ( 11.99999999999999822, 0.000000000000000000, 0.000000000000000000 ) ) ;
#60256=DIRECTION ( 'NONE',  ( 0.000000000000000000, 0.000000000000000000, -1.000000000000000000 ) ) ;
#60262=DIRECTION ( 'NONE',  ( 1.000000000000000000, 0.000000000000000000, 0.000000000000000000 ) ) ;
#60263=EDGE_CURVE ( 'NONE', #42705, #7392, #706, .T. ) ;
#60276=CARTESIAN_POINT ( 'NONE',  ( 12.00000000000000000, -3.948201729842032215, 23.21447184625297666 ) ) ;
#60284=DIRECTION ( 'NONE',  ( -1.000000000000000000, -0.000000000000000000, -0.000000000000000000 ) ) ;
#60286=LINE ( 'NONE', #11900, #60069 ) ;
#60288=EDGE_CURVE ( 'NONE', #48071, #32115, #65593, .T. ) ;
#60289=EDGE_LOOP ( 'NONE', ( #46522, #41050, #18612, #3544 ) ) ;
#60297=ORIENTED_EDGE ( 'NONE', *, *, #56268, .F. ) ;
#60298=ORIENTED_EDGE ( 'NONE', *, *, #62579, .F. ) ;
#60300=ORIENTED_EDGE ( 'NONE', *, *, #27220, .F. ) ;
#60303=EDGE_CURVE ( 'NONE', #19443, #6124, #20077, .T. ) ;
#60306=CIRCLE ( 'NONE', #68683, 82.00000000000000000 ) ;
#60318=CARTESIAN_POINT ( 'NONE',  ( 12.00000000000000000, 16.83928648764922542, -16.46020748918050458 ) ) ;
#60326=ORIENTED_EDGE ( 'NONE', *, *, #59435, .F. ) ;
#60340=DIRECTION ( 'NONE',  ( -0.000000000000000000, 0.9510565162951539753, 0.3090169943749461745 ) ) ;
#60343=DIRECTION ( 'NONE',  ( 0.000000000000000000, 0.000000000000000000, 1.000000000000000000 ) ) ;
#60347=DIRECTION ( 'NONE',  ( 0.000000000000000000, 0.7604059656000277112, 0.6494480483301875440 ) ) ;
#60371=VECTOR ( 'NONE', #15854, 1000.000000000000000 ) ;
#60384=CYLINDRICAL_SURFACE ( 'NONE', #39282, 82.00000000000000000 ) ;
#60390=DIRECTION ( 'NONE',  ( 0.000000000000000000, 0.000000000000000000, 1.000000000000000000 ) ) ;
#60392=ORIENTED_EDGE ( 'NONE', *, *, #38173, .F. ) ;
#60395=ORIENTED_EDGE ( 'NONE', *, *, #74204, .T. ) ;
#60401=CARTESIAN_POINT ( 'NONE',  ( 11.99999999999999822, 0.000000000000000000, 0.000000000000000000 ) ) ;
#60409=EDGE_LOOP ( 'NONE', ( #35525, #7048, #40111, #19802 ) ) ;
#60412=ORIENTED_EDGE ( 'NONE', *, *, #20965, .F. ) ;
#60418=CARTESIAN_POINT ( 'NONE',  ( 12.00000000000000000, 22.07842321921480888, -8.187992925817425771 ) ) ;
#60421=AXIS2_PLACEMENT_3D ( 'NONE', #70570, #42035, #34913 ) ;
#60422=VECTOR ( 'NONE', #15767, 1000.000000000000114 ) ;
#60424=ORIENTED_EDGE ( 'NONE', *, *, #31246, .F. ) ;
#60427=FACE_OUTER_BOUND ( 'NONE', #15191, .T. ) ;
#60438=DIRECTION ( 'NONE',  ( 0.000000000000000000, -0.9969173337331270757, -0.07845909572785580988 ) ) ;
#60441=CARTESIAN_POINT ( 'NONE',  ( 15.00000000000000000, -25.60904388321925040, -6.976881207771165272 ) ) ;
#60442=DIRECTION ( 'NONE',  ( -1.000000000000000000, 0.000000000000000000, -0.000000000000000000 ) ) ;
#60444=EDGE_CURVE ( 'NONE', #6493, #15073, #42739, .T. ) ;
#60457=FACE_OUTER_BOUND ( 'NONE', #33968, .T. ) ;
#60459=CIRCLE ( 'NONE', #31610, 82.00000000000000000 ) ;
#60460=CARTESIAN_POINT ( 'NONE',  ( 0.000000000000000000, 0.000000000000000000, 0.000000000000000000 ) ) ;
#60475=DIRECTION ( 'NONE',  ( 1.000000000000000000, -0.000000000000000000, -0.000000000000000000 ) ) ;
#60479=AXIS2_PLACEMENT_3D ( 'NONE', #58933, #30339, #11939 ) ;
#60480=VERTEX_POINT ( 'NONE', #33961 ) ;
#60491=DIRECTION ( 'NONE',  ( 0.000000000000000000, 0.000000000000000000, -1.000000000000000000 ) ) ;
#60495=ORIENTED_EDGE ( 'NONE', *, *, #16445, .F. ) ;
#60501=CARTESIAN_POINT ( 'NONE',  ( 0.000000000000000000, 21.60688246758586928, 79.10210256391376049 ) ) ;
#60503=DIRECTION ( 'NONE',  ( 0.000000000000000000, 0.9510565162951503115, -0.3090169943749573878 ) ) ;
#60505=AXIS2_PLACEMENT_3D ( 'NONE', #35951, #6295, #58902 ) ;
#60514=DIRECTION ( 'NONE',  ( -1.000000000000000000, -0.000000000000000000, -0.000000000000000000 ) ) ;
#60518=DIRECTION ( 'NONE',  ( 0.000000000000000000, 0.000000000000000000, 1.000000000000000000 ) ) ;
#60519=CYLINDRICAL_SURFACE ( 'NONE', #10418, 31.99999999999998579 ) ;
#60523=DIRECTION ( 'NONE',  ( 0.000000000000000000, 0.000000000000000000, 1.000000000000000000 ) ) ;
#60535=DIRECTION ( 'NONE',  ( -1.000000000000000000, 0.000000000000000000, 0.000000000000000000 ) ) ;
#60541=CARTESIAN_POINT ( 'NONE',  ( 0.000000000000000000, 56.15606465354958488, 59.75363087400094741 ) ) ;
#60542=DIRECTION ( 'NONE',  ( -1.000000000000000000, 0.000000000000000000, -0.000000000000000000 ) ) ;
#60548=VERTEX_POINT ( 'NONE', #58006 ) ;
#60552=LINE ( 'NONE', #65455, #14938 ) ;
#60553=EDGE_CURVE ( 'NONE', #45, #37858, #6726, .T. ) ;
#60555=AXIS2_PLACEMENT_3D ( 'NONE', #67313, #32347, #43657 ) ;
#60558=DIRECTION ( 'NONE',  ( -1.000000000000000000, -0.000000000000000000, 0.000000000000000000 ) ) ;
#60560=ORIENTED_EDGE ( 'NONE', *, *, #49247, .F. ) ;
#60570=ORIENTED_EDGE ( 'NONE', *, *, #46582, .T. ) ;
#60573=VERTEX_POINT ( 'NONE', #176 ) ;
#60579=CARTESIAN_POINT ( 'NONE',  ( 11.99999999999999822, 29.01471420065563933, 76.69515212746024702 ) ) ;
#60580=VECTOR ( 'NONE', #47332, 1000.000000000000000 ) ;
#60581=ORIENTED_EDGE ( 'NONE', *, *, #21923, .T. ) ;
#60585=AXIS2_PLACEMENT_3D ( 'NONE', #2739, #36528, #71101 ) ;
#60589=FACE_OUTER_BOUND ( 'NONE', #55432, .T. ) ;
#60595=EDGE_CURVE ( 'NONE', #26934, #9345, #43980, .T. ) ;
#60604=DIRECTION ( 'NONE',  ( -0.000000000000000000, 0.8090169943749426773, -0.5877852522924796874 ) ) ;
#60605=DIRECTION ( 'NONE',  ( -1.000000000000000000, 0.000000000000000000, 0.000000000000000000 ) ) ;
#60613=ORIENTED_EDGE ( 'NONE', *, *, #49247, .T. ) ;
#60617=CARTESIAN_POINT ( 'NONE',  ( 11.99999999999999822, -77.49459641780886443, -0.8261519478439277586 ) ) ;
#60639=CARTESIAN_POINT ( 'NONE',  ( -10.00000000000000000, 0.000000000000000000, 0.000000000000000000 ) ) ;
#60641=CARTESIAN_POINT ( 'NONE',  ( 15.00000000000000000, -19.89357724625003598, -12.59942793731059041 ) ) ;
#60642=EDGE_LOOP ( 'NONE', ( #4634, #22887, #22008, #18665 ) ) ;
#60643=DIRECTION ( 'NONE',  ( 0.000000000000000000, -0.8090169943749401238, -0.5877852522924831291 ) ) ;
#60644=DIRECTION ( 'NONE',  ( 0.000000000000000000, 0.000000000000000000, -1.000000000000000000 ) ) ;
#60645=DIRECTION ( 'NONE',  ( 0.000000000000000000, 0.000000000000000000, -1.000000000000000000 ) ) ;
#60648=ORIENTED_EDGE ( 'NONE', *, *, #43578, .T. ) ;
#60653=DIRECTION ( 'NONE',  ( 0.000000000000000000, -0.6494480483301904306, 0.7604059656000251577 ) ) ;
#60670=ORIENTED_EDGE ( 'NONE', *, *, #20696, .F. ) ;
#60674=ORIENTED_EDGE ( 'NONE', *, *, #65355, .F. ) ;
#60675=CIRCLE ( 'NONE', #33061, 31.99999999999998224 ) ;
#60685=CARTESIAN_POINT ( 'NONE',  ( 0.000000000000000000, -60.67117009219175827, 55.16347631943019536 ) ) ;
#60696=DIRECTION ( 'NONE',  ( 0.000000000000000000, -0.5224985647159559043, 0.8526401643540879594 ) ) ;
#60710=CARTESIAN_POINT ( 'NONE',  ( 11.99999999999999822, -73.95703589263958122, -23.16143007188505010 ) ) ;
#60715=ORIENTED_EDGE ( 'NONE', *, *, #59753, .F. ) ;
#60720=CARTESIAN_POINT ( 'NONE',  ( 11.99999999999999822, 0.000000000000000000, 0.000000000000000000 ) ) ;
#60724=CARTESIAN_POINT ( 'NONE',  ( 0.000000000000000000, -76.66974797899828786, -11.30684508768420393 ) ) ;
#60725=DIRECTION ( 'NONE',  ( 0.000000000000000000, 0.9969173337331281859, -0.07845909572784182107 ) ) ;
#60726=EDGE_CURVE ( 'NONE', #50776, #42720, #63664, .T. ) ;
#60735=DIRECTION ( 'NONE',  ( 0.000000000000000000, 0.5224985647159441360, 0.8526401643540952868 ) ) ;
#60745=VERTEX_POINT ( 'NONE', #71853 ) ;
#60747=AXIS2_PLACEMENT_3D ( 'NONE', #33159, #39189, #6104 ) ;
#60751=EDGE_CURVE ( 'NONE', #36331, #70989, #7979, .T. ) ;
#60754=CARTESIAN_POINT ( 'NONE',  ( 0.000000000000000000, 78.73519480814985627, -22.90783923731548199 ) ) ;
#60758=ORIENTED_EDGE ( 'NONE', *, *, #70659, .F. ) ;
#60768=DIRECTION ( 'NONE',  ( 1.000000000000000000, 0.000000000000000000, 0.000000000000000000 ) ) ;
#60769=VERTEX_POINT ( 'NONE', #13249 ) ;
#60773=ORIENTED_EDGE ( 'NONE', *, *, #35205, .T. ) ;
#60779=LINE ( 'NONE', #26551, #30647 ) ;
#60780=CARTESIAN_POINT ( 'NONE',  ( 0.000000000000000000, 0.000000000000000000, 0.000000000000000000 ) ) ;
#60782=EDGE_CURVE ( 'NONE', #51687, #3457, #3110, .T. ) ;
#60783=CARTESIAN_POINT ( 'NONE',  ( 50.00005079999999680, 0.000000000000000000, 21.00000000000000000 ) ) ;
#60792=VECTOR ( 'NONE', #20748, 1000.000000000000000 ) ;
#60800=DIRECTION ( 'NONE',  ( -1.000000000000000000, -0.000000000000000000, 0.000000000000000000 ) ) ;
#60803=AXIS2_PLACEMENT_3D ( 'NONE', #25230, #6465, #60195 ) ;
#60817=CARTESIAN_POINT ( 'NONE',  ( 0.000000000000000000, -16.65972982744991171, 80.28980883073752750 ) ) ;
#60818=VECTOR ( 'NONE', #73233, 1000.000000000000000 ) ;
#60821=CARTESIAN_POINT ( 'NONE',  ( 11.99999999999999822, 0.000000000000000000, 0.000000000000000000 ) ) ;
#60822=LINE ( 'NONE', #66828, #16800 ) ;
#60831=DIRECTION ( 'NONE',  ( 0.000000000000000000, 0.000000000000000000, -1.000000000000000000 ) ) ;
#60837=ORIENTED_EDGE ( 'NONE', *, *, #26712, .F. ) ;
#60844=AXIS2_PLACEMENT_3D ( 'NONE', #51117, #74041, #67672 ) ;
#60852=AXIS2_PLACEMENT_3D ( 'NONE', #46317, #68884, #62130 ) ;
#60856=VERTEX_POINT ( 'NONE', #13614 ) ;
#60857=DIRECTION ( 'NONE',  ( -1.000000000000000000, -0.000000000000000000, 0.000000000000000000 ) ) ;
#60871=ORIENTED_EDGE ( 'NONE', *, *, #19373, .T. ) ;
#60873=CARTESIAN_POINT ( 'NONE',  ( 0.000000000000000000, -71.21200624218768382, -40.65526001592688488 ) ) ;
#60890=CARTESIAN_POINT ( 'NONE',  ( 11.99999999999999822, 72.35160999960817207, 20.41045688087850607 ) ) ;
#60893=CARTESIAN_POINT ( 'NONE',  ( 0.000000000000000000, -2.946379043146863719, 75.11764819372146462 ) ) ;
#60895=CARTESIAN_POINT ( 'NONE',  ( 0.000000000000000000, 58.39081064771822582, -50.95692526931267707 ) ) ;
#60896=CIRCLE ( 'NONE', #11661, 31.99999999999998224 ) ;
#60902=DIRECTION ( 'NONE',  ( 0.000000000000000000, 0.000000000000000000, 1.000000000000000000 ) ) ;
#60909=DIRECTION ( 'NONE',  ( 0.000000000000000000, 0.000000000000000000, 1.000000000000000000 ) ) ;
#60912=DIRECTION ( 'NONE',  ( 0.000000000000000000, -0.4539904997395541875, 0.8910065241883641241 ) ) ;
#60914=EDGE_LOOP ( 'NONE', ( #11000, #28769, #41883, #29305 ) ) ;
#60920=CIRCLE ( 'NONE', #41708, 77.49900000000000944 ) ;
#60923=CARTESIAN_POINT ( 'NONE',  ( 11.99999999999999822, 24.73286445877705475, 73.44644590900068692 ) ) ;
#60931=ORIENTED_EDGE ( 'NONE', *, *, #23113, .F. ) ;
#60933=CYLINDRICAL_SURFACE ( 'NONE', #12828, 31.99999999999998579 ) ;
#60934=EDGE_CURVE ( 'NONE', #31764, #27635, #4209, .T. ) ;
#60939=EDGE_CURVE ( 'NONE', #26439, #11277, #10373, .T. ) ;
#60945=ORIENTED_EDGE ( 'NONE', *, *, #66407, .T. ) ;
#60948=ORIENTED_EDGE ( 'NONE', *, *, #4083, .T. ) ;
#60950=CARTESIAN_POINT ( 'NONE',  ( 0.000000000000000000, -46.54456581323847786, 59.03342792756247093 ) ) ;
#60956=ORIENTED_EDGE ( 'NONE', *, *, #11023, .F. ) ;
#60964=DIRECTION ( 'NONE',  ( -1.000000000000000000, -0.000000000000000000, 0.000000000000000000 ) ) ;
#60975=DIRECTION ( 'NONE',  ( -1.000000000000000000, 0.000000000000000000, 0.000000000000000000 ) ) ;
#60984=DIRECTION ( 'NONE',  ( 1.000000000000000000, 0.000000000000000000, 0.000000000000000000 ) ) ;
#60988=DIRECTION ( 'NONE',  ( -1.000000000000000000, 0.000000000000000000, 0.000000000000000000 ) ) ;
#60991=ORIENTED_EDGE ( 'NONE', *, *, #21907, .T. ) ;
#60998=VECTOR ( 'NONE', #5377, 1000.000000000000114 ) ;
#61001=AXIS2_PLACEMENT_3D ( 'NONE', #21118, #4230, #67363 ) ;
#61005=EDGE_LOOP ( 'NONE', ( #15042, #6564, #48250, #57600 ) ) ;
#61013=DIRECTION ( 'NONE',  ( 0.000000000000000000, 0.4539904997395413089, 0.8910065241883705633 ) ) ;
#61015=ADVANCED_FACE ( 'NONE', ( #50414 ), #38404, .T. ) ;
#61016=ORIENTED_EDGE ( 'NONE', *, *, #17229, .T. ) ;
#61033=VERTEX_POINT ( 'NONE', #44795 ) ;
#61041=DIRECTION ( 'NONE',  ( -0.000000000000000000, 1.000000000000000000, 0.000000000000000000 ) ) ;
#61056=CARTESIAN_POINT ( 'NONE',  ( 11.99999999999999822, -80.55351364060578589, -15.33399622253569383 ) ) ;
#61064=ORIENTED_EDGE ( 'NONE', *, *, #44994, .F. ) ;
#61066=VECTOR ( 'NONE', #16599, 1000.000000000000000 ) ;
#61078=DIRECTION ( 'NONE',  ( -1.000000000000000000, 0.000000000000000000, 0.000000000000000000 ) ) ;
#61080=CARTESIAN_POINT ( 'NONE',  ( 11.99999999999999822, 65.64334221924909230, 41.19522573413756561 ) ) ;
#61084=EDGE_CURVE ( 'NONE', #19565, #53812, #18066, .T. ) ;
#61103=CARTESIAN_POINT ( 'NONE',  ( 11.99999999999999822, 0.000000000000000000, 0.000000000000000000 ) ) ;
#61111=LINE ( 'NONE', #42706, #72946 ) ;
#61122=CARTESIAN_POINT ( 'NONE',  ( 0.000000000000000000, 39.78640506895604290, 66.50666863322015843 ) ) ;
#61124=ADVANCED_FACE ( 'NONE', ( #34242 ), #28225, .F. ) ;
#61125=CARTESIAN_POINT ( 'NONE',  ( 11.99999999999999822, -12.93880638057369659, 76.41127070299266677 ) ) ;
#61127=ORIENTED_EDGE ( 'NONE', *, *, #35924, .T. ) ;
#61135=DIRECTION ( 'NONE',  ( 0.000000000000000000, -0.07845909572783056618, -0.9969173337331290741 ) ) ;
#61140=EDGE_CURVE ( 'NONE', #45315, #57888, #13947, .T. ) ;
#61147=EDGE_CURVE ( 'NONE', #73431, #17494, #58657, .T. ) ;
#61152=VECTOR ( 'NONE', #55911, 1000.000000000000000 ) ;
#61159=DIRECTION ( 'NONE',  ( -1.000000000000000000, -0.000000000000000000, 0.000000000000000000 ) ) ;
#61164=DIRECTION ( 'NONE',  ( 0.000000000000000000, -0.6691306063588654540, -0.7431448254773878048 ) ) ;
#61168=ORIENTED_EDGE ( 'NONE', *, *, #63875, .F. ) ;
#61170=ORIENTED_EDGE ( 'NONE', *, *, #13581, .F. ) ;
#61183=LINE ( 'NONE', #67187, #63644 ) ;
#61187=LINE ( 'NONE', #43542, #61152 ) ;
#61190=EDGE_CURVE ( 'NONE', #50412, #38492, #71594, .T. ) ;
#61194=DIRECTION ( 'NONE',  ( -1.000000000000000000, -0.000000000000000000, 0.000000000000000000 ) ) ;
#61195=DIRECTION ( 'NONE',  ( 0.000000000000000000, 0.9969173337331281859, -0.07845909572784182107 ) ) ;
#61207=CYLINDRICAL_SURFACE ( 'NONE', #18458, 31.99999999999998579 ) ;
#61208=CARTESIAN_POINT ( 'NONE',  ( 6.000000000000000000, 10.30890764327501152, -81.34940948281325745 ) ) ;
#61210=DIRECTION ( 'NONE',  ( 0.000000000000000000, -0.8090169943749497827, -0.5877852522924698064 ) ) ;
#61213=AXIS2_PLACEMENT_3D ( 'NONE', #37119, #55138, #26929 ) ;
#61218=CIRCLE ( 'NONE', #27619, 77.49899999999999523 ) ;
#61232=DIRECTION ( 'NONE',  ( -1.000000000000000000, -0.000000000000000000, -0.000000000000000000 ) ) ;
#61234=EDGE_CURVE ( 'NONE', #44223, #9893, #7158, .T. ) ;
#61248=ORIENTED_EDGE ( 'NONE', *, *, #7576, .T. ) ;
#61251=VERTEX_POINT ( 'NONE', #13885 ) ;
#61268=DIRECTION ( 'NONE',  ( -1.000000000000000000, 0.000000000000000000, 0.000000000000000000 ) ) ;
#61274=DIRECTION ( 'NONE',  ( 0.000000000000000000, -0.4067366430758009299, -0.9135454576426005335 ) ) ;
#61275=AXIS2_PLACEMENT_3D ( 'NONE', #43678, #38018, #38762 ) ;
#61281=AXIS2_PLACEMENT_3D ( 'NONE', #43370, #66291, #38447 ) ;
#61283=EDGE_CURVE ( 'NONE', #16098, #28286, #72866, .T. ) ;
#61284=LINE ( 'NONE', #3782, #21492 ) ;
#61288=EDGE_CURVE ( 'NONE', #59443, #38652, #42847, .T. ) ;
#61291=VERTEX_POINT ( 'NONE', #36093 ) ;
#61303=CARTESIAN_POINT ( 'NONE',  ( 0.000000000000000000, 28.89263327155746097, 71.91182617369197771 ) ) ;
#61305=AXIS2_PLACEMENT_3D ( 'NONE', #6619, #53224, #64882 ) ;
#61306=EDGE_CURVE ( 'NONE', #68814, #61974, #36825, .T. ) ;
#61307=ADVANCED_FACE ( 'NONE', ( #13529 ), #71399, .T. ) ;
#61312=CARTESIAN_POINT ( 'NONE',  ( 0.000000000000000000, -8.966570791700167575, -81.50828551894237251 ) ) ;
#61315=DIRECTION ( 'NONE',  ( 0.000000000000000000, -0.8526401643540860720, -0.5224985647159589019 ) ) ;
#61321=CARTESIAN_POINT ( 'NONE',  ( 11.99999999999999822, 26.02418014898310261, 70.52718814184268581 ) ) ;
#61322=ORIENTED_EDGE ( 'NONE', *, *, #55064, .T. ) ;
#61325=ORIENTED_EDGE ( 'NONE', *, *, #48225, .F. ) ;
#61326=CARTESIAN_POINT ( 'NONE',  ( 0.000000000000000000, -51.29473840253269401, 63.97538442413407012 ) ) ;
#61329=FACE_OUTER_BOUND ( 'NONE', #44847, .T. ) ;
#61332=ORIENTED_EDGE ( 'NONE', *, *, #36221, .T. ) ;
#61333=ORIENTED_EDGE ( 'NONE', *, *, #34550, .T. ) ;
#61341=CARTESIAN_POINT ( 'NONE',  ( 12.00000000000000000, -25.60904388321915803, 6.976881207771517879 ) ) ;
#61342=CARTESIAN_POINT ( 'NONE',  ( 12.00000000000000000, -19.89357724624986545, 12.59942793731086219 ) ) ;
#61345=DIRECTION ( 'NONE',  ( -1.000000000000000000, -0.000000000000000000, 0.000000000000000000 ) ) ;
#61361=VECTOR ( 'NONE', #16044, 1000.000000000000000 ) ;
#61370=ADVANCED_FACE ( 'NONE', ( #4876 ), #50703, .F. ) ;
#61374=VERTEX_POINT ( 'NONE', #9000 ) ;
#61375=DIRECTION ( 'NONE',  ( 0.000000000000000000, 0.000000000000000000, 1.000000000000000000 ) ) ;
#61388=DIRECTION ( 'NONE',  ( -1.000000000000000000, 0.000000000000000000, -0.000000000000000000 ) ) ;
#61393=CYLINDRICAL_SURFACE ( 'NONE', #34254, 82.00000000000000000 ) ;
#61394=ORIENTED_EDGE ( 'NONE', *, *, #11228, .T. ) ;
#61395=FACE_OUTER_BOUND ( 'NONE', #58302, .T. ) ;
#61399=VERTEX_POINT ( 'NONE', #21011 ) ;
#61406=LINE ( 'NONE', #11369, #42021 ) ;
#61407=CARTESIAN_POINT ( 'NONE',  ( 12.00000000000000000, 8.688484142253932063, -21.88630264137371029 ) ) ;
#61411=AXIS2_PLACEMENT_3D ( 'NONE', #52357, #68923, #6869 ) ;
#61431=EDGE_LOOP ( 'NONE', ( #6303, #55482, #47929, #9964 ) ) ;
#61432=DIRECTION ( 'NONE',  ( 0.000000000000000000, 0.000000000000000000, 1.000000000000000000 ) ) ;
#61435=LINE ( 'NONE', #73053, #6002 ) ;
#61448=CARTESIAN_POINT ( 'NONE',  ( 11.99999999999999822, 28.89263327155849126, -71.91182617369157981 ) ) ;
#61450=DIRECTION ( 'NONE',  ( 0.000000000000000000, 0.000000000000000000, 1.000000000000000000 ) ) ;
#61451=DIRECTION ( 'NONE',  ( 0.000000000000000000, 0.07845909572784512398, -0.9969173337331279638 ) ) ;
#61454=EDGE_CURVE ( 'NONE', #19565, #9220, #37947, .T. ) ;
#61456=CARTESIAN_POINT ( 'NONE',  ( 6.000000000000000000, -39.47590169984898267, 71.87247863392400404 ) ) ;
#61458=EDGE_CURVE ( 'NONE', #61374, #53067, #22140, .T. ) ;
#61461=CARTESIAN_POINT ( 'NONE',  ( 0.000000000000000000, 0.000000000000000000, 0.000000000000000000 ) ) ;
#61465=ADVANCED_FACE ( 'NONE', ( #16498 ), #60519, .T. ) ;
#61468=DIRECTION ( 'NONE',  ( 0.000000000000000000, 0.000000000000000000, 1.000000000000000000 ) ) ;
#61472=AXIS2_PLACEMENT_3D ( 'NONE', #27387, #15753, #21761 ) ;
#61482=ORIENTED_EDGE ( 'NONE', *, *, #49814, .F. ) ;
#61483=CIRCLE ( 'NONE', #57882, 77.49899999999999523 ) ;
#61484=DIRECTION ( 'NONE',  ( 0.000000000000000000, -0.5000000000000028866, -0.8660254037844369313 ) ) ;
#61491=DIRECTION ( 'NONE',  ( 0.000000000000000000, 0.000000000000000000, 1.000000000000000000 ) ) ;
#61502=CYLINDRICAL_SURFACE ( 'NONE', #20180, 77.49899999999999523 ) ;
#61503=CARTESIAN_POINT ( 'NONE',  ( 0.000000000000000000, 72.35432306680485226, -20.40083707022909110 ) ) ;
#61514=ORIENTED_EDGE ( 'NONE', *, *, #18518, .F. ) ;
#61516=DIRECTION ( 'NONE',  ( -1.000000000000000000, -0.000000000000000000, 0.000000000000000000 ) ) ;
#61518=EDGE_CURVE ( 'NONE', #31113, #47563, #35639, .T. ) ;
#61519=CYLINDRICAL_SURFACE ( 'NONE', #16987, 77.49899999999999523 ) ;
#61520=CARTESIAN_POINT ( 'NONE',  ( 5.999999999999999112, -68.55367621811110723, -44.99326035066126650 ) ) ;
#61524=DIRECTION ( 'NONE',  ( -1.000000000000000000, -0.000000000000000000, -0.000000000000000000 ) ) ;
#61526=CARTESIAN_POINT ( 'NONE',  ( 11.99999999999999822, 0.000000000000000000, 0.000000000000000000 ) ) ;
#61529=ORIENTED_EDGE ( 'NONE', *, *, #60263, .T. ) ;
#61532=AXIS2_PLACEMENT_3D ( 'NONE', #57468, #28891, #45461 ) ;
#61533=CYLINDRICAL_SURFACE ( 'NONE', #22809, 31.99999999999998579 ) ;
#61536=VECTOR ( 'NONE', #28875, 1000.000000000000000 ) ;
#61542=EDGE_CURVE ( 'NONE', #55710, #10397, #15754, .T. ) ;
#61543=CARTESIAN_POINT ( 'NONE',  ( -10.00000000000000000, 0.000000000000000000, 0.000000000000000000 ) ) ;
#61546=CARTESIAN_POINT ( 'NONE',  ( -10.00000000000000000, 0.000000000000000000, 0.000000000000000000 ) ) ;
#61553=CARTESIAN_POINT ( 'NONE',  ( 5.999999999999999112, -46.11716303203136391, -67.80270845531939017 ) ) ;
#61557=DIRECTION ( 'NONE',  ( 0.000000000000000000, 0.1564344650402242909, 0.9876883405951387696 ) ) ;
#61559=ORIENTED_EDGE ( 'NONE', *, *, #33346, .T. ) ;
#61564=EDGE_CURVE ( 'NONE', #9521, #38802, #14006, .T. ) ;
#61565=ORIENTED_EDGE ( 'NONE', *, *, #36227, .F. ) ;
#61567=EDGE_CURVE ( 'NONE', #50834, #1543, #45278, .T. ) ;
#61579=DIRECTION ( 'NONE',  ( -1.000000000000000000, 0.000000000000000000, -0.000000000000000000 ) ) ;
#61580=LINE ( 'NONE', #23217, #45359 ) ;
#61582=VERTEX_POINT ( 'NONE', #29605 ) ;
#61589=CARTESIAN_POINT ( 'NONE',  ( 0.000000000000000000, -73.95703589263990807, 23.16143007188399139 ) ) ;
#61594=ORIENTED_EDGE ( 'NONE', *, *, #68679, .F. ) ;
#61603=CARTESIAN_POINT ( 'NONE',  ( 0.000000000000000000, 10.30890764327501152, -81.34940948281325745 ) ) ;
#61607=ORIENTED_EDGE ( 'NONE', *, *, #38215, .F. ) ;
#61608=LINE ( 'NONE', #15741, #2102 ) ;
#61610=VERTEX_POINT ( 'NONE', #731 ) ;
#61614=EDGE_CURVE ( 'NONE', #16267, #39310, #57286, .T. ) ;
#61616=CARTESIAN_POINT ( 'NONE',  ( 11.99999999999999822, -77.49459641780886443, 0.8261519478428549501 ) ) ;
#61623=CARTESIAN_POINT ( 'NONE',  ( 11.99999999999999822, 73.73191006444572793, -14.66109333815486515 ) ) ;
#61629=CARTESIAN_POINT ( 'NONE',  ( 15.00000000000000000, 9.615535125379096826, 24.73947219025905042 ) ) ;
#61633=CARTESIAN_POINT ( 'NONE',  ( 11.99999999999999822, 75.54627589209944460, 17.28742895386110945 ) ) ;
#61636=CARTESIAN_POINT ( 'NONE',  ( 0.000000000000000000, 46.53671651293948486, 59.03961581697416250 ) ) ;
#61638=AXIS2_PLACEMENT_3D ( 'NONE', #19953, #14322, #53804 ) ;
#61643=CIRCLE ( 'NONE', #67653, 77.49899999999999523 ) ;
#61652=DIRECTION ( 'NONE',  ( 0.000000000000000000, 0.000000000000000000, 1.000000000000000000 ) ) ;
#61665=ORIENTED_EDGE ( 'NONE', *, *, #11687, .F. ) ;
#61687=EDGE_CURVE ( 'NONE', #50461, #42081, #62764, .T. ) ;
#61698=VERTEX_POINT ( 'NONE', #28504 ) ;
#61699=CARTESIAN_POINT ( 'NONE',  ( 11.99999999999999822, -81.96053171279901051, -2.543863470249249747 ) ) ;
#61700=ADVANCED_FACE ( 'NONE', ( #5985 ), #28890, .T. ) ;
#61710=DIRECTION ( 'NONE',  ( 0.000000000000000000, 0.000000000000000000, 1.000000000000000000 ) ) ;
#61730=EDGE_CURVE ( 'NONE', #68378, #45315, #41283, .T. ) ;
#61732=CARTESIAN_POINT ( 'NONE',  ( 0.000000000000000000, -24.73286445877654671, -73.44644590900084324 ) ) ;
#61739=DIRECTION ( 'NONE',  ( -1.000000000000000000, -0.000000000000000000, 0.000000000000000000 ) ) ;
#61754=ORIENTED_EDGE ( 'NONE', *, *, #56827, .T. ) ;
#61756=DIRECTION ( 'NONE',  ( -1.000000000000000000, -0.000000000000000000, -0.000000000000000000 ) ) ;
#61762=VERTEX_POINT ( 'NONE', #52930 ) ;
#61772=CARTESIAN_POINT ( 'NONE',  ( 11.99999999999999822, -36.73666225445940370, 65.58780272294062286 ) ) ;
#61775=ORIENTED_EDGE ( 'NONE', *, *, #14783, .F. ) ;
#61777=CARTESIAN_POINT ( 'NONE',  ( 15.00000000000000000, 14.60985201121729737, 18.46759930825687235 ) ) ;
#61780=ORIENTED_EDGE ( 'NONE', *, *, #45023, .F. ) ;
#61784=ORIENTED_EDGE ( 'NONE', *, *, #16579, .T. ) ;
#61794=EDGE_CURVE ( 'NONE', #56516, #12353, #30913, .T. ) ;
#61805=CARTESIAN_POINT ( 'NONE',  ( 11.99999999999999822, 0.000000000000000000, 0.000000000000000000 ) ) ;
#61814=ORIENTED_EDGE ( 'NONE', *, *, #24892, .F. ) ;
#61817=CYLINDRICAL_SURFACE ( 'NONE', #73927, 77.49899999999999523 ) ;
#61821=DIRECTION ( 'NONE',  ( -1.000000000000000000, -0.000000000000000000, 0.000000000000000000 ) ) ;
#61822=CARTESIAN_POINT ( 'NONE',  ( 11.99999999999999822, 0.000000000000000000, 0.000000000000000000 ) ) ;
#61828=EDGE_CURVE ( 'NONE', #62864, #26970, #14548, .T. ) ;
#61832=DIRECTION ( 'NONE',  ( -1.000000000000000000, -0.000000000000000000, 0.000000000000000000 ) ) ;
#61834=CARTESIAN_POINT ( 'NONE',  ( 11.99999999999999822, -28.89263327155693517, -71.91182617369219088 ) ) ;
#61849=AXIS2_PLACEMENT_3D ( 'NONE', #11260, #15669, #73534 ) ;
#61850=FACE_OUTER_BOUND ( 'NONE', #38758, .T. ) ;
#61853=FACE_OUTER_BOUND ( 'NONE', #21521, .T. ) ;
#61857=AXIS2_PLACEMENT_3D ( 'NONE', #72873, #51447, #73630 ) ;
#61887=ORIENTED_EDGE ( 'NONE', *, *, #72896, .F. ) ;
#61897=DIRECTION ( 'NONE',  ( 0.000000000000000000, 0.000000000000000000, 1.000000000000000000 ) ) ;
#61903=ADVANCED_FACE ( 'NONE', ( #72061 ), #26568, .T. ) ;
#61907=CARTESIAN_POINT ( 'NONE',  ( 15.00000000000000000, 8.688484142253932063, -21.88630264137371029 ) ) ;
#61912=AXIS2_PLACEMENT_3D ( 'NONE', #4385, #5502, #17133 ) ;
#61924=CARTESIAN_POINT ( 'NONE',  ( 11.99999999999999822, -46.54456581323847786, 59.03342792756247093 ) ) ;
#61934=AXIS2_PLACEMENT_3D ( 'NONE', #58418, #42252, #47510 ) ;
#61939=CARTESIAN_POINT ( 'NONE',  ( 11.99999999999999822, -55.20638768913797634, 51.02545421589302777 ) ) ;
#61944=VERTEX_POINT ( 'NONE', #35811 ) ;
#61956=DIRECTION ( 'NONE',  ( 0.000000000000000000, -0.9723699203976741146, -0.2334453638559160493 ) ) ;
#61958=CIRCLE ( 'NONE', #22185, 82.00000000000000000 ) ;
#61974=VERTEX_POINT ( 'NONE', #44762 ) ;
#61975=CARTESIAN_POINT ( 'NONE',  ( 0.000000000000000000, -10.30890764327441289, 81.34940948281332851 ) ) ;
#61982=DIRECTION ( 'NONE',  ( -1.000000000000000000, 0.000000000000000000, -0.000000000000000000 ) ) ;
#61985=VERTEX_POINT ( 'NONE', #72919 ) ;
#61986=DIRECTION ( 'NONE',  ( 0.000000000000000000, 0.000000000000000000, 1.000000000000000000 ) ) ;
#61991=CARTESIAN_POINT ( 'NONE',  ( 11.99999999999999822, -80.28980883073769803, 16.65972982744905551 ) ) ;
#61994=ADVANCED_FACE ( 'NONE', ( #4922 ), #4174, .F. ) ;
#61997=ORIENTED_EDGE ( 'NONE', *, *, #28923, .F. ) ;
#62004=CARTESIAN_POINT ( 'NONE',  ( 15.00000000000000000, 6.762365576493647445, 25.66652317338391498 ) ) ;
#62011=DIRECTION ( 'NONE',  ( 0.000000000000000000, 0.5877852522924743583, -0.8090169943749466741 ) ) ;
#62015=DIRECTION ( 'NONE',  ( 0.000000000000000000, -0.3826834323650970537, 0.9238795325112838519 ) ) ;
#62020=PLANE ( 'NONE',  #41303 ) ;
#62024=CIRCLE ( 'NONE', #71606, 82.00000000000000000 ) ;
#62029=ORIENTED_EDGE ( 'NONE', *, *, #59020, .T. ) ;
#62038=EDGE_CURVE ( 'NONE', #25707, #63817, #52984, .T. ) ;
#62040=ORIENTED_EDGE ( 'NONE', *, *, #46683, .F. ) ;
#62041=CARTESIAN_POINT ( 'NONE',  ( 11.99999999999999822, 11.30684508768339569, 76.66974797899841576 ) ) ;
#62057=EDGE_LOOP ( 'NONE', ( #12016, #37840, #12467, #11966 ) ) ;
#62060=AXIS2_PLACEMENT_3D ( 'NONE', #10860, #46925, #33788 ) ;
#62069=VECTOR ( 'NONE', #13975, 1000.000000000000000 ) ;
#62071=VECTOR ( 'NONE', #6976, 1000.000000000000000 ) ;
#62075=EDGE_CURVE ( 'NONE', #13574, #67492, #71741, .T. ) ;
#62077=VECTOR ( 'NONE', #58209, 1000.000000000000000 ) ;
#62080=DIRECTION ( 'NONE',  ( 0.000000000000000000, 0.000000000000000000, 1.000000000000000000 ) ) ;
#62082=ORIENTED_EDGE ( 'NONE', *, *, #41022, .F. ) ;
#62090=DIRECTION ( 'NONE',  ( -1.000000000000000000, 0.000000000000000000, 0.000000000000000000 ) ) ;
#62092=VERTEX_POINT ( 'NONE', #58613 ) ;
#62098=DIRECTION ( 'NONE',  ( 0.000000000000000000, -0.07845909572783058006, -0.9969173337331290741 ) ) ;
#62100=CARTESIAN_POINT ( 'NONE',  ( 11.99999999999999822, 0.000000000000000000, 0.000000000000000000 ) ) ;
#62105=DIRECTION ( 'NONE',  ( -1.000000000000000000, -0.000000000000000000, -0.000000000000000000 ) ) ;
#62107=CARTESIAN_POINT ( 'NONE',  ( 5.999999999999999112, 46.11716303203283474, -67.80270845531839541 ) ) ;
#62108=EDGE_CURVE ( 'NONE', #73384, #39400, #69399, .T. ) ;
#62112=LINE ( 'NONE', #68870, #8220 ) ;
#62117=CYLINDRICAL_SURFACE ( 'NONE', #65456, 31.99999999999998579 ) ;
#62119=CIRCLE ( 'NONE', #9299, 82.00000000000000000 ) ;
#62120=CIRCLE ( 'NONE', #42910, 77.49900000000002365 ) ;
#62130=DIRECTION ( 'NONE',  ( 0.000000000000000000, -0.9238795325112821866, -0.3826834323651006065 ) ) ;
#62137=VERTEX_POINT ( 'NONE', #415 ) ;
#62138=ORIENTED_EDGE ( 'NONE', *, *, #47603, .T. ) ;
#62139=DIRECTION ( 'NONE',  ( -1.000000000000000000, 0.000000000000000000, 0.000000000000000000 ) ) ;
#62144=CARTESIAN_POINT ( 'NONE',  ( 0.000000000000000000, 0.000000000000000000, 0.000000000000000000 ) ) ;
#62148=ORIENTED_EDGE ( 'NONE', *, *, #2065, .F. ) ;
#62150=DIRECTION ( 'NONE',  ( 0.000000000000000000, 0.000000000000000000, 1.000000000000000000 ) ) ;
#62160=CARTESIAN_POINT ( 'NONE',  ( 5.999999999999999112, -33.71516098798685590, -74.74816331893465815 ) ) ;
#62167=VERTEX_POINT ( 'NONE', #36788 ) ;
#62168=CYLINDRICAL_SURFACE ( 'NONE', #19053, 82.00000000000000000 ) ;
#62174=AXIS2_PLACEMENT_3D ( 'NONE', #6262, #67924, #73545 ) ;
#62179=ORIENTED_EDGE ( 'NONE', *, *, #33106, .F. ) ;
#62182=DIRECTION ( 'NONE',  ( 0.000000000000000000, -1.000000000000000000, -1.040834085586084730E-14 ) ) ;
#62183=DIRECTION ( 'NONE',  ( -1.000000000000000000, -0.000000000000000000, 0.000000000000000000 ) ) ;
#62197=AXIS2_PLACEMENT_3D ( 'NONE', #28485, #34501, #35272 ) ;
#62200=VECTOR ( 'NONE', #46873, 1000.000000000000000 ) ;
#62205=ADVANCED_FACE ( 'NONE', ( #14599 ), #13493, .T. ) ;
#62208=ORIENTED_EDGE ( 'NONE', *, *, #51793, .T. ) ;
#62211=EDGE_CURVE ( 'NONE', #68341, #13137, #54099, .T. ) ;
#62225=AXIS2_PLACEMENT_3D ( 'NONE', #7077, #1850, #52944 ) ;
#62239=EDGE_LOOP ( 'NONE', ( #71367, #43143, #13575, #14249 ) ) ;
#62243=ORIENTED_EDGE ( 'NONE', *, *, #72124, .F. ) ;
#62246=EDGE_CURVE ( 'NONE', #23563, #62167, #25511, .T. ) ;
#62248=DIRECTION ( 'NONE',  ( 0.000000000000000000, 0.000000000000000000, 1.000000000000000000 ) ) ;
#62253=CARTESIAN_POINT ( 'NONE',  ( 11.99999999999999822, -68.27212725128254078, -31.46837873495049465 ) ) ;
#62279=CARTESIAN_POINT ( 'NONE',  ( 11.99999999999999822, -75.11764819372145041, 29.05362095685286050 ) ) ;
#62282=AXIS2_PLACEMENT_3D ( 'NONE', #4669, #50115, #50875 ) ;
#62297=CYLINDRICAL_SURFACE ( 'NONE', #2830, 82.00000000000000000 ) ;
#62298=DIRECTION ( 'NONE',  ( -1.000000000000000000, 0.000000000000000000, -0.000000000000000000 ) ) ;
#62301=AXIS2_PLACEMENT_3D ( 'NONE', #7256, #1652, #52743 ) ;
#62315=CIRCLE ( 'NONE', #53874, 82.00000000000000000 ) ;
#62322=VERTEX_POINT ( 'NONE', #3720 ) ;
#62324=ORIENTED_EDGE ( 'NONE', *, *, #35040, .F. ) ;
#62329=DIRECTION ( 'NONE',  ( 0.000000000000000000, 0.000000000000000000, 1.000000000000000000 ) ) ;
#62333=CARTESIAN_POINT ( 'NONE',  ( 12.00000000000000000, 16.83928648764945635, 16.46020748918027010 ) ) ;
#62337=ORIENTED_EDGE ( 'NONE', *, *, #43333, .F. ) ;
#62339=ORIENTED_EDGE ( 'NONE', *, *, #29082, .T. ) ;
#62343=EDGE_CURVE ( 'NONE', #29316, #15874, #58561, .T. ) ;
#62351=EDGE_LOOP ( 'NONE', ( #3689, #19705, #50500, #6947 ) ) ;
#62353=ORIENTED_EDGE ( 'NONE', *, *, #22425, .F. ) ;
#62362=PLANE ( 'NONE',  #22050 ) ;
#62370=ORIENTED_EDGE ( 'NONE', *, *, #18899, .T. ) ;
#62375=EDGE_LOOP ( 'NONE', ( #36741, #8820, #17831, #13488 ) ) ;
#62385=DIRECTION ( 'NONE',  ( 0.000000000000000000, 0.000000000000000000, 1.000000000000000000 ) ) ;
#62393=EDGE_CURVE ( 'NONE', #38016, #28475, #53776, .T. ) ;
#62397=EDGE_CURVE ( 'NONE', #47439, #65482, #38656, .T. ) ;
#62417=VECTOR ( 'NONE', #21366, 1000.000000000000000 ) ;
#62421=AXIS2_PLACEMENT_3D ( 'NONE', #54645, #31701, #43391 ) ;
#62423=EDGE_CURVE ( 'NONE', #72940, #32025, #67594, .T. ) ;
#62432=ORIENTED_EDGE ( 'NONE', *, *, #58237, .F. ) ;
#62435=EDGE_LOOP ( 'NONE', ( #31239, #3521, #54111, #28356 ) ) ;
#62437=LINE ( 'NONE', #33839, #30431 ) ;
#62439=CARTESIAN_POINT ( 'NONE',  ( 0.000000000000000000, 0.000000000000000000, 0.000000000000000000 ) ) ;
#62440=DIRECTION ( 'NONE',  ( -1.000000000000000000, 0.000000000000000000, -0.000000000000000000 ) ) ;
#62448=CIRCLE ( 'NONE', #39636, 31.99999999999998579 ) ;
#62452=CARTESIAN_POINT ( 'NONE',  ( -10.00000000000000000, 0.000000000000000000, 0.000000000000000000 ) ) ;
#62471=AXIS2_PLACEMENT_3D ( 'NONE', #30349, #64954, #18697 ) ;
#62472=FACE_OUTER_BOUND ( 'NONE', #12389, .T. ) ;
#62486=ORIENTED_EDGE ( 'NONE', *, *, #13132, .T. ) ;
#62492=CYLINDRICAL_SURFACE ( 'NONE', #47775, 77.49899999999999523 ) ;
#62496=ORIENTED_EDGE ( 'NONE', *, *, #64197, .T. ) ;
#62498=DIRECTION ( 'NONE',  ( -1.000000000000000000, 0.000000000000000000, 0.000000000000000000 ) ) ;
#62499=CARTESIAN_POINT ( 'NONE',  ( 11.99999999999999822, 28.89263327155746097, 71.91182617369197771 ) ) ;
#62500=CARTESIAN_POINT ( 'NONE',  ( 5.999999999999999112, 59.75363087400153006, -56.15606465354896670 ) ) ;
#62508=EDGE_CURVE ( 'NONE', #8415, #42183, #4088, .T. ) ;
#62515=EDGE_CURVE ( 'NONE', #62167, #29219, #29722, .T. ) ;
#62516=ORIENTED_EDGE ( 'NONE', *, *, #25412, .F. ) ;
#62517=DIRECTION ( 'NONE',  ( 0.000000000000000000, 0.000000000000000000, 1.000000000000000000 ) ) ;
#62520=DIRECTION ( 'NONE',  ( -1.000000000000000000, 0.000000000000000000, 0.000000000000000000 ) ) ;
#62523=DIRECTION ( 'NONE',  ( -1.000000000000000000, 0.000000000000000000, -0.000000000000000000 ) ) ;
#62525=ORIENTED_EDGE ( 'NONE', *, *, #31116, .T. ) ;
#62526=ORIENTED_EDGE ( 'NONE', *, *, #3412, .T. ) ;
#62529=ORIENTED_EDGE ( 'NONE', *, *, #40923, .T. ) ;
#62534=VERTEX_POINT ( 'NONE', #34864 ) ;
#62543=CARTESIAN_POINT ( 'NONE',  ( 15.00000000000000000, 23.59884966291538078, 12.14883922797231008 ) ) ;
#62553=CARTESIAN_POINT ( 'NONE',  ( 15.00000000000000000, 0.000000000000000000, 0.000000000000000000 ) ) ;
#62554=DIRECTION ( 'NONE',  ( 0.000000000000000000, 0.000000000000000000, 1.000000000000000000 ) ) ;
#62556=CARTESIAN_POINT ( 'NONE',  ( 0.000000000000000000, 28.89263327155848415, -71.91182617369156560 ) ) ;
#62558=CARTESIAN_POINT ( 'NONE',  ( 0.000000000000000000, 62.50329211542435104, 41.76937507738811917 ) ) ;
#62564=AXIS2_PLACEMENT_3D ( 'NONE', #14081, #2496, #60343 ) ;
#62571=CARTESIAN_POINT ( 'NONE',  ( 0.000000000000000000, 0.000000000000000000, 0.000000000000000000 ) ) ;
#62573=DIRECTION ( 'NONE',  ( 0.000000000000000000, 0.000000000000000000, 1.000000000000000000 ) ) ;
#62574=DIRECTION ( 'NONE',  ( -1.000000000000000000, 0.000000000000000000, -0.000000000000000000 ) ) ;
#62579=EDGE_CURVE ( 'NONE', #68468, #7579, #44242, .T. ) ;
#62585=CARTESIAN_POINT ( 'NONE',  ( 0.000000000000000000, 0.000000000000000000, 0.000000000000000000 ) ) ;
#62588=VECTOR ( 'NONE', #30002, 1000.000000000000000 ) ;
#62594=ORIENTED_EDGE ( 'NONE', *, *, #52746, .T. ) ;
#62603=CYLINDRICAL_SURFACE ( 'NONE', #2288, 31.99999999999998579 ) ;
#62617=ORIENTED_EDGE ( 'NONE', *, *, #35132, .T. ) ;
#62619=CARTESIAN_POINT ( 'NONE',  ( 11.99999999999999822, 46.54456581323805153, 59.03342792756280488 ) ) ;
#62623=ORIENTED_EDGE ( 'NONE', *, *, #61084, .F. ) ;
#62628=AXIS2_PLACEMENT_3D ( 'NONE', #9556, #32472, #50511 ) ;
#62629=CIRCLE ( 'NONE', #18175, 82.00000000000000000 ) ;
#62632=AXIS2_PLACEMENT_3D ( 'NONE', #1029, #18634, #18275 ) ;
#62639=CARTESIAN_POINT ( 'NONE',  ( 11.99999999999999822, -31.46837873494930093, -68.27212725128309501 ) ) ;
#62651=DIRECTION ( 'NONE',  ( -1.000000000000000000, 0.000000000000000000, 0.000000000000000000 ) ) ;
#62664=DIRECTION ( 'NONE',  ( 0.000000000000000000, -0.4539904997395350361, -0.8910065241883738940 ) ) ;
#62671=ORIENTED_EDGE ( 'NONE', *, *, #74205, .F. ) ;
#62673=AXIS2_PLACEMENT_3D ( 'NONE', #1194, #11308, #34241 ) ;
#62677=CARTESIAN_POINT ( 'NONE',  ( 0.000000000000000000, 21.60688246758697062, -79.10210256391344785 ) ) ;
#62679=CARTESIAN_POINT ( 'NONE',  ( 11.99999999999999822, 39.78640506895604290, 66.50666863322015843 ) ) ;
#62683=DIRECTION ( 'NONE',  ( 1.000000000000000000, 0.000000000000000000, 0.000000000000000000 ) ) ;
#62685=VECTOR ( 'NONE', #14064, 1000.000000000000000 ) ;
#62692=ORIENTED_EDGE ( 'NONE', *, *, #39987, .F. ) ;
#62695=AXIS2_PLACEMENT_3D ( 'NONE', #55929, #4827, #66842 ) ;
#62705=LINE ( 'NONE', #50641, #28791 ) ;
#62717=ORIENTED_EDGE ( 'NONE', *, *, #69410, .F. ) ;
#62720=EDGE_LOOP ( 'NONE', ( #14418, #52992, #32253, #13515 ) ) ;
#62723=ORIENTED_EDGE ( 'NONE', *, *, #34555, .F. ) ;
#62730=ORIENTED_EDGE ( 'NONE', *, *, #74004, .F. ) ;
#62742=CARTESIAN_POINT ( 'NONE',  ( 11.99999999999999822, 36.72794159290334903, -65.59268652807170952 ) ) ;
#62747=PLANE ( 'NONE',  #71111 ) ;
#62753=ORIENTED_EDGE ( 'NONE', *, *, #60263, .F. ) ;
#62757=ORIENTED_EDGE ( 'NONE', *, *, #17902, .F. ) ;
#62758=DIRECTION ( 'NONE',  ( -1.000000000000000000, -0.000000000000000000, -0.000000000000000000 ) ) ;
#62764=LINE ( 'NONE', #34159, #24852 ) ;
#62771=CARTESIAN_POINT ( 'NONE',  ( -10.00000000000000000, 0.000000000000000000, 0.000000000000000000 ) ) ;
#62773=DIRECTION ( 'NONE',  ( -1.000000000000000000, -0.000000000000000000, 0.000000000000000000 ) ) ;
#62776=DIRECTION ( 'NONE',  ( 0.000000000000000000, 0.3090169943749461745, -0.9510565162951539753 ) ) ;
#62778=DIRECTION ( 'NONE',  ( -1.000000000000000000, -0.000000000000000000, 0.000000000000000000 ) ) ;
#62783=FACE_OUTER_BOUND ( 'NONE', #36171, .T. ) ;
#62787=CIRCLE ( 'NONE', #3957, 31.99999999999998934 ) ;
#62793=CYLINDRICAL_SURFACE ( 'NONE', #68382, 77.49899999999999523 ) ;
#62801=EDGE_LOOP ( 'NONE', ( #31725, #58632, #46871, #49709 ) ) ;
#62806=ORIENTED_EDGE ( 'NONE', *, *, #6174, .F. ) ;
#62811=ORIENTED_EDGE ( 'NONE', *, *, #61614, .F. ) ;
#62817=EDGE_LOOP ( 'NONE', ( #38304, #69975, #58024, #12217 ) ) ;
#62821=VERTEX_POINT ( 'NONE', #10355 ) ;
#62825=VERTEX_POINT ( 'NONE', #44204 ) ;
#62831=AXIS2_PLACEMENT_3D ( 'NONE', #54272, #38450, #42993 ) ;
#62835=DIRECTION ( 'NONE',  ( -1.000000000000000000, -0.000000000000000000, 0.000000000000000000 ) ) ;
#62845=ADVANCED_FACE ( 'NONE', ( #44955 ), #38186, .T. ) ;
#62852=PLANE ( 'NONE',  #71064 ) ;
#62854=AXIS2_PLACEMENT_3D ( 'NONE', #30728, #36010, #19085 ) ;
#62858=ADVANCED_FACE ( 'NONE', ( #4364 ), #61502, .T. ) ;
#62864=VERTEX_POINT ( 'NONE', #68253 ) ;
#62871=CARTESIAN_POINT ( 'NONE',  ( 11.99999999999999822, 46.11716303203186840, 67.80270845531904911 ) ) ;
#62883=CIRCLE ( 'NONE', #36440, 31.99999999999998579 ) ;
#62884=DIRECTION ( 'NONE',  ( -1.000000000000000000, -0.000000000000000000, 0.000000000000000000 ) ) ;
#62887=DIRECTION ( 'NONE',  ( -1.000000000000000000, -0.000000000000000000, -0.000000000000000000 ) ) ;
#62888=ORIENTED_EDGE ( 'NONE', *, *, #51288, .T. ) ;
#62889=VECTOR ( 'NONE', #28197, 1000.000000000000000 ) ;
#62894=VERTEX_POINT ( 'NONE', #34395 ) ;
#62898=VECTOR ( 'NONE', #34075, 1000.000000000000000 ) ;
#62906=ADVANCED_FACE ( 'NONE', ( #51695 ), #35141, .T. ) ;
#62910=ORIENTED_EDGE ( 'NONE', *, *, #59106, .F. ) ;
#62917=ORIENTED_EDGE ( 'NONE', *, *, #19242, .F. ) ;
#62925=DIRECTION ( 'NONE',  ( 0.000000000000000000, -0.7431448254773953543, -0.6691306063588570163 ) ) ;
#62927=DIRECTION ( 'NONE',  ( -1.000000000000000000, -0.000000000000000000, 0.000000000000000000 ) ) ;
#62931=AXIS2_PLACEMENT_3D ( 'NONE', #16493, #28885, #5236 ) ;
#62941=AXIS2_PLACEMENT_3D ( 'NONE', #54613, #14005, #7278 ) ;
#62944=DIRECTION ( 'NONE',  ( -1.000000000000000000, -0.000000000000000000, -0.000000000000000000 ) ) ;
#62946=ORIENTED_EDGE ( 'NONE', *, *, #32434, .F. ) ;
#62950=CARTESIAN_POINT ( 'NONE',  ( 11.99999999999999822, 0.000000000000000000, 0.000000000000000000 ) ) ;
#62954=LINE ( 'NONE', #7535, #39962 ) ;
#62964=CARTESIAN_POINT ( 'NONE',  ( 0.000000000000000000, -41.19522573413689059, -65.64334221924951862 ) ) ;
#62965=DIRECTION ( 'NONE',  ( -1.000000000000000000, 0.000000000000000000, -0.000000000000000000 ) ) ;
#62970=AXIS2_PLACEMENT_3D ( 'NONE', #62543, #44502, #44871 ) ;
#62980=EDGE_CURVE ( 'NONE', #49355, #25988, #974, .T. ) ;
#62994=ORIENTED_EDGE ( 'NONE', *, *, #47883, .T. ) ;
#63001=EDGE_CURVE ( 'NONE', #19051, #12910, #41521, .T. ) ;
#63012=AXIS2_PLACEMENT_3D ( 'NONE', #17341, #4972, #6443 ) ;
#63013=LINE ( 'NONE', #41530, #33563 ) ;
#63018=DIRECTION ( 'NONE',  ( -1.000000000000000000, -0.000000000000000000, -0.000000000000000000 ) ) ;
#63025=EDGE_CURVE ( 'NONE', #8298, #25226, #6220, .T. ) ;
#63028=FACE_OUTER_BOUND ( 'NONE', #8915, .T. ) ;
#63032=DIRECTION ( 'NONE',  ( 0.000000000000000000, 0.8090169943749486725, -0.5877852522924713607 ) ) ;
#63035=EDGE_CURVE ( 'NONE', #7392, #3697, #13038, .T. ) ;
#63038=ADVANCED_FACE ( 'NONE', ( #64460 ), #70822, .F. ) ;
#63042=VERTEX_POINT ( 'NONE', #36990 ) ;
#63047=CARTESIAN_POINT ( 'NONE',  ( 0.000000000000000000, -56.15606465355000410, 59.75363087400056372 ) ) ;
#63054=CARTESIAN_POINT ( 'NONE',  ( 11.99999999999999822, -75.11764819372145041, -2.946379043147127064 ) ) ;
#63060=ORIENTED_EDGE ( 'NONE', *, *, #18069, .F. ) ;
#63061=CYLINDRICAL_SURFACE ( 'NONE', #68882, 82.00000000000000000 ) ;
#63065=CARTESIAN_POINT ( 'NONE',  ( 11.99999999999999822, -11.30684508768393748, 76.66974797899833050 ) ) ;
#63067=ORIENTED_EDGE ( 'NONE', *, *, #3163, .T. ) ;
#63069=CARTESIAN_POINT ( 'NONE',  ( 0.000000000000000000, 77.32052557432841411, 5.256550761633121738 ) ) ;
#63071=EDGE_CURVE ( 'NONE', #54637, #28318, #33483, .T. ) ;
#63074=ADVANCED_FACE ( 'NONE', ( #30595 ), #48273, .T. ) ;
#63075=VERTEX_POINT ( 'NONE', #47535 ) ;
#63098=EDGE_LOOP ( 'NONE', ( #37014, #19074, #68045, #65823 ) ) ;
#63100=ORIENTED_EDGE ( 'NONE', *, *, #55159, .F. ) ;
#63107=EDGE_CURVE ( 'NONE', #52404, #12733, #27477, .T. ) ;
#63110=CARTESIAN_POINT ( 'NONE',  ( 11.99999999999999822, 65.58780272294076497, 36.73666225445916211 ) ) ;
#63111=CARTESIAN_POINT ( 'NONE',  ( 0.000000000000000000, 0.000000000000000000, 0.000000000000000000 ) ) ;
#63113=ORIENTED_EDGE ( 'NONE', *, *, #70659, .T. ) ;
#63116=AXIS2_PLACEMENT_3D ( 'NONE', #60460, #44656, #73197 ) ;
#63118=ORIENTED_EDGE ( 'NONE', *, *, #60934, .F. ) ;
#63121=FACE_BOUND ( 'NONE', #70476, .T. ) ;
#63122=VERTEX_POINT ( 'NONE', #65576 ) ;
#63126=ORIENTED_EDGE ( 'NONE', *, *, #813, .T. ) ;
#63132=VERTEX_POINT ( 'NONE', #19321 ) ;
#63134=EDGE_CURVE ( 'NONE', #9528, #28379, #22664, .T. ) ;
#63138=CARTESIAN_POINT ( 'NONE',  ( 11.99999999999999822, 0.000000000000000000, 0.000000000000000000 ) ) ;
#63140=CARTESIAN_POINT ( 'NONE',  ( 11.99999999999999822, -68.67312586195022561, 35.91791733033451806 ) ) ;
#63142=FACE_OUTER_BOUND ( 'NONE', #72722, .T. ) ;
#63148=CARTESIAN_POINT ( 'NONE',  ( 15.00000000000000000, -19.89357724624986545, 12.59942793731086219 ) ) ;
#63150=DIRECTION ( 'NONE',  ( -1.000000000000000000, 0.000000000000000000, 0.000000000000000000 ) ) ;
#63160=ADVANCED_FACE ( 'NONE', ( #2817 ), #9529, .T. ) ;
#63181=ORIENTED_EDGE ( 'NONE', *, *, #68532, .F. ) ;
#63187=EDGE_LOOP ( 'NONE', ( #8412, #17604, #33301, #38922 ) ) ;
#63191=DIRECTION ( 'NONE',  ( -1.000000000000000000, -0.000000000000000000, -0.000000000000000000 ) ) ;
#63193=ORIENTED_EDGE ( 'NONE', *, *, #22240, .F. ) ;
#63196=CYLINDRICAL_SURFACE ( 'NONE', #50533, 77.49899999999999523 ) ;
#63198=ORIENTED_EDGE ( 'NONE', *, *, #62343, .T. ) ;
#63199=EDGE_CURVE ( 'NONE', #3531, #61698, #33428, .T. ) ;
#63201=ORIENTED_EDGE ( 'NONE', *, *, #52008, .F. ) ;
#63213=DIRECTION ( 'NONE',  ( -1.000000000000000000, 0.000000000000000000, 0.000000000000000000 ) ) ;
#63231=DIRECTION ( 'NONE',  ( -1.000000000000000000, 0.000000000000000000, -0.000000000000000000 ) ) ;
#63236=DIRECTION ( 'NONE',  ( 0.000000000000000000, -0.7604059656000369261, 0.6494480483301767748 ) ) ;
#63238=ADVANCED_FACE ( 'NONE', ( #49398 ), #62168, .T. ) ;
#63239=CYLINDRICAL_SURFACE ( 'NONE', #64379, 31.99999999999998579 ) ;
#63250=VECTOR ( 'NONE', #52704, 1000.000000000000000 ) ;
#63252=EDGE_CURVE ( 'NONE', #4121, #9267, #27576, .T. ) ;
#63258=ORIENTED_EDGE ( 'NONE', *, *, #55358, .F. ) ;
#63261=DIRECTION ( 'NONE',  ( -1.000000000000000000, 0.000000000000000000, 0.000000000000000000 ) ) ;
#63267=AXIS2_PLACEMENT_3D ( 'NONE', #46214, #45106, #40201 ) ;
#63276=DIRECTION ( 'NONE',  ( 1.000000000000000000, 0.000000000000000000, 0.000000000000000000 ) ) ;
#63279=CARTESIAN_POINT ( 'NONE',  ( 0.000000000000000000, 62.50884508063427347, 41.76106447765511831 ) ) ;
#63285=VERTEX_POINT ( 'NONE', #72324 ) ;
#63296=DIRECTION ( 'NONE',  ( 0.000000000000000000, 0.000000000000000000, 1.000000000000000000 ) ) ;
#63304=CYLINDRICAL_SURFACE ( 'NONE', #44745, 82.00000000000000000 ) ;
#63305=FACE_OUTER_BOUND ( 'NONE', #612, .T. ) ;
#63306=FACE_OUTER_BOUND ( 'NONE', #25510, .T. ) ;
#63308=VECTOR ( 'NONE', #56361, 1000.000000000000000 ) ;
#63311=AXIS2_PLACEMENT_3D ( 'NONE', #1174, #11291, #46617 ) ;
#63320=FILL_AREA_STYLE ('',( #12898 ) ) ;
#63321=ADVANCED_FACE ( 'NONE', ( #73432 ), #33206, .F. ) ;
#63322=ADVANCED_FACE ( 'NONE', ( #33958 ), #3564, .F. ) ;
#63326=FACE_OUTER_BOUND ( 'NONE', #51345, .T. ) ;
#63335=ORIENTED_EDGE ( 'NONE', *, *, #46582, .F. ) ;
#63337=ORIENTED_EDGE ( 'NONE', *, *, #31223, .F. ) ;
#63342=VERTEX_POINT ( 'NONE', #56907 ) ;
#63344=ORIENTED_EDGE ( 'NONE', *, *, #4864, .F. ) ;
#63347=EDGE_CURVE ( 'NONE', #14951, #60573, #17408, .T. ) ;
#63348=EDGE_LOOP ( 'NONE', ( #15495, #72755, #23848, #54533 ) ) ;
#63353=AXIS2_PLACEMENT_3D ( 'NONE', #44998, #33312, #33702 ) ;
#63356=ORIENTED_EDGE ( 'NONE', *, *, #59597, .T. ) ;
#63358=DIRECTION ( 'NONE',  ( -1.000000000000000000, 0.000000000000000000, 0.000000000000000000 ) ) ;
#63366=CARTESIAN_POINT ( 'NONE',  ( 0.000000000000000000, -79.10210256391353312, -21.60688246758670061 ) ) ;
#63371=ORIENTED_EDGE ( 'NONE', *, *, #58805, .F. ) ;
#63376=FACE_OUTER_BOUND ( 'NONE', #10761, .T. ) ;
#63377=DIRECTION ( 'NONE',  ( 0.000000000000000000, -0.8090169943749402348, -0.5877852522924830181 ) ) ;
#63378=DIRECTION ( 'NONE',  ( 0.000000000000000000, 0.000000000000000000, 1.000000000000000000 ) ) ;
#63380=ORIENTED_EDGE ( 'NONE', *, *, #66744, .T. ) ;
#63392=CARTESIAN_POINT ( 'NONE',  ( 11.99999999999999822, 17.28742895386189460, -75.54627589209927407 ) ) ;
#63395=VECTOR ( 'NONE', #117, 1000.000000000000000 ) ;
#63397=CARTESIAN_POINT ( 'NONE',  ( 12.00000000000000000, -10.45096189432344502, -21.10159698893425784 ) ) ;
#63417=EDGE_CURVE ( 'NONE', #67162, #63432, #51622, .T. ) ;
#63420=CIRCLE ( 'NONE', #12998, 31.99999999999998934 ) ;
#63421=CIRCLE ( 'NONE', #38172, 77.49899999999999523 ) ;
#63424=DIRECTION ( 'NONE',  ( 1.000000000000000000, 0.000000000000000000, 0.000000000000000000 ) ) ;
#63432=VERTEX_POINT ( 'NONE', #64025 ) ;
#63445=ORIENTED_EDGE ( 'NONE', *, *, #60041, .F. ) ;
#63465=VECTOR ( 'NONE', #17006, 1000.000000000000000 ) ;
#63475=AXIS2_PLACEMENT_3D ( 'NONE', #54617, #3504, #20020 ) ;
#63476=FACE_BOUND ( 'NONE', #64428, .T. ) ;
#63479=CARTESIAN_POINT ( 'NONE',  ( 0.000000000000000000, 44.99326035066052043, 68.55367621811159040 ) ) ;
#63497=CARTESIAN_POINT ( 'NONE',  ( 11.99999999999999822, 73.72996012237460661, -14.67089635893632504 ) ) ;
#63498=VECTOR ( 'NONE', #21421, 1000.000000000000000 ) ;
#63500=AXIS2_PLACEMENT_3D ( 'NONE', #46303, #29360, #52305 ) ;
#63505=LINE ( 'NONE', #67650, #454 ) ;
#63509=VECTOR ( 'NONE', #25717, 1000.000000000000000 ) ;
#63511=EDGE_CURVE ( 'NONE', #6829, #70343, #31637, .T. ) ;
#63512=ORIENTED_EDGE ( 'NONE', *, *, #33105, .T. ) ;
#63522=ADVANCED_FACE ( 'NONE', ( #65503 ), #53471, .F. ) ;
#63525=VERTEX_POINT ( 'NONE', #2008 ) ;
#63528=ORIENTED_EDGE ( 'NONE', *, *, #48358, .T. ) ;
#63531=ORIENTED_EDGE ( 'NONE', *, *, #34162, .F. ) ;
#63536=ORIENTED_EDGE ( 'NONE', *, *, #24856, .T. ) ;
#63538=CIRCLE ( 'NONE', #56345, 31.99999999999998934 ) ;
#63545=AXIS2_PLACEMENT_3D ( 'NONE', #38719, #49249, #37975 ) ;
#63551=VERTEX_POINT ( 'NONE', #1642 ) ;
#63560=DIRECTION ( 'NONE',  ( -1.000000000000000000, 0.000000000000000000, -0.000000000000000000 ) ) ;
#63561=CARTESIAN_POINT ( 'NONE',  ( 11.99999999999999822, 80.55351364060611274, -15.33399622253397609 ) ) ;
#63578=AXIS2_PLACEMENT_3D ( 'NONE', #65609, #14829, #54690 ) ;
#63599=CARTESIAN_POINT ( 'NONE',  ( 15.00000000000000000, -25.60904388321925040, -6.976881207771165272 ) ) ;
#63618=ADVANCED_FACE ( 'NONE', ( #32738 ), #16203, .T. ) ;
#63620=VERTEX_POINT ( 'NONE', #61341 ) ;
#63623=FACE_OUTER_BOUND ( 'NONE', #47270, .T. ) ;
#63627=FACE_OUTER_BOUND ( 'NONE', #28879, .T. ) ;
#63629=ORIENTED_EDGE ( 'NONE', *, *, #9141, .T. ) ;
#63631=ORIENTED_EDGE ( 'NONE', *, *, #66278, .T. ) ;
#63634=VERTEX_POINT ( 'NONE', #72955 ) ;
#63635=ORIENTED_EDGE ( 'NONE', *, *, #16538, .F. ) ;
#63637=VERTEX_POINT ( 'NONE', #20733 ) ;
#63641=VERTEX_POINT ( 'NONE', #56442 ) ;
#63643=ORIENTED_EDGE ( 'NONE', *, *, #53571, .T. ) ;
#63644=VECTOR ( 'NONE', #44641, 999.9999999999998863 ) ;
#63651=FACE_OUTER_BOUND ( 'NONE', #65569, .T. ) ;
#63655=CIRCLE ( 'NONE', #69646, 77.49900000000002365 ) ;
#63664=LINE ( 'NONE', #12133, #10318 ) ;
#63670=DIRECTION ( 'NONE',  ( -1.000000000000000000, -0.000000000000000000, 0.000000000000000000 ) ) ;
#63700=CYLINDRICAL_SURFACE ( 'NONE', #44904, 31.99999999999998579 ) ;
#63701=DIRECTION ( 'NONE',  ( 0.000000000000000000, -0.9945218953682742891, -0.1045284632676436315 ) ) ;
#63703=CIRCLE ( 'NONE', #61275, 82.00000000000000000 ) ;
#63716=ORIENTED_EDGE ( 'NONE', *, *, #451, .T. ) ;
#63724=VERTEX_POINT ( 'NONE', #68466 ) ;
#63725=AXIS2_PLACEMENT_3D ( 'NONE', #21295, #14185, #42772 ) ;
#63728=CARTESIAN_POINT ( 'NONE',  ( 11.99999999999999822, -14.67089635893764665, 73.72996012237435082 ) ) ;
#63759=AXIS2_PLACEMENT_3D ( 'NONE', #64123, #17874, #1376 ) ;
#63762=CIRCLE ( 'NONE', #73324, 31.99999999999999289 ) ;
#63765=VECTOR ( 'NONE', #56382, 1000.000000000000000 ) ;
#63771=EDGE_CURVE ( 'NONE', #45, #24268, #21578, .T. ) ;
#63776=CARTESIAN_POINT ( 'NONE',  ( 0.000000000000000000, 77.19088730480524418, 6.903761155838049390 ) ) ;
#63777=DIRECTION ( 'NONE',  ( 0.000000000000000000, 0.3090169943749410675, 0.9510565162951556406 ) ) ;
#63779=DIRECTION ( 'NONE',  ( 0.000000000000000000, 0.000000000000000000, 1.000000000000000000 ) ) ;
#63796=APPLICATION_CONTEXT ( 'automotive_design' ) ;
#63800=AXIS2_PLACEMENT_3D ( 'NONE', #21945, #50124, #33587 ) ;
#63804=EDGE_LOOP ( 'NONE', ( #50092, #4176, #7403, #72675 ) ) ;
#63817=VERTEX_POINT ( 'NONE', #16957 ) ;
#63821=DIRECTION ( 'NONE',  ( 0.000000000000000000, -0.8660254037844363761, 0.5000000000000039968 ) ) ;
#63837=EDGE_CURVE ( 'NONE', #55085, #63132, #15578, .T. ) ;
#63851=CARTESIAN_POINT ( 'NONE',  ( 15.00000000000000000, 14.60985201121703980, -18.46759930825707841 ) ) ;
#63867=VECTOR ( 'NONE', #569, 1000.000000000000000 ) ;
#63870=DIRECTION ( 'NONE',  ( -0.000000000000000000, -1.000000000000000000, -1.445602896647339656E-16 ) ) ;
#63874=DIRECTION ( 'NONE',  ( -1.000000000000000000, 0.000000000000000000, 0.000000000000000000 ) ) ;
#63875=EDGE_CURVE ( 'NONE', #40071, #6388, #55171, .T. ) ;
#63883=EDGE_LOOP ( 'NONE', ( #27279, #57905, #64581, #73453 ) ) ;
#63893=ORIENTED_EDGE ( 'NONE', *, *, #18587, .F. ) ;
#63894=AXIS2_PLACEMENT_3D ( 'NONE', #43606, #26657, #27390 ) ;
#63895=DIRECTION ( 'NONE',  ( 0.000000000000000000, 0.000000000000000000, 1.000000000000000000 ) ) ;
#63899=LINE ( 'NONE', #1515, #48417 ) ;
#63902=ADVANCED_FACE ( 'NONE', ( #30799 ), #65775, .T. ) ;
#63909=DIRECTION ( 'NONE',  ( -1.000000000000000000, 0.000000000000000000, 0.000000000000000000 ) ) ;
#63911=ORIENTED_EDGE ( 'NONE', *, *, #9989, .T. ) ;
#63915=EDGE_CURVE ( 'NONE', #19352, #26439, #18421, .T. ) ;
#63917=CARTESIAN_POINT ( 'NONE',  ( 11.99999999999999822, 0.000000000000000000, 0.000000000000000000 ) ) ;
#63922=EDGE_CURVE ( 'NONE', #70343, #5982, #30072, .T. ) ;
#63925=FACE_OUTER_BOUND ( 'NONE', #7317, .T. ) ;
#63926=CARTESIAN_POINT ( 'NONE',  ( 6.000000000000000000, -74.18225833017864090, -34.94270380257717790 ) ) ;
#63927=VERTEX_POINT ( 'NONE', #2664 ) ;
#63935=DIRECTION ( 'NONE',  ( 0.000000000000000000, 0.000000000000000000, -1.000000000000000000 ) ) ;
#63939=ORIENTED_EDGE ( 'NONE', *, *, #3818, .F. ) ;
#63943=DIRECTION ( 'NONE',  ( -1.000000000000000000, 0.000000000000000000, -0.000000000000000000 ) ) ;
#63953=ADVANCED_FACE ( 'NONE', ( #1921 ), #3023, .T. ) ;
#63958=CIRCLE ( 'NONE', #12306, 82.00000000000000000 ) ;
#63961=CARTESIAN_POINT ( 'NONE',  ( 15.00000000000000000, 6.762365576493647445, 25.66652317338391498 ) ) ;
#63966=CARTESIAN_POINT ( 'NONE',  ( 11.99999999999999822, 0.000000000000000000, 0.000000000000000000 ) ) ;
#63974=LINE ( 'NONE', #57219, #44948 ) ;
#63978=DIRECTION ( 'NONE',  ( 0.000000000000000000, 0.9723699203976773342, -0.2334453638559026156 ) ) ;
#63989=EDGE_LOOP ( 'NONE', ( #38489, #21354, #39202, #59370 ) ) ;
#63996=EDGE_CURVE ( 'NONE', #33546, #68607, #32354, .T. ) ;
#64000=VERTEX_POINT ( 'NONE', #72140 ) ;
#64004=CARTESIAN_POINT ( 'NONE',  ( 11.99999999999999822, -54.21277698773636899, -55.38113227695839669 ) ) ;
#64007=ORIENTED_EDGE ( 'NONE', *, *, #37335, .F. ) ;
#64009=VERTEX_POINT ( 'NONE', #28413 ) ;
#64015=DIRECTION ( 'NONE',  ( 0.000000000000000000, 0.000000000000000000, 1.000000000000000000 ) ) ;
#64016=CARTESIAN_POINT ( 'NONE',  ( 11.99999999999999822, -34.94270380257585629, -74.18225833017926618 ) ) ;
#64025=CARTESIAN_POINT ( 'NONE',  ( 12.00000000000000000, 24.81905959214275370, 9.408202855044498492 ) ) ;
#64027=FACE_OUTER_BOUND ( 'NONE', #37893, .T. ) ;
#64030=DIRECTION ( 'NONE',  ( 1.000000000000000000, 0.000000000000000000, -0.000000000000000000 ) ) ;
#64033=DIRECTION ( 'NONE',  ( 0.000000000000000000, 0.3090169943749480619, -0.9510565162951533091 ) ) ;
#64034=DIRECTION ( 'NONE',  ( 0.000000000000000000, -0.9723699203976741146, -0.2334453638559158550 ) ) ;
#64048=ORIENTED_EDGE ( 'NONE', *, *, #59330, .F. ) ;
#64064=DIRECTION ( 'NONE',  ( 0.000000000000000000, -0.3090169943749548342, 0.9510565162951510887 ) ) ;
#64070=VECTOR ( 'NONE', #71414, 999.9999999999998863 ) ;
#64078=EDGE_LOOP ( 'NONE', ( #41623, #55593, #36979, #49732 ) ) ;
#64086=ORIENTED_EDGE ( 'NONE', *, *, #61458, .T. ) ;
#64087=EDGE_CURVE ( 'NONE', #6766, #71207, #52769, .T. ) ;
#64096=ORIENTED_EDGE ( 'NONE', *, *, #23013, .T. ) ;
#64100=CYLINDRICAL_SURFACE ( 'NONE', #73530, 82.00000000000000000 ) ;
#64109=LINE ( 'NONE', #13327, #300 ) ;
#64117=CARTESIAN_POINT ( 'NONE',  ( 11.99999999999999822, -56.15606465355001120, 59.75363087400055662 ) ) ;
#64123=CARTESIAN_POINT ( 'NONE',  ( 11.99999999999999822, 0.000000000000000000, 0.000000000000000000 ) ) ;
#64128=VERTEX_POINT ( 'NONE', #8501 ) ;
#64129=ORIENTED_EDGE ( 'NONE', *, *, #36307, .T. ) ;
#64131=LINE ( 'NONE', #73627, #41764 ) ;
#64132=DIRECTION ( 'NONE',  ( -1.000000000000000000, 0.000000000000000000, -0.000000000000000000 ) ) ;
#64137=DIRECTION ( 'NONE',  ( 0.000000000000000000, 0.8526401643540936215, -0.5224985647159469115 ) ) ;
#64150=DIRECTION ( 'NONE',  ( 0.000000000000000000, 1.000000000000000000, 3.469446951953615767E-15 ) ) ;
#64158=EDGE_LOOP ( 'NONE', ( #22491, #44435, #56415, #31253 ) ) ;
#64165=CARTESIAN_POINT ( 'NONE',  ( 15.00000000000000000, 20.85821328998741109, -10.92862929874522671 ) ) ;
#64166=DIRECTION ( 'NONE',  ( -1.000000000000000000, 0.000000000000000000, 0.000000000000000000 ) ) ;
#64170=CIRCLE ( 'NONE', #55628, 31.99999999999998579 ) ;
#64183=EDGE_LOOP ( 'NONE', ( #18551, #61168, #22336, #48090 ) ) ;
#64185=EDGE_LOOP ( 'NONE', ( #45360, #72916, #56257, #63528 ) ) ;
#64186=VERTEX_POINT ( 'NONE', #47982 ) ;
#64189=LINE ( 'NONE', #17944, #23373 ) ;
#64194=ORIENTED_EDGE ( 'NONE', *, *, #15952, .T. ) ;
#64196=EDGE_LOOP ( 'NONE', ( #54308, #60149, #62730, #61887 ) ) ;
#64197=EDGE_CURVE ( 'NONE', #22572, #50206, #35947, .T. ) ;
#64208=CARTESIAN_POINT ( 'NONE',  ( 12.00000000000000000, 23.59884966291538078, 12.14883922797231008 ) ) ;
#64216=DIRECTION ( 'NONE',  ( -1.000000000000000000, -0.000000000000000000, -0.000000000000000000 ) ) ;
#64221=AXIS2_PLACEMENT_3D ( 'NONE', #44743, #26683, #44362 ) ;
#64225=ORIENTED_EDGE ( 'NONE', *, *, #14323, .T. ) ;
#64227=AXIS2_PLACEMENT_3D ( 'NONE', #55727, #16995, #22261 ) ;
#64230=CARTESIAN_POINT ( 'NONE',  ( 15.00000000000000000, 8.688484142254226938, 21.88630264137359305 ) ) ;
#64233=DIRECTION ( 'NONE',  ( 0.000000000000000000, 0.000000000000000000, 1.000000000000000000 ) ) ;
#64235=CARTESIAN_POINT ( 'NONE',  ( 11.99999999999999822, -77.16300072079681627, 27.74655509720640367 ) ) ;
#64238=AXIS2_PLACEMENT_3D ( 'NONE', #27561, #68161, #73418 ) ;
#64247=ADVANCED_FACE ( 'NONE', ( #59632 ), #48342, .T. ) ;
#64249=DIRECTION ( 'NONE',  ( 0.000000000000000000, 0.000000000000000000, 1.000000000000000000 ) ) ;
#64271=ORIENTED_EDGE ( 'NONE', *, *, #54571, .F. ) ;
#64276=DIRECTION ( 'NONE',  ( 0.000000000000000000, -0.6494480483301739993, -0.7604059656000391465 ) ) ;
#64290=ORIENTED_EDGE ( 'NONE', *, *, #40513, .T. ) ;
#64295=VERTEX_POINT ( 'NONE', #17013 ) ;
#64301=ORIENTED_EDGE ( 'NONE', *, *, #45709, .F. ) ;
#64306=ORIENTED_EDGE ( 'NONE', *, *, #22268, .F. ) ;
#64333=EDGE_CURVE ( 'NONE', #47446, #57658, #22829, .T. ) ;
#64338=CARTESIAN_POINT ( 'NONE',  ( 11.99999999999999822, 0.000000000000000000, 0.000000000000000000 ) ) ;
#64340=DIRECTION ( 'NONE',  ( 0.000000000000000000, -0.2079116908177651990, -0.9781476007338044676 ) ) ;
#64345=FACE_OUTER_BOUND ( 'NONE', #42069, .T. ) ;
#64346=ORIENTED_EDGE ( 'NONE', *, *, #31473, .T. ) ;
#64348=FACE_OUTER_BOUND ( 'NONE', #16941, .T. ) ;
#64372=ORIENTED_EDGE ( 'NONE', *, *, #33725, .T. ) ;
#64379=AXIS2_PLACEMENT_3D ( 'NONE', #33908, #62884, #1230 ) ;
#64380=CARTESIAN_POINT ( 'NONE',  ( 0.000000000000000000, 0.000000000000000000, 0.000000000000000000 ) ) ;
#64394=CARTESIAN_POINT ( 'NONE',  ( 0.000000000000000000, 79.10210256391368944, 21.60688246758614994 ) ) ;
#64395=CARTESIAN_POINT ( 'NONE',  ( 11.99999999999999822, 0.000000000000000000, 0.000000000000000000 ) ) ;
#64396=DIRECTION ( 'NONE',  ( 0.000000000000000000, -0.8910065241883626808, -0.4539904997395568520 ) ) ;
#64397=CARTESIAN_POINT ( 'NONE',  ( -10.00000000000000000, 0.000000000000000000, 0.000000000000000000 ) ) ;
#64399=DIRECTION ( 'NONE',  ( 1.000000000000000000, -0.000000000000000000, 0.000000000000000000 ) ) ;
#64401=FACE_OUTER_BOUND ( 'NONE', #39128, .T. ) ;
#64405=DIRECTION ( 'NONE',  ( 0.000000000000000000, -0.2079116908177532363, 0.9781476007338069101 ) ) ;
#64413=ORIENTED_EDGE ( 'NONE', *, *, #46401, .F. ) ;
#64423=ADVANCED_FACE ( 'NONE', ( #54662 ), #20066, .F. ) ;
#64425=CARTESIAN_POINT ( 'NONE',  ( 0.000000000000000000, 40.65526001592611749, 71.21200624218811015 ) ) ;
#64428=EDGE_LOOP ( 'NONE', ( #21910, #60674, #44201, #59089 ) ) ;
#64440=VERTEX_POINT ( 'NONE', #37001 ) ;
#64446=EDGE_CURVE ( 'NONE', #14708, #1257, #71192, .T. ) ;
#64449=ORIENTED_EDGE ( 'NONE', *, *, #59435, .T. ) ;
#64452=ORIENTED_EDGE ( 'NONE', *, *, #45669, .T. ) ;
#64460=FACE_OUTER_BOUND ( 'NONE', #21321, .T. ) ;
#64461=ORIENTED_EDGE ( 'NONE', *, *, #32932, .F. ) ;
#64466=DIRECTION ( 'NONE',  ( -1.000000000000000000, -0.000000000000000000, -0.000000000000000000 ) ) ;
#64467=DIRECTION ( 'NONE',  ( -1.000000000000000000, -0.000000000000000000, 0.000000000000000000 ) ) ;
#64468=CARTESIAN_POINT ( 'NONE',  ( 11.99999999999999822, 26.01480285779933510, -70.53064760720289428 ) ) ;
#64488=AXIS2_PLACEMENT_3D ( 'NONE', #10740, #16757, #39696 ) ;
#64489=DIRECTION ( 'NONE',  ( 0.000000000000000000, 0.6494480483301793283, 0.7604059656000345946 ) ) ;
#64494=VERTEX_POINT ( 'NONE', #60685 ) ;
#64495=ADVANCED_FACE ( 'NONE', ( #49388 ), #3189, .T. ) ;
#64497=DIRECTION ( 'NONE',  ( 0.000000000000000000, -0.8660254037844363761, 0.5000000000000039968 ) ) ;
#64509=CIRCLE ( 'NONE', #60852, 77.49900000000000944 ) ;
#64511=EDGE_CURVE ( 'NONE', #4927, #30858, #9443, .T. ) ;
#64536=EDGE_CURVE ( 'NONE', #10181, #28846, #68448, .T. ) ;
#64545=ORIENTED_EDGE ( 'NONE', *, *, #14842, .F. ) ;
#64551=DIRECTION ( 'NONE',  ( -1.000000000000000000, 0.000000000000000000, 0.000000000000000000 ) ) ;
#64554=VERTEX_POINT ( 'NONE', #16665 ) ;
#64556=ORIENTED_EDGE ( 'NONE', *, *, #66974, .T. ) ;
#64561=EDGE_LOOP ( 'NONE', ( #21556, #12742, #20871, #35586 ) ) ;
#64581=ORIENTED_EDGE ( 'NONE', *, *, #26993, .F. ) ;
#64593=EDGE_CURVE ( 'NONE', #70197, #32025, #5406, .T. ) ;
#64604=EDGE_CURVE ( 'NONE', #4428, #74042, #50497, .T. ) ;
#64605=VECTOR ( 'NONE', #31661, 1000.000000000000000 ) ;
#64606=DIRECTION ( 'NONE',  ( 0.000000000000000000, 0.000000000000000000, -1.000000000000000000 ) ) ;
#64607=ADVANCED_FACE ( 'NONE', ( #21932 ), #22683, .T. ) ;
#64609=AXIS2_PLACEMENT_3D ( 'NONE', #44826, #5724, #33521 ) ;
#64610=CARTESIAN_POINT ( 'NONE',  ( 15.00000000000000000, 20.85821328998756385, 10.92862929874494249 ) ) ;
#64613=CARTESIAN_POINT ( 'NONE',  ( 15.00000000000000000, -22.32062822937469093, 14.36278369418830181 ) ) ;
#64618=VERTEX_POINT ( 'NONE', #4291 ) ;
#64619=DIRECTION ( 'NONE',  ( -1.000000000000000000, 0.000000000000000000, 0.000000000000000000 ) ) ;
#64623=ORIENTED_EDGE ( 'NONE', *, *, #24892, .T. ) ;
#64625=CIRCLE ( 'NONE', #10634, 31.99999999999998934 ) ;
#64629=ORIENTED_EDGE ( 'NONE', *, *, #19247, .F. ) ;
#64631=CIRCLE ( 'NONE', #43016, 31.99999999999998579 ) ;
#64635=ORIENTED_EDGE ( 'NONE', *, *, #26509, .T. ) ;
#64639=ORIENTED_EDGE ( 'NONE', *, *, #16752, .F. ) ;
#64643=ORIENTED_EDGE ( 'NONE', *, *, #35303, .T. ) ;
#64651=DIRECTION ( 'NONE',  ( 1.000000000000000000, -0.000000000000000000, -0.000000000000000000 ) ) ;
#64655=VERTEX_POINT ( 'NONE', #57262 ) ;
#64664=DIRECTION ( 'NONE',  ( 1.000000000000000000, 0.000000000000000000, 0.000000000000000000 ) ) ;
#64674=EDGE_CURVE ( 'NONE', #7335, #36701, #31064, .T. ) ;
#64680=CARTESIAN_POINT ( 'NONE',  ( 0.000000000000000000, 63.97538442413426907, 51.29473840253246664 ) ) ;
#64682=ADVANCED_FACE ( 'NONE', ( #39972 ), #73042, .T. ) ;
#64690=CARTESIAN_POINT ( 'NONE',  ( 11.99999999999999822, -55.16347631943085617, 60.67117009219116852 ) ) ;
#64692=CARTESIAN_POINT ( 'NONE',  ( 0.000000000000000000, 81.34940948281337114, 10.30890764327411446 ) ) ;
#64695=CARTESIAN_POINT ( 'NONE',  ( -10.00000000000000000, 0.000000000000000000, 0.000000000000000000 ) ) ;
#64707=VECTOR ( 'NONE', #72138, 1000.000000000000000 ) ;
#64712=AXIS2_PLACEMENT_3D ( 'NONE', #57216, #68118, #17354 ) ;
#64713=CARTESIAN_POINT ( 'NONE',  ( 6.000000000000000000, 79.10210256391398786, -21.60688246758503794 ) ) ;
#64721=EDGE_LOOP ( 'NONE', ( #66047, #17211, #3641, #13294 ) ) ;
#64736=DIRECTION ( 'NONE',  ( -1.000000000000000000, 0.000000000000000000, -0.000000000000000000 ) ) ;
#64740=ADVANCED_FACE ( 'NONE', ( #29401 ), #53464, .T. ) ;
#64744=ORIENTED_EDGE ( 'NONE', *, *, #72896, .T. ) ;
#64749=VECTOR ( 'NONE', #8947, 1000.000000000000000 ) ;
#64764=DIRECTION ( 'NONE',  ( 0.000000000000000000, -0.9510565162951507556, 0.3090169943749561110 ) ) ;
#64768=CIRCLE ( 'NONE', #31141, 82.00000000000000000 ) ;
#64777=CIRCLE ( 'NONE', #32328, 82.00000000000000000 ) ;
#64778=DIRECTION ( 'NONE',  ( -1.000000000000000000, -0.000000000000000000, -0.000000000000000000 ) ) ;
#64782=FACE_OUTER_BOUND ( 'NONE', #41334, .T. ) ;
#64796=LINE ( 'NONE', #20015, #37692 ) ;
#64797=EDGE_CURVE ( 'NONE', #71422, #28318, #55114, .T. ) ;
#64801=AXIS2_PLACEMENT_3D ( 'NONE', #37762, #44517, #60696 ) ;
#64816=DIRECTION ( 'NONE',  ( 0.000000000000000000, 0.000000000000000000, 1.000000000000000000 ) ) ;
#64825=CARTESIAN_POINT ( 'NONE',  ( 15.00000000000000000, 22.07842321921492612, 8.187992925817123790 ) ) ;
#64827=EDGE_LOOP ( 'NONE', ( #27000, #24585, #67686, #66775 ) ) ;
#64832=ORIENTED_EDGE ( 'NONE', *, *, #17384, .T. ) ;
#64836=CARTESIAN_POINT ( 'NONE',  ( 11.99999999999999822, -51.02545421589363883, 55.20638768913742922 ) ) ;
#64839=LINE ( 'NONE', #60318, #1943 ) ;
#64848=DIRECTION ( 'NONE',  ( -1.000000000000000000, -0.000000000000000000, 0.000000000000000000 ) ) ;
#64851=VERTEX_POINT ( 'NONE', #34688 ) ;
#64854=DIRECTION ( 'NONE',  ( 0.000000000000000000, -0.9876883405951359940, -0.1564344650402420545 ) ) ;
#64857=CARTESIAN_POINT ( 'NONE',  ( 15.00000000000000000, -13.04903810567646971, 19.60159698893442481 ) ) ;
#64862=LINE ( 'NONE', #13341, #27558 ) ;
#64875=AXIS2_PLACEMENT_3D ( 'NONE', #45850, #29260, #46942 ) ;
#64876=VECTOR ( 'NONE', #70359, 1000.000000000000000 ) ;
#64882=DIRECTION ( 'NONE',  ( 0.000000000000000000, -0.6494480483301739993, -0.7604059656000390355 ) ) ;
#64885=DIRECTION ( 'NONE',  ( -1.000000000000000000, -0.000000000000000000, -0.000000000000000000 ) ) ;
#64895=CARTESIAN_POINT ( 'NONE',  ( 11.99999999999999822, -44.99326035066006568, -68.55367621811190304 ) ) ;
#64899=ORIENTED_EDGE ( 'NONE', *, *, #70005, .F. ) ;
#64902=CIRCLE ( 'NONE', #25301, 77.49900000000000944 ) ;
#64904=AXIS2_PLACEMENT_3D ( 'NONE', #12616, #2127, #42320 ) ;
#64906=CIRCLE ( 'NONE', #45714, 31.99999999999998579 ) ;
#64918=VECTOR ( 'NONE', #34996, 1000.000000000000000 ) ;
#64925=AXIS2_PLACEMENT_3D ( 'NONE', #57914, #5679, #51895 ) ;
#64927=CIRCLE ( 'NONE', #2552, 31.99999999999998579 ) ;
#64934=EDGE_CURVE ( 'NONE', #60240, #26714, #3513, .T. ) ;
#64939=CARTESIAN_POINT ( 'NONE',  ( 5.999999999999999112, -63.97538442413390669, -51.29473840253292138 ) ) ;
#64940=EDGE_LOOP ( 'NONE', ( #38793, #40832, #40787, #55563 ) ) ;
#64947=DIRECTION ( 'NONE',  ( 0.000000000000000000, -0.7604059656000369261, 0.6494480483301766638 ) ) ;
#64954=DIRECTION ( 'NONE',  ( -1.000000000000000000, 0.000000000000000000, 0.000000000000000000 ) ) ;
#64959=DIRECTION ( 'NONE',  ( -1.000000000000000000, 0.000000000000000000, 0.000000000000000000 ) ) ;
#64963=AXIS2_PLACEMENT_3D ( 'NONE', #59235, #47952, #63779 ) ;
#64964=AXIS2_PLACEMENT_3D ( 'NONE', #19708, #42655, #54672 ) ;
#64967=EDGE_CURVE ( 'NONE', #45508, #7045, #43115, .T. ) ;
#64980=FACE_OUTER_BOUND ( 'NONE', #52929, .T. ) ;
#64992=VECTOR ( 'NONE', #37970, 1000.000000000000000 ) ;
#65001=DIRECTION ( 'NONE',  ( -1.000000000000000000, -0.000000000000000000, -0.000000000000000000 ) ) ;
#65003=ORIENTED_EDGE ( 'NONE', *, *, #60444, .T. ) ;
#65007=EDGE_CURVE ( 'NONE', #36975, #44200, #13963, .T. ) ;
#65009=ORIENTED_EDGE ( 'NONE', *, *, #48624, .T. ) ;
#65014=CIRCLE ( 'NONE', #42215, 82.00000000000000000 ) ;
#65023=ORIENTED_EDGE ( 'NONE', *, *, #50846, .T. ) ;
#65024=DIRECTION ( 'NONE',  ( 0.000000000000000000, 0.000000000000000000, 1.000000000000000000 ) ) ;
#65036=CIRCLE ( 'NONE', #73442, 31.99999999999998579 ) ;
#65037=ORIENTED_EDGE ( 'NONE', *, *, #73513, .F. ) ;
#65038=EDGE_CURVE ( 'NONE', #24628, #53485, #4947, .T. ) ;
#65039=ORIENTED_EDGE ( 'NONE', *, *, #72571, .F. ) ;
#65040=CARTESIAN_POINT ( 'NONE',  ( 12.00000000000000000, -10.45096189432314127, 21.10159698893440350 ) ) ;
#65041=CIRCLE ( 'NONE', #60211, 77.49899999999999523 ) ;
#65048=DIRECTION ( 'NONE',  ( 0.000000000000000000, 0.000000000000000000, -1.000000000000000000 ) ) ;
#65052=VERTEX_POINT ( 'NONE', #27091 ) ;
#65054=CARTESIAN_POINT ( 'NONE',  ( 11.99999999999999822, -59.03342792756231461, -46.54456581323868392 ) ) ;
#65056=CYLINDRICAL_SURFACE ( 'NONE', #2695, 31.99999999999998579 ) ;
#65059=EDGE_CURVE ( 'NONE', #29201, #40792, #33860, .T. ) ;
#65075=DIRECTION ( 'NONE',  ( 0.000000000000000000, 0.000000000000000000, 1.000000000000000000 ) ) ;
#65077=VECTOR ( 'NONE', #25368, 1000.000000000000000 ) ;
#65082=CARTESIAN_POINT ( 'NONE',  ( 11.99999999999999822, -41.76106447765443619, -62.50884508063471401 ) ) ;
#65083=FACE_OUTER_BOUND ( 'NONE', #6507, .T. ) ;
#65085=AXIS2_PLACEMENT_3D ( 'NONE', #56452, #50035, #38033 ) ;
#65086=CIRCLE ( 'NONE', #7492, 31.99999999999998579 ) ;
#65090=CARTESIAN_POINT ( 'NONE',  ( 11.99999999999999822, -73.72996012237449293, 14.67089635893687571 ) ) ;
#65108=CARTESIAN_POINT ( 'NONE',  ( -10.00000000000000000, 0.000000000000000000, 0.000000000000000000 ) ) ;
#65110=EDGE_CURVE ( 'NONE', #10549, #38728, #45155, .T. ) ;
#65115=EDGE_CURVE ( 'NONE', #63637, #21721, #63762, .T. ) ;
#65123=VECTOR ( 'NONE', #62778, 1000.000000000000000 ) ;
#65125=DIRECTION ( 'NONE',  ( -1.000000000000000000, 0.000000000000000000, 0.000000000000000000 ) ) ;
#65145=DIRECTION ( 'NONE',  ( -1.000000000000000000, 0.000000000000000000, -0.000000000000000000 ) ) ;
#65154=CARTESIAN_POINT ( 'NONE',  ( 11.99999999999999822, -71.27951684758045303, 30.41916302227090085 ) ) ;
#65170=EDGE_CURVE ( 'NONE', #17494, #68748, #10182, .T. ) ;
#65172=CARTESIAN_POINT ( 'NONE',  ( 11.99999999999999822, -74.65374052328644439, -8.840884882375878107 ) ) ;
#65173=VERTEX_POINT ( 'NONE', #63561 ) ;
#65175=DIRECTION ( 'NONE',  ( 0.000000000000000000, -0.1045284632676436454, 0.9945218953682744001 ) ) ;
#65180=DIRECTION ( 'NONE',  ( -1.000000000000000000, 0.000000000000000000, -0.000000000000000000 ) ) ;
#65185=CARTESIAN_POINT ( 'NONE',  ( 11.99999999999999822, 20.41045688087930898, -72.35160999960793049 ) ) ;
#65186=ORIENTED_EDGE ( 'NONE', *, *, #8325, .F. ) ;
#65187=EDGE_CURVE ( 'NONE', #53274, #6219, #66168, .T. ) ;
#65188=FACE_OUTER_BOUND ( 'NONE', #30251, .T. ) ;
#65191=CARTESIAN_POINT ( 'NONE',  ( 11.99999999999999822, -44.99326035066103202, 68.55367621811127776 ) ) ;
#65192=CIRCLE ( 'NONE', #36357, 31.99999999999998579 ) ;
#65193=ORIENTED_EDGE ( 'NONE', *, *, #37002, .F. ) ;
#65195=ORIENTED_EDGE ( 'NONE', *, *, #23015, .F. ) ;
#65196=DIRECTION ( 'NONE',  ( 0.000000000000000000, 0.000000000000000000, 1.000000000000000000 ) ) ;
#65197=EDGE_LOOP ( 'NONE', ( #4730, #72862, #72006, #8733 ) ) ;
#65206=DIRECTION ( 'NONE',  ( 0.000000000000000000, -0.2334453638558922350, -0.9723699203976797767 ) ) ;
#65209=DIRECTION ( 'NONE',  ( -1.000000000000000000, -0.000000000000000000, -0.000000000000000000 ) ) ;
#65212=LINE ( 'NONE', #13686, #21032 ) ;
#65219=VECTOR ( 'NONE', #3313, 1000.000000000000000 ) ;
#65225=FACE_OUTER_BOUND ( 'NONE', #62817, .T. ) ;
#65228=CARTESIAN_POINT ( 'NONE',  ( 11.99999999999999822, 0.000000000000000000, 0.000000000000000000 ) ) ;
#65232=CARTESIAN_POINT ( 'NONE',  ( 11.99999999999999822, 0.000000000000000000, 0.000000000000000000 ) ) ;
#65234=AXIS2_PLACEMENT_3D ( 'NONE', #3156, #43373, #60653 ) ;
#65236=DIRECTION ( 'NONE',  ( 0.000000000000000000, 0.000000000000000000, 1.000000000000000000 ) ) ;
#65242=DIRECTION ( 'NONE',  ( -1.000000000000000000, -0.000000000000000000, 0.000000000000000000 ) ) ;
#65255=CYLINDRICAL_SURFACE ( 'NONE', #64963, 31.99999999999998579 ) ;
#65269=ADVANCED_FACE ( 'NONE', ( #40620 ), #63196, .T. ) ;
#65272=ORIENTED_EDGE ( 'NONE', *, *, #73643, .T. ) ;
#65277=ADVANCED_FACE ( 'NONE', ( #46627 ), #52261, .T. ) ;
#65279=CARTESIAN_POINT ( 'NONE',  ( 0.000000000000000000, -76.41127070299280888, 12.93880638057290788 ) ) ;
#65280=ORIENTED_EDGE ( 'NONE', *, *, #1674, .T. ) ;
#65281=CARTESIAN_POINT ( 'NONE',  ( 12.00000000000000000, 6.762365576493647445, 25.66652317338391498 ) ) ;
#65286=FACE_OUTER_BOUND ( 'NONE', #63989, .T. ) ;
#65292=VERTEX_POINT ( 'NONE', #35352 ) ;
#65305=EDGE_CURVE ( 'NONE', #29501, #33770, #47004, .T. ) ;
#65309=ORIENTED_EDGE ( 'NONE', *, *, #64446, .F. ) ;
#65314=CIRCLE ( 'NONE', #28052, 31.99999999999998934 ) ;
#65317=CARTESIAN_POINT ( 'NONE',  ( 11.99999999999999822, 46.21855187248630870, 62.20884554314035597 ) ) ;
#65319=CARTESIAN_POINT ( 'NONE',  ( 11.99999999999999822, 31.46837873495072913, -68.27212725128242710 ) ) ;
#65320=CARTESIAN_POINT ( 'NONE',  ( 15.00000000000000000, -3.948201729842032215, 23.21447184625297666 ) ) ;
#65321=ORIENTED_EDGE ( 'NONE', *, *, #35471, .T. ) ;
#65322=ORIENTED_EDGE ( 'NONE', *, *, #23089, .T. ) ;
#65324=CARTESIAN_POINT ( 'NONE',  ( 11.99999999999999822, -62.20884554314051229, 46.21855187248609553 ) ) ;
#65331=ORIENTED_EDGE ( 'NONE', *, *, #58058, .T. ) ;
#65340=CYLINDRICAL_SURFACE ( 'NONE', #26746, 77.49899999999999523 ) ;
#65342=CARTESIAN_POINT ( 'NONE',  ( 11.99999999999999822, -66.50666863322028632, 39.78640506895582973 ) ) ;
#65350=AXIS2_PLACEMENT_3D ( 'NONE', #11507, #34439, #28808 ) ;
#65355=EDGE_CURVE ( 'NONE', #5291, #30315, #8989, .T. ) ;
#65358=ORIENTED_EDGE ( 'NONE', *, *, #29092, .T. ) ;
#65374=ORIENTED_EDGE ( 'NONE', *, *, #66532, .T. ) ;
#65378=ORIENTED_EDGE ( 'NONE', *, *, #16028, .T. ) ;
#65392=ORIENTED_EDGE ( 'NONE', *, *, #64967, .T. ) ;
#65395=AXIS2_PLACEMENT_3D ( 'NONE', #29364, #16994, #63236 ) ;
#65396=ADVANCED_FACE ( 'NONE', ( #8243 ), #70642, .T. ) ;
#65406=ORIENTED_EDGE ( 'NONE', *, *, #45168, .F. ) ;
#65418=DIRECTION ( 'NONE',  ( 0.000000000000000000, 0.000000000000000000, 1.000000000000000000 ) ) ;
#65421=CARTESIAN_POINT ( 'NONE',  ( 0.000000000000000000, -72.35432306680469594, -20.40083707022958848 ) ) ;
#65439=DIRECTION ( 'NONE',  ( -1.000000000000000000, 0.000000000000000000, -0.000000000000000000 ) ) ;
#65442=CARTESIAN_POINT ( 'NONE',  ( 11.99999999999999822, 23.16143007188426850, 73.95703589263983702 ) ) ;
#65443=EDGE_CURVE ( 'NONE', #67992, #15234, #64927, .T. ) ;
#65452=CARTESIAN_POINT ( 'NONE',  ( 15.00000000000000000, 16.83928648764922542, -16.46020748918050458 ) ) ;
#65453=DIRECTION ( 'NONE',  ( 1.000000000000000000, 0.000000000000000000, -0.000000000000000000 ) ) ;
#65455=CARTESIAN_POINT ( 'NONE',  ( 6.000000000000000000, 34.94270380257639630, 74.18225833017899618 ) ) ;
#65456=AXIS2_PLACEMENT_3D ( 'NONE', #12355, #50069, #10598 ) ;
#65465=AXIS2_PLACEMENT_3D ( 'NONE', #34051, #53197, #52443 ) ;
#65469=EDGE_LOOP ( 'NONE', ( #71451, #33376, #72450, #17112 ) ) ;
#65473=VERTEX_POINT ( 'NONE', #61991 ) ;
#65475=ORIENTED_EDGE ( 'NONE', *, *, #48775, .F. ) ;
#65476=CARTESIAN_POINT ( 'NONE',  ( 11.99999999999999822, 71.87247863392470038, -39.47590169984768949 ) ) ;
#65479=ORIENTED_EDGE ( 'NONE', *, *, #14839, .T. ) ;
#65482=VERTEX_POINT ( 'NONE', #68380 ) ;
#65485=ORIENTED_EDGE ( 'NONE', *, *, #59405, .F. ) ;
#65491=VERTEX_POINT ( 'NONE', #16869 ) ;
#65503=FACE_OUTER_BOUND ( 'NONE', #28920, .T. ) ;
#65508=DIRECTION ( 'NONE',  ( 0.000000000000000000, 0.000000000000000000, 1.000000000000000000 ) ) ;
#65512=LINE ( 'NONE', #3844, #66066 ) ;
#65513=ORIENTED_EDGE ( 'NONE', *, *, #35735, .T. ) ;
#65521=CIRCLE ( 'NONE', #58315, 77.49899999999999523 ) ;
#65522=DIRECTION ( 'NONE',  ( -0.000000000000000000, -2.312964634635746211E-15, 1.000000000000000000 ) ) ;
#65527=CARTESIAN_POINT ( 'NONE',  ( 12.00000000000000000, -0.9646360437375368635, -23.52805723605589705 ) ) ;
#65529=EDGE_CURVE ( 'NONE', #1257, #55684, #15704, .T. ) ;
#65538=CARTESIAN_POINT ( 'NONE',  ( 0.000000000000000000, -55.16347631942998220, -60.67117009219196433 ) ) ;
#65556=AXIS2_PLACEMENT_3D ( 'NONE', #29860, #34397, #6934 ) ;
#65564=CARTESIAN_POINT ( 'NONE',  ( 15.00000000000000000, 8.688484142253932063, -21.88630264137371029 ) ) ;
#65565=ORIENTED_EDGE ( 'NONE', *, *, #17803, .F. ) ;
#65569=EDGE_LOOP ( 'NONE', ( #58243, #28380, #65193, #14913 ) ) ;
#65572=CARTESIAN_POINT ( 'NONE',  ( 11.99999999999999822, 20.40083707022987625, -72.35432306680462489 ) ) ;
#65573=ORIENTED_EDGE ( 'NONE', *, *, #48535, .T. ) ;
#65574=EDGE_LOOP ( 'NONE', ( #60108, #32871, #43400, #8974 ) ) ;
#65576=CARTESIAN_POINT ( 'NONE',  ( 0.000000000000000000, -17.28742895386031719, -75.54627589209962935 ) ) ;
#65584=DIRECTION ( 'NONE',  ( 0.000000000000000000, 0.000000000000000000, -1.000000000000000000 ) ) ;
#65592=CYLINDRICAL_SURFACE ( 'NONE', #34948, 82.00000000000000000 ) ;
#65593=LINE ( 'NONE', #30613, #24703 ) ;
#65596=DIRECTION ( 'NONE',  ( 0.000000000000000000, 0.9510565162951521989, 0.3090169943749515591 ) ) ;
#65601=EDGE_LOOP ( 'NONE', ( #71271, #28212, #5483, #60613 ) ) ;
#65606=EDGE_CURVE ( 'NONE', #40982, #19944, #7349, .T. ) ;
#65609=CARTESIAN_POINT ( 'NONE',  ( 12.00000000000000355, 0.000000000000000000, 0.000000000000000000 ) ) ;
#65610=AXIS2_PLACEMENT_3D ( 'NONE', #73340, #55693, #27100 ) ;
#65615=CYLINDRICAL_SURFACE ( 'NONE', #1026, 31.99999999999998579 ) ;
#65626=ADVANCED_FACE ( 'NONE', ( #46541 ), #52924, .T. ) ;
#65634=AXIS2_PLACEMENT_3D ( 'NONE', #29645, #1141, #53335 ) ;
#65644=DIRECTION ( 'NONE',  ( -1.000000000000000000, -0.000000000000000000, 0.000000000000000000 ) ) ;
#65649=CARTESIAN_POINT ( 'NONE',  ( 11.99999999999999822, 69.42325613327440692, 34.44570377933622041 ) ) ;
#65660=VECTOR ( 'NONE', #19256, 1000.000000000000000 ) ;
#65670=VECTOR ( 'NONE', #20664, 999.9999999999998863 ) ;
#65681=DIRECTION ( 'NONE',  ( -1.000000000000000000, -0.000000000000000000, 0.000000000000000000 ) ) ;
#65696=ADVANCED_FACE ( 'NONE', ( #6689, #34148, #28495, #63476, #29595, #51434, #40166, #17599, #17968, #12447, #22888, #63121, #45825, #68747, #34510, #51813, #57458 ), #23249, .F. ) ;
#65703=DIRECTION ( 'NONE',  ( 0.000000000000000000, -1.000000000000000000, -1.040834085586084730E-14 ) ) ;
#65707=CARTESIAN_POINT ( 'NONE',  ( 0.000000000000000000, 51.29473840253317007, -63.97538442413369353 ) ) ;
#65711=VECTOR ( 'NONE', #10022, 1000.000000000000000 ) ;
#65721=EDGE_CURVE ( 'NONE', #54492, #70171, #62629, .T. ) ;
#65726=DIRECTION ( 'NONE',  ( 0.000000000000000000, 0.000000000000000000, 1.000000000000000000 ) ) ;
#65728=VERTEX_POINT ( 'NONE', #14165 ) ;
#65730=AXIS2_PLACEMENT_3D ( 'NONE', #30777, #54109, #42452 ) ;
#65732=FACE_OUTER_BOUND ( 'NONE', #29555, .T. ) ;
#65733=CYLINDRICAL_SURFACE ( 'NONE', #52009, 31.99999999999998579 ) ;
#65739=VERTEX_POINT ( 'NONE', #36361 ) ;
#65741=CARTESIAN_POINT ( 'NONE',  ( 11.99999999999999822, 71.27951684758069462, -30.41916302227037150 ) ) ;
#65745=CARTESIAN_POINT ( 'NONE',  ( 11.99999999999999822, 0.000000000000000000, 0.000000000000000000 ) ) ;
#65766=CYLINDRICAL_SURFACE ( 'NONE', #19348, 31.99999999999998579 ) ;
#65771=EDGE_LOOP ( 'NONE', ( #65280, #48370, #6950, #23235 ) ) ;
#65775=CYLINDRICAL_SURFACE ( 'NONE', #70781, 82.00000000000000000 ) ;
#65780=DIRECTION ( 'NONE',  ( -1.000000000000000000, 0.000000000000000000, 0.000000000000000000 ) ) ;
#65781=CARTESIAN_POINT ( 'NONE',  ( 11.99999999999999822, -54.21277698773713638, 55.38113227695764351 ) ) ;
#65784=AXIS2_PLACEMENT_3D ( 'NONE', #39305, #26892, #49820 ) ;
#65790=CARTESIAN_POINT ( 'NONE',  ( 11.99999999999999822, -55.38113227695745167, -54.21277698773732823 ) ) ;
#65796=ADVANCED_FACE ( 'NONE', ( #35992 ), #25459, .T. ) ;
#65799=EDGE_CURVE ( 'NONE', #28741, #8298, #32540, .T. ) ;
#65800=CARTESIAN_POINT ( 'NONE',  ( 11.99999999999999822, 67.80270845531956070, -46.11716303203111522 ) ) ;
#65803=CARTESIAN_POINT ( 'NONE',  ( 11.99999999999999822, -66.50666863321974631, -39.78640506895675344 ) ) ;
#65809=ADVANCED_FACE ( 'NONE', ( #53290 ), #1828, .T. ) ;
#65814=CARTESIAN_POINT ( 'NONE',  ( 11.99999999999999822, -58.39081064771786345, 50.95692526931308919 ) ) ;
#65819=AXIS2_PLACEMENT_3D ( 'NONE', #9859, #43358, #32774 ) ;
#65820=ORIENTED_EDGE ( 'NONE', *, *, #46851, .T. ) ;
#65823=ORIENTED_EDGE ( 'NONE', *, *, #40768, .T. ) ;
#65828=ORIENTED_EDGE ( 'NONE', *, *, #17176, .F. ) ;
#65830=ORIENTED_EDGE ( 'NONE', *, *, #53238, .T. ) ;
#65833=ORIENTED_EDGE ( 'NONE', *, *, #74204, .F. ) ;
#65835=AXIS2_PLACEMENT_3D ( 'NONE', #45349, #44971, #4019 ) ;
#65837=AXIS2_PLACEMENT_3D ( 'NONE', #22277, #15140, #61013 ) ;
#65843=DIRECTION ( 'NONE',  ( 0.000000000000000000, 0.000000000000000000, 1.000000000000000000 ) ) ;
#65850=ORIENTED_EDGE ( 'NONE', *, *, #21450, .T. ) ;
#65852=CARTESIAN_POINT ( 'NONE',  ( 12.00000000000000000, -0.9646360437372099028, 23.52805723605590771 ) ) ;
#65855=EDGE_CURVE ( 'NONE', #27913, #28647, #51764, .T. ) ;
#65858=FACE_OUTER_BOUND ( 'NONE', #55348, .T. ) ;
#65864=CARTESIAN_POINT ( 'NONE',  ( 12.00000000000000000, 9.615535125378766423, -24.73947219025917121 ) ) ;
#65879=AXIS2_PLACEMENT_3D ( 'NONE', #16983, #6446, #52295 ) ;
#65881=DIRECTION ( 'NONE',  ( -1.000000000000000000, 0.000000000000000000, 0.000000000000000000 ) ) ;
#65896=ADVANCED_FACE ( 'NONE', ( #68931 ), #11402, .T. ) ;
#65898=AXIS2_PLACEMENT_3D ( 'NONE', #55813, #66724, #32121 ) ;
#65910=LINE ( 'NONE', #31302, #50930 ) ;
#65916=EDGE_LOOP ( 'NONE', ( #14324, #60837, #25440, #21129 ) ) ;
#65919=FACE_OUTER_BOUND ( 'NONE', #39372, .T. ) ;
#65926=AXIS2_PLACEMENT_3D ( 'NONE', #35869, #41893, #43012 ) ;
#65927=CARTESIAN_POINT ( 'NONE',  ( 6.000000000000000000, -80.28980883073769803, 16.65972982744905551 ) ) ;
#65933=ORIENTED_EDGE ( 'NONE', *, *, #45546, .F. ) ;
#65936=ORIENTED_EDGE ( 'NONE', *, *, #73736, .T. ) ;
#65941=LINE ( 'NONE', #37736, #56401 ) ;
#65942=CARTESIAN_POINT ( 'NONE',  ( 0.000000000000000000, 2.571758278209441661E-15, -21.00000000000000000 ) ) ;
#65948=CARTESIAN_POINT ( 'NONE',  ( 15.00000000000000000, -23.29833615347109088, -3.418703333116486665 ) ) ;
#65949=ORIENTED_EDGE ( 'NONE', *, *, #21666, .F. ) ;
#65954=EDGE_CURVE ( 'NONE', #11454, #18706, #65521, .T. ) ;
#65957=CARTESIAN_POINT ( 'NONE',  ( 11.99999999999999822, 46.21855187248719687, -62.20884554313968806 ) ) ;
#65962=VECTOR ( 'NONE', #51473, 1000.000000000000000 ) ;
#65966=ORIENTED_EDGE ( 'NONE', *, *, #63922, .F. ) ;
#65970=ORIENTED_EDGE ( 'NONE', *, *, #4681, .F. ) ;
#65972=DIRECTION ( 'NONE',  ( -1.000000000000000000, -0.000000000000000000, 0.000000000000000000 ) ) ;
#65976=DIRECTION ( 'NONE',  ( 0.000000000000000000, 0.000000000000000000, 1.000000000000000000 ) ) ;
#65991=CIRCLE ( 'NONE', #43179, 31.99999999999999289 ) ;
#65996=DIRECTION ( 'NONE',  ( -1.000000000000000000, -0.000000000000000000, 0.000000000000000000 ) ) ;
#66003=CARTESIAN_POINT ( 'NONE',  ( 6.000000000000000000, 2.543863470249533965, -81.96053171279901051 ) ) ;
#66010=CARTESIAN_POINT ( 'NONE',  ( 15.00000000000000000, -26.23277895567245466, 4.042438405570107918 ) ) ;
#66021=VERTEX_POINT ( 'NONE', #45263 ) ;
#66029=CARTESIAN_POINT ( 'NONE',  ( 11.99999999999999822, -74.65491531819111515, 23.16904090965678265 ) ) ;
#66032=AXIS2_PLACEMENT_3D ( 'NONE', #25728, #4672, #21942 ) ;
#66034=EDGE_LOOP ( 'NONE', ( #30400, #14354, #10176, #17305 ) ) ;
#66038=ORIENTED_EDGE ( 'NONE', *, *, #33885, .T. ) ;
#66044=FACE_OUTER_BOUND ( 'NONE', #52487, .T. ) ;
#66046=EDGE_CURVE ( 'NONE', #22373, #8165, #28307, .T. ) ;
#66047=ORIENTED_EDGE ( 'NONE', *, *, #43833, .T. ) ;
#66061=LINE ( 'NONE', #42743, #10870 ) ;
#66062=EDGE_LOOP ( 'NONE', ( #6018, #17014, #17575, #65378 ) ) ;
#66066=VECTOR ( 'NONE', #54590, 1000.000000000000000 ) ;
#66068=ORIENTED_EDGE ( 'NONE', *, *, #16366, .T. ) ;
#66070=DIRECTION ( 'NONE',  ( -1.000000000000000000, -0.000000000000000000, 0.000000000000000000 ) ) ;
#66071=AXIS2_PLACEMENT_3D ( 'NONE', #61321, #55667, #27834 ) ;
#66073=EDGE_CURVE ( 'NONE', #67235, #50834, #58377, .T. ) ;
#66078=ORIENTED_EDGE ( 'NONE', *, *, #34734, .T. ) ;
#66084=CARTESIAN_POINT ( 'NONE',  ( -10.00000000000000000, 0.000000000000000000, 0.000000000000000000 ) ) ;
#66091=DIRECTION ( 'NONE',  ( -1.000000000000000000, 0.000000000000000000, -0.000000000000000000 ) ) ;
#66099=AXIS2_PLACEMENT_3D ( 'NONE', #18686, #13047, #69106 ) ;
#66105=EDGE_CURVE ( 'NONE', #27755, #19421, #6693, .T. ) ;
#66106=AXIS2_PLACEMENT_3D ( 'NONE', #45365, #32934, #62664 ) ;
#66107=AXIS2_PLACEMENT_3D ( 'NONE', #1998, #2742, #36905 ) ;
#66111=ORIENTED_EDGE ( 'NONE', *, *, #71864, .F. ) ;
#66119=ADVANCED_FACE ( 'NONE', ( #2392 ), #12872, .T. ) ;
#66123=ORIENTED_EDGE ( 'NONE', *, *, #41830, .T. ) ;
#66132=CARTESIAN_POINT ( 'NONE',  ( 6.000000000000000000, -74.18225833017913828, 34.94270380257611208 ) ) ;
#66139=ORIENTED_EDGE ( 'NONE', *, *, #4186, .T. ) ;
#66149=DIRECTION ( 'NONE',  ( 0.000000000000000000, 0.000000000000000000, 1.000000000000000000 ) ) ;
#66160=VERTEX_POINT ( 'NONE', #29790 ) ;
#66161=ADVANCED_FACE ( 'NONE', ( #64401 ), #52742, .T. ) ;
#66168=CIRCLE ( 'NONE', #33735, 31.99999999999998934 ) ;
#66172=AXIS2_PLACEMENT_3D ( 'NONE', #73644, #2777, #54610 ) ;
#66176=DIRECTION ( 'NONE',  ( 0.000000000000000000, 0.9723699203976773342, -0.2334453638559024491 ) ) ;
#66180=CARTESIAN_POINT ( 'NONE',  ( 0.000000000000000000, -55.38113227695820484, 54.21277698773656084 ) ) ;
#66181=CARTESIAN_POINT ( 'NONE',  ( 12.00000000000000000, -18.13022148937242761, 15.02647892043569122 ) ) ;
#66182=LINE ( 'NONE', #51751, #26851 ) ;
#66196=EDGE_LOOP ( 'NONE', ( #18826, #16176, #31024, #20783 ) ) ;
#66198=EDGE_CURVE ( 'NONE', #14207, #22781, #37313, .T. ) ;
#66208=VERTEX_POINT ( 'NONE', #26008 ) ;
#66210=ORIENTED_EDGE ( 'NONE', *, *, #28400, .T. ) ;
#66221=CARTESIAN_POINT ( 'NONE',  ( 11.99999999999999822, 34.94270380257741238, -74.18225833017854143 ) ) ;
#66222=ORIENTED_EDGE ( 'NONE', *, *, #55327, .F. ) ;
#66223=LINE ( 'NONE', #13946, #97 ) ;
#66234=DIRECTION ( 'NONE',  ( -1.000000000000000000, 0.000000000000000000, -0.000000000000000000 ) ) ;
#66243=ORIENTED_EDGE ( 'NONE', *, *, #16617, .F. ) ;
#66245=LINE ( 'NONE', #61342, #41989 ) ;
#66260=VECTOR ( 'NONE', #46083, 1000.000000000000000 ) ;
#66263=DIRECTION ( 'NONE',  ( 0.000000000000000000, 0.000000000000000000, -1.000000000000000000 ) ) ;
#66269=CARTESIAN_POINT ( 'NONE',  ( 11.99999999999999822, 69.42325613327489009, -34.44570377933524696 ) ) ;
#66271=CARTESIAN_POINT ( 'NONE',  ( 11.99999999999999822, 73.44644590900094272, -24.73286445877629802 ) ) ;
#66274=DIRECTION ( 'NONE',  ( -1.000000000000000000, -0.000000000000000000, -0.000000000000000000 ) ) ;
#66276=CIRCLE ( 'NONE', #72261, 31.99999999999998579 ) ;
#66278=EDGE_CURVE ( 'NONE', #42793, #2723, #26741, .T. ) ;
#66281=DIRECTION ( 'NONE',  ( -1.000000000000000000, 0.000000000000000000, -0.000000000000000000 ) ) ;
#66291=DIRECTION ( 'NONE',  ( -1.000000000000000000, 0.000000000000000000, 0.000000000000000000 ) ) ;
#66300=AXIS2_PLACEMENT_3D ( 'NONE', #42042, #25110, #13081 ) ;
#66309=CIRCLE ( 'NONE', #7480, 31.99999999999999645 ) ;
#66325=LINE ( 'NONE', #36993, #10268 ) ;
#66327=LINE ( 'NONE', #37385, #40130 ) ;
#66329=LINE ( 'NONE', #8053, #46844 ) ;
#66341=DIRECTION ( 'NONE',  ( 0.000000000000000000, -0.9781476007338043566, 0.2079116908177651712 ) ) ;
#66343=DIRECTION ( 'NONE',  ( -1.000000000000000000, 0.000000000000000000, 0.000000000000000000 ) ) ;
#66349=ORIENTED_EDGE ( 'NONE', *, *, #3779, .F. ) ;
#66373=ORIENTED_EDGE ( 'NONE', *, *, #2981, .T. ) ;
#66376=EDGE_CURVE ( 'NONE', #54478, #23480, #45124, .T. ) ;
#66385=CARTESIAN_POINT ( 'NONE',  ( 15.00000000000000000, 5.835314593368470248, -22.81335362449854642 ) ) ;
#66388=ORIENTED_EDGE ( 'NONE', *, *, #54836, .F. ) ;
#66407=EDGE_CURVE ( 'NONE', #56025, #32525, #66795, .T. ) ;
#66410=CARTESIAN_POINT ( 'NONE',  ( 6.000000000000000000, 21.60688246758586928, 79.10210256391376049 ) ) ;
#66427=DIRECTION ( 'NONE',  ( 1.000000000000000000, 0.000000000000000000, 0.000000000000000000 ) ) ;
#66431=LINE ( 'NONE', #72771, #67175 ) ;
#66432=VERTEX_POINT ( 'NONE', #45555 ) ;
#66445=DIRECTION ( 'NONE',  ( 0.000000000000000000, 0.000000000000000000, 1.000000000000000000 ) ) ;
#66446=CARTESIAN_POINT ( 'NONE',  ( 15.00000000000000000, -19.89357724624986545, 12.59942793731086219 ) ) ;
#66455=ORIENTED_EDGE ( 'NONE', *, *, #20965, .T. ) ;
#66457=FACE_OUTER_BOUND ( 'NONE', #4084, .T. ) ;
#66462=ORIENTED_EDGE ( 'NONE', *, *, #4294, .F. ) ;
#66468=ADVANCED_FACE ( 'NONE', ( #38778 ), #33490, .T. ) ;
#66474=ORIENTED_EDGE ( 'NONE', *, *, #61283, .F. ) ;
#66486=VERTEX_POINT ( 'NONE', #11672 ) ;
#66488=EDGE_CURVE ( 'NONE', #68607, #52228, #22229, .T. ) ;
#66493=DIRECTION ( 'NONE',  ( 0.000000000000000000, -0.7604059656000227152, -0.6494480483301933171 ) ) ;
#66496=VERTEX_POINT ( 'NONE', #56823 ) ;
#66499=CIRCLE ( 'NONE', #17279, 82.00000000000000000 ) ;
#66506=DIRECTION ( 'NONE',  ( 0.000000000000000000, 0.000000000000000000, 1.000000000000000000 ) ) ;
#66508=DIRECTION ( 'NONE',  ( 1.000000000000000000, 0.000000000000000000, 0.000000000000000000 ) ) ;
#66511=EDGE_LOOP ( 'NONE', ( #72224, #65966, #46652, #39097 ) ) ;
#66515=DIRECTION ( 'NONE',  ( 0.000000000000000000, -0.7604059656000369261, 0.6494480483301766638 ) ) ;
#66518=ORIENTED_EDGE ( 'NONE', *, *, #57404, .T. ) ;
#66523=CARTESIAN_POINT ( 'NONE',  ( 11.99999999999999822, 0.000000000000000000, 0.000000000000000000 ) ) ;
#66525=CARTESIAN_POINT ( 'NONE',  ( 11.99999999999999822, 21.60688246758696351, -79.10210256391344785 ) ) ;
#66528=AXIS2_PLACEMENT_3D ( 'NONE', #46849, #41204, #12615 ) ;
#66529=AXIS2_PLACEMENT_3D ( 'NONE', #23363, #45934, #28988 ) ;
#66532=EDGE_CURVE ( 'NONE', #57513, #47511, #50419, .T. ) ;
#66539=CYLINDRICAL_SURFACE ( 'NONE', #31457, 77.49899999999999523 ) ;
#66541=LINE ( 'NONE', #20667, #42751 ) ;
#66542=DIRECTION ( 'NONE',  ( -1.000000000000000000, -0.000000000000000000, 0.000000000000000000 ) ) ;
#66552=EDGE_CURVE ( 'NONE', #23772, #55755, #13914, .T. ) ;
#66553=CARTESIAN_POINT ( 'NONE',  ( 15.00000000000000000, -23.29833615347109088, -3.418703333116486665 ) ) ;
#66554=DIRECTION ( 'NONE',  ( -1.000000000000000000, -0.000000000000000000, -0.000000000000000000 ) ) ;
#66558=VERTEX_POINT ( 'NONE', #41732 ) ;
#66561=DIRECTION ( 'NONE',  ( 0.000000000000000000, -0.3090169943749549453, 0.9510565162951511997 ) ) ;
#66563=CARTESIAN_POINT ( 'NONE',  ( 11.99999999999999822, 0.000000000000000000, 0.000000000000000000 ) ) ;
#66574=AXIS2_PLACEMENT_3D ( 'NONE', #17628, #22538, #11249 ) ;
#66576=VERTEX_POINT ( 'NONE', #7531 ) ;
#66582=DIRECTION ( 'NONE',  ( -1.000000000000000000, 0.000000000000000000, 0.000000000000000000 ) ) ;
#66584=FACE_OUTER_BOUND ( 'NONE', #67033, .T. ) ;
#66595=ORIENTED_EDGE ( 'NONE', *, *, #6248, .F. ) ;
#66596=ORIENTED_EDGE ( 'NONE', *, *, #62343, .F. ) ;
#66608=CARTESIAN_POINT ( 'NONE',  ( 12.00000000000000000, 14.60985201121729737, 18.46759930825687235 ) ) ;
#66611=DIRECTION ( 'NONE',  ( -1.000000000000000000, 0.000000000000000000, -0.000000000000000000 ) ) ;
#66612=DIRECTION ( 'NONE',  ( 0.000000000000000000, 0.5224985647159441360, 0.8526401643540951758 ) ) ;
#66613=ORIENTED_EDGE ( 'NONE', *, *, #40085, .F. ) ;
#66615=ORIENTED_EDGE ( 'NONE', *, *, #1654, .T. ) ;
#66618=CARTESIAN_POINT ( 'NONE',  ( 6.000000000000000000, -40.65526001592564853, -71.21200624218839437 ) ) ;
#66627=CARTESIAN_POINT ( 'NONE',  ( 11.99999999999999822, 26.01480285779837232, 70.53064760720326376 ) ) ;
#66628=EDGE_CURVE ( 'NONE', #28475, #31156, #23707, .T. ) ;
#66632=CYLINDRICAL_SURFACE ( 'NONE', #44163, 82.00000000000000000 ) ;
#66639=DIRECTION ( 'NONE',  ( -1.000000000000000000, 0.000000000000000000, 0.000000000000000000 ) ) ;
#66641=CARTESIAN_POINT ( 'NONE',  ( -10.00000000000000000, 0.000000000000000000, 0.000000000000000000 ) ) ;
#66643=ORIENTED_EDGE ( 'NONE', *, *, #52044, .T. ) ;
#66650=EDGE_CURVE ( 'NONE', #7440, #46823, #15152, .T. ) ;
#66654=FACE_OUTER_BOUND ( 'NONE', #7996, .T. ) ;
#66655=CYLINDRICAL_SURFACE ( 'NONE', #37539, 31.99999999999998579 ) ;
#66657=ORIENTED_EDGE ( 'NONE', *, *, #21907, .F. ) ;
#66664=ORIENTED_EDGE ( 'NONE', *, *, #51288, .F. ) ;
#66665=CARTESIAN_POINT ( 'NONE',  ( 11.99999999999999822, 2.956366410620650420, 75.11725578898469280 ) ) ;
#66671=VECTOR ( 'NONE', #7512, 999.9999999999998863 ) ;
#66674=ORIENTED_EDGE ( 'NONE', *, *, #18832, .T. ) ;
#66681=CYLINDRICAL_SURFACE ( 'NONE', #595, 77.49899999999999523 ) ;
#66682=DIRECTION ( 'NONE',  ( -1.000000000000000000, 0.000000000000000000, 0.000000000000000000 ) ) ;
#66699=CARTESIAN_POINT ( 'NONE',  ( -10.00000000000000000, 0.000000000000000000, 0.000000000000000000 ) ) ;
#66705=AXIS2_PLACEMENT_3D ( 'NONE', #65185, #1331, #24578 ) ;
#66706=ORIENTED_EDGE ( 'NONE', *, *, #4707, .T. ) ;
#66723=FACE_OUTER_BOUND ( 'NONE', #3263, .T. ) ;
#66724=DIRECTION ( 'NONE',  ( -1.000000000000000000, 0.000000000000000000, 0.000000000000000000 ) ) ;
#66726=DIRECTION ( 'NONE',  ( 0.000000000000000000, 0.000000000000000000, 1.000000000000000000 ) ) ;
#66733=EDGE_LOOP ( 'NONE', ( #20168, #325, #21891, #16074 ) ) ;
#66744=EDGE_CURVE ( 'NONE', #29501, #65482, #12736, .T. ) ;
#66749=AXIS2_PLACEMENT_3D ( 'NONE', #45953, #62887, #46311 ) ;
#66755=DIRECTION ( 'NONE',  ( 1.000000000000000000, 0.000000000000000000, 0.000000000000000000 ) ) ;
#66766=FACE_OUTER_BOUND ( 'NONE', #66803, .T. ) ;
#66767=DIRECTION ( 'NONE',  ( 0.000000000000000000, 0.9510565162951523099, 0.3090169943749516146 ) ) ;
#66768=CARTESIAN_POINT ( 'NONE',  ( 11.99999999999999822, -16.65972982744991171, 80.28980883073751329 ) ) ;
#66775=ORIENTED_EDGE ( 'NONE', *, *, #20697, .T. ) ;
#66785=CYLINDRICAL_SURFACE ( 'NONE', #68376, 77.49899999999999523 ) ;
#66786=ORIENTED_EDGE ( 'NONE', *, *, #29457, .F. ) ;
#66795=CIRCLE ( 'NONE', #45183, 31.99999999999998579 ) ;
#66803=EDGE_LOOP ( 'NONE', ( #43221, #6144, #61775, #63337 ) ) ;
#66807=VECTOR ( 'NONE', #54088, 1000.000000000000000 ) ;
#66808=DIRECTION ( 'NONE',  ( -1.000000000000000000, 0.000000000000000000, 0.000000000000000000 ) ) ;
#66822=EDGE_CURVE ( 'NONE', #54007, #35131, #46405, .T. ) ;
#66828=CARTESIAN_POINT ( 'NONE',  ( 15.00000000000000000, -0.9646360437372099028, 23.52805723605590771 ) ) ;
#66830=CYLINDRICAL_SURFACE ( 'NONE', #31192, 31.99999999999998579 ) ;
#66834=CIRCLE ( 'NONE', #2051, 31.99999999999998579 ) ;
#66838=DIRECTION ( 'NONE',  ( -1.000000000000000000, 0.000000000000000000, 0.000000000000000000 ) ) ;
#66842=DIRECTION ( 'NONE',  ( 0.000000000000000000, 0.2334453638558989796, 0.9723699203976782224 ) ) ;
#66845=ORIENTED_EDGE ( 'NONE', *, *, #28802, .T. ) ;
#66852=CARTESIAN_POINT ( 'NONE',  ( 15.00000000000000000, -18.13022148937242761, 15.02647892043569122 ) ) ;
#66859=ORIENTED_EDGE ( 'NONE', *, *, #11148, .T. ) ;
#66866=CYLINDRICAL_SURFACE ( 'NONE', #3319, 82.00000000000000000 ) ;
#66869=ORIENTED_EDGE ( 'NONE', *, *, #47644, .F. ) ;
#66878=EDGE_CURVE ( 'NONE', #69865, #590, #31843, .T. ) ;
#66880=DIRECTION ( 'NONE',  ( 1.000000000000000000, 0.000000000000000000, 0.000000000000000000 ) ) ;
#66881=AXIS2_PLACEMENT_3D ( 'NONE', #20273, #70653, #36456 ) ;
#66882=DIRECTION ( 'NONE',  ( -1.000000000000000000, 0.000000000000000000, 0.000000000000000000 ) ) ;
#66885=AXIS2_PLACEMENT_3D ( 'NONE', #10848, #49568, #61986 ) ;
#66889=CIRCLE ( 'NONE', #64488, 77.49899999999999523 ) ;
#66890=CARTESIAN_POINT ( 'NONE',  ( 0.000000000000000000, 0.000000000000000000, 0.000000000000000000 ) ) ;
#66891=DIRECTION ( 'NONE',  ( -1.000000000000000000, -0.000000000000000000, 0.000000000000000000 ) ) ;
#66892=CARTESIAN_POINT ( 'NONE',  ( 0.000000000000000000, -6.903761155838323837, 77.19088730480521576 ) ) ;
#66897=DIRECTION ( 'NONE',  ( 0.000000000000000000, -0.9238795325112822976, -0.3826834323651006620 ) ) ;
#66903=ADVANCED_FACE ( 'NONE', ( #50707 ), #28510, .F. ) ;
#66908=DIRECTION ( 'NONE',  ( 0.000000000000000000, -0.9723699203976740035, -0.2334453638559160216 ) ) ;
#66916=EDGE_LOOP ( 'NONE', ( #45792, #23046, #5481, #10322 ) ) ;
#66929=ORIENTED_EDGE ( 'NONE', *, *, #67635, .F. ) ;
#66932=VERTEX_POINT ( 'NONE', #22900 ) ;
#66935=VERTEX_POINT ( 'NONE', #33400 ) ;
#66942=VERTEX_POINT ( 'NONE', #62004 ) ;
#66943=EDGE_LOOP ( 'NONE', ( #34970, #29743, #40518, #16469 ) ) ;
#66946=CARTESIAN_POINT ( 'NONE',  ( 0.000000000000000000, -75.11764819372145041, -2.946379043147127064 ) ) ;
#66950=ORIENTED_EDGE ( 'NONE', *, *, #73580, .F. ) ;
#66956=ORIENTED_EDGE ( 'NONE', *, *, #1685, .T. ) ;
#66974=EDGE_CURVE ( 'NONE', #19944, #28475, #41464, .T. ) ;
#66976=EDGE_CURVE ( 'NONE', #7335, #37614, #33036, .T. ) ;
#66987=CIRCLE ( 'NONE', #21358, 77.49899999999999523 ) ;
#66994=CYLINDRICAL_SURFACE ( 'NONE', #10667, 82.00000000000000000 ) ;
#67003=DIRECTION ( 'NONE',  ( -1.000000000000000000, 0.000000000000000000, -0.000000000000000000 ) ) ;
#67010=DIRECTION ( 'NONE',  ( 1.000000000000000000, -0.000000000000000000, -0.000000000000000000 ) ) ;
#67015=ORIENTED_EDGE ( 'NONE', *, *, #41746, .T. ) ;
#67022=EDGE_CURVE ( 'NONE', #32475, #4971, #46239, .T. ) ;
#67028=CARTESIAN_POINT ( 'NONE',  ( -10.00000000000000000, 0.000000000000000000, 0.000000000000000000 ) ) ;
#67031=AXIS2_PLACEMENT_3D ( 'NONE', #25396, #6624, #47219 ) ;
#67032=EDGE_CURVE ( 'NONE', #38079, #66432, #9034, .T. ) ;
#67033=EDGE_LOOP ( 'NONE', ( #62757, #12829, #11460, #49199 ) ) ;
#67039=DIRECTION ( 'NONE',  ( -1.000000000000000000, 0.000000000000000000, 0.000000000000000000 ) ) ;
#67046=CARTESIAN_POINT ( 'NONE',  ( 6.000000000000000000, -80.28980883073747066, -16.65972982745017461 ) ) ;
#67053=CARTESIAN_POINT ( 'NONE',  ( 15.00000000000000000, -22.32062822937489344, -14.36278369418800160 ) ) ;
#67061=PLANE ( 'NONE',  #16996 ) ;
#67063=VERTEX_POINT ( 'NONE', #1474 ) ;
#67064=AXIS2_PLACEMENT_3D ( 'NONE', #32350, #55664, #4553 ) ;
#67070=CARTESIAN_POINT ( 'NONE',  ( 11.99999999999999822, 0.000000000000000000, 0.000000000000000000 ) ) ;
#67077=VECTOR ( 'NONE', #55461, 1000.000000000000000 ) ;
#67083=CARTESIAN_POINT ( 'NONE',  ( 11.99999999999999822, 54.21277698773752007, -55.38113227695726692 ) ) ;
#67084=CARTESIAN_POINT ( 'NONE',  ( 15.00000000000000000, 20.85821328998741109, -10.92862929874522671 ) ) ;
#67089=AXIS2_PLACEMENT_3D ( 'NONE', #15909, #15160, #62150 ) ;
#67091=AXIS2_PLACEMENT_3D ( 'NONE', #13998, #36566, #31663 ) ;
#67110=DIRECTION ( 'NONE',  ( -1.000000000000000000, 0.000000000000000000, -0.000000000000000000 ) ) ;
#67127=ORIENTED_EDGE ( 'NONE', *, *, #38896, .F. ) ;
#67139=AXIS2_PLACEMENT_3D ( 'NONE', #47455, #13238, #524 ) ;
#67153=DIRECTION ( 'NONE',  ( -1.000000000000000000, -0.000000000000000000, -0.000000000000000000 ) ) ;
#67154=DIRECTION ( 'NONE',  ( -1.000000000000000000, 0.000000000000000000, 0.000000000000000000 ) ) ;
#67155=CIRCLE ( 'NONE', #63578, 21.00000000000000000 ) ;
#67156=DIRECTION ( 'NONE',  ( -1.000000000000000000, -0.000000000000000000, 0.000000000000000000 ) ) ;
#67158=LINE ( 'NONE', #4390, #72297 ) ;
#67159=FACE_OUTER_BOUND ( 'NONE', #37572, .T. ) ;
#67160=EDGE_LOOP ( 'NONE', ( #71247, #9181, #52492, #10911 ) ) ;
#67162=VERTEX_POINT ( 'NONE', #34524 ) ;
#67173=CYLINDRICAL_SURFACE ( 'NONE', #21045, 77.49899999999999523 ) ;
#67174=AXIS2_PLACEMENT_3D ( 'NONE', #6228, #69000, #58828 ) ;
#67175=VECTOR ( 'NONE', #50221, 1000.000000000000000 ) ;
#67181=DIRECTION ( 'NONE',  ( -1.000000000000000000, -0.000000000000000000, -0.000000000000000000 ) ) ;
#67185=DIRECTION ( 'NONE',  ( 0.000000000000000000, 0.000000000000000000, 1.000000000000000000 ) ) ;
#67187=CARTESIAN_POINT ( 'NONE',  ( 12.00000000000000000, 20.85821328998756385, 10.92862929874494249 ) ) ;
#67193=FACE_OUTER_BOUND ( 'NONE', #72444, .T. ) ;
#67196=AXIS2_PLACEMENT_3D ( 'NONE', #19895, #42480, #48111 ) ;
#67220=DIRECTION ( 'NONE',  ( -1.000000000000000000, 0.000000000000000000, 0.000000000000000000 ) ) ;
#67234=EDGE_CURVE ( 'NONE', #65491, #57151, #20571, .T. ) ;
#67235=VERTEX_POINT ( 'NONE', #14923 ) ;
#67240=EDGE_CURVE ( 'NONE', #26872, #34723, #33021, .T. ) ;
#67241=VERTEX_POINT ( 'NONE', #9281 ) ;
#67252=ORIENTED_EDGE ( 'NONE', *, *, #18098, .T. ) ;
#67265=AXIS2_PLACEMENT_3D ( 'NONE', #1301, #69302, #12521 ) ;
#67266=DIRECTION ( 'NONE',  ( 0.000000000000000000, 0.7604059656000276002, 0.6494480483301876550 ) ) ;
#67267=AXIS2_PLACEMENT_3D ( 'NONE', #60081, #21680, #44252 ) ;
#67268=DIRECTION ( 'NONE',  ( -1.000000000000000000, -0.000000000000000000, -0.000000000000000000 ) ) ;
#67271=FACE_OUTER_BOUND ( 'NONE', #71324, .T. ) ;
#67276=FACE_OUTER_BOUND ( 'NONE', #68654, .T. ) ;
#67277=CARTESIAN_POINT ( 'NONE',  ( 11.99999999999999822, 0.000000000000000000, 0.000000000000000000 ) ) ;
#67278=DIRECTION ( 'NONE',  ( 1.000000000000000000, -0.000000000000000000, -0.000000000000000000 ) ) ;
#67285=AXIS2_PLACEMENT_3D ( 'NONE', #16622, #6103, #39561 ) ;
#67287=LINE ( 'NONE', #15784, #49147 ) ;
#67290=DIRECTION ( 'NONE',  ( -1.000000000000000000, 0.000000000000000000, 0.000000000000000000 ) ) ;
#67295=EDGE_CURVE ( 'NONE', #12759, #56516, #16235, .T. ) ;
#67298=DIRECTION ( 'NONE',  ( -1.000000000000000000, 0.000000000000000000, 0.000000000000000000 ) ) ;
#67305=CIRCLE ( 'NONE', #32471, 31.99999999999998579 ) ;
#67313=CARTESIAN_POINT ( 'NONE',  ( -10.00000000000000000, 0.000000000000000000, 0.000000000000000000 ) ) ;
#67331=VERTEX_POINT ( 'NONE', #21289 ) ;
#67350=ORIENTED_EDGE ( 'NONE', *, *, #55264, .T. ) ;
#67363=DIRECTION ( 'NONE',  ( 0.000000000000000000, 0.9510565162951543083, 0.3090169943749449533 ) ) ;
#67364=FACE_OUTER_BOUND ( 'NONE', #64827, .T. ) ;
#67365=CARTESIAN_POINT ( 'NONE',  ( 15.00000000000000000, -1.278221433540507546, -26.51162292216071492 ) ) ;
#67367=CYLINDRICAL_SURFACE ( 'NONE', #70075, 31.99999999999998579 ) ;
#67368=ORIENTED_EDGE ( 'NONE', *, *, #37034, .T. ) ;
#67369=CARTESIAN_POINT ( 'NONE',  ( 11.99999999999999822, -20.41045688087772092, -72.35160999960838524 ) ) ;
#67375=LINE ( 'NONE', #40950, #57035 ) ;
#67383=ADVANCED_FACE ( 'NONE', ( #44995 ), #67173, .T. ) ;
#67391=ORIENTED_EDGE ( 'NONE', *, *, #7819, .F. ) ;
#67392=CARTESIAN_POINT ( 'NONE',  ( 11.99999999999999822, -14.66109333815513160, 73.73191006444567108 ) ) ;
#67402=EDGE_LOOP ( 'NONE', ( #32095, #30787, #21840, #45068 ) ) ;
#67410=ORIENTED_EDGE ( 'NONE', *, *, #39386, .F. ) ;
#67412=CIRCLE ( 'NONE', #10966, 31.99999999999998579 ) ;
#67418=DIRECTION ( 'NONE',  ( -1.000000000000000000, -0.000000000000000000, -0.000000000000000000 ) ) ;
#67420=CARTESIAN_POINT ( 'NONE',  ( 0.000000000000000000, 0.000000000000000000, 0.000000000000000000 ) ) ;
#67421=DIRECTION ( 'NONE',  ( 0.000000000000000000, -0.000000000000000000, 1.000000000000000000 ) ) ;
#67432=CARTESIAN_POINT ( 'NONE',  ( 11.99999999999999822, 26.02418014898407961, -70.52718814184231633 ) ) ;
#67434=DIRECTION ( 'NONE',  ( -1.000000000000000000, -0.000000000000000000, -0.000000000000000000 ) ) ;
#67443=AXIS2_PLACEMENT_3D ( 'NONE', #35474, #24569, #1318 ) ;
#67445=FACE_OUTER_BOUND ( 'NONE', #10820, .T. ) ;
#67446=CARTESIAN_POINT ( 'NONE',  ( 0.000000000000000000, 0.000000000000000000, 0.000000000000000000 ) ) ;
#67447=LINE ( 'NONE', #33597, #2431 ) ;
#67453=ORIENTED_EDGE ( 'NONE', *, *, #9748, .F. ) ;
#67457=DIRECTION ( 'NONE',  ( 0.000000000000000000, 0.000000000000000000, 1.000000000000000000 ) ) ;
#67462=ADVANCED_FACE ( 'NONE', ( #32578 ), #55525, .T. ) ;
#67469=DIRECTION ( 'NONE',  ( 0.000000000000000000, 0.000000000000000000, 1.000000000000000000 ) ) ;
#67480=AXIS2_PLACEMENT_3D ( 'NONE', #66699, #33584, #21943 ) ;
#67487=AXIS2_PLACEMENT_3D ( 'NONE', #70155, #28462, #74334 ) ;
#67489=VECTOR ( 'NONE', #12877, 1000.000000000000114 ) ;
#67491=ORIENTED_EDGE ( 'NONE', *, *, #51464, .T. ) ;
#67492=VERTEX_POINT ( 'NONE', #47207 ) ;
#67498=CARTESIAN_POINT ( 'NONE',  ( 11.99999999999999822, 0.000000000000000000, 0.000000000000000000 ) ) ;
#67505=ORIENTED_EDGE ( 'NONE', *, *, #42872, .T. ) ;
#67506=DIRECTION ( 'NONE',  ( 0.000000000000000000, 0.000000000000000000, 1.000000000000000000 ) ) ;
#67508=DIRECTION ( 'NONE',  ( 0.000000000000000000, -0.5877852522924691403, 0.8090169943749504489 ) ) ;
#67513=EDGE_LOOP ( 'NONE', ( #39506, #66210, #20216, #68753 ) ) ;
#67515=ORIENTED_EDGE ( 'NONE', *, *, #46196, .F. ) ;
#67524=DIRECTION ( 'NONE',  ( 0.000000000000000000, 0.000000000000000000, 1.000000000000000000 ) ) ;
#67533=CIRCLE ( 'NONE', #57931, 31.99999999999998579 ) ;
#67536=EDGE_CURVE ( 'NONE', #22824, #6493, #73922, .T. ) ;
#67540=VECTOR ( 'NONE', #24346, 1000.000000000000000 ) ;
#67543=CARTESIAN_POINT ( 'NONE',  ( 11.99999999999999822, 0.000000000000000000, 0.000000000000000000 ) ) ;
#67557=ADVANCED_FACE ( 'NONE', ( #40089 ), #51356, .T. ) ;
#67559=CYLINDRICAL_SURFACE ( 'NONE', #28801, 31.99999999999998579 ) ;
#67562=DIRECTION ( 'NONE',  ( 0.000000000000000000, 0.000000000000000000, 1.000000000000000000 ) ) ;
#67565=EDGE_CURVE ( 'NONE', #21247, #63634, #24280, .T. ) ;
#67574=DIRECTION ( 'NONE',  ( -1.000000000000000000, 0.000000000000000000, 0.000000000000000000 ) ) ;
#67581=ADVANCED_FACE ( 'NONE', ( #23905 ), #69034, .T. ) ;
#67589=ORIENTED_EDGE ( 'NONE', *, *, #63025, .F. ) ;
#67593=ORIENTED_EDGE ( 'NONE', *, *, #27792, .F. ) ;
#67594=LINE ( 'NONE', #27353, #28547 ) ;
#67597=ORIENTED_EDGE ( 'NONE', *, *, #33870, .T. ) ;
#67601=ORIENTED_EDGE ( 'NONE', *, *, #18426, .F. ) ;
#67606=CARTESIAN_POINT ( 'NONE',  ( 11.99999999999999822, 0.000000000000000000, 0.000000000000000000 ) ) ;
#67610=DIRECTION ( 'NONE',  ( 0.000000000000000000, 0.000000000000000000, 1.000000000000000000 ) ) ;
#67612=CARTESIAN_POINT ( 'NONE',  ( 11.99999999999999822, -41.19522573413689059, -65.64334221924951862 ) ) ;
#67615=DIRECTION ( 'NONE',  ( 0.000000000000000000, 0.000000000000000000, 1.000000000000000000 ) ) ;
#67623=AXIS2_PLACEMENT_3D ( 'NONE', #69768, #45382, #11157 ) ;
#67635=EDGE_CURVE ( 'NONE', #11463, #48336, #17467, .T. ) ;
#67639=DIRECTION ( 'NONE',  ( 0.000000000000000000, 0.000000000000000000, 1.000000000000000000 ) ) ;
#67643=LINE ( 'NONE', #9009, #45980 ) ;
#67645=CARTESIAN_POINT ( 'NONE',  ( 11.99999999999999822, -62.50884508063395373, -41.76106447765554464 ) ) ;
#67649=CIRCLE ( 'NONE', #54436, 31.99999999999998934 ) ;
#67650=CARTESIAN_POINT ( 'NONE',  ( 6.000000000000000000, -10.30890764327441289, 81.34940948281332851 ) ) ;
#67653=AXIS2_PLACEMENT_3D ( 'NONE', #66890, #72518, #21019 ) ;
#67662=ADVANCED_FACE ( 'NONE', ( #20098 ), #13719, .T. ) ;
#67672=DIRECTION ( 'NONE',  ( 0.000000000000000000, -0.9969173337331270757, -0.07845909572785580988 ) ) ;
#67680=DIRECTION ( 'NONE',  ( -1.000000000000000000, -0.000000000000000000, 0.000000000000000000 ) ) ;
#67681=ORIENTED_EDGE ( 'NONE', *, *, #9348, .T. ) ;
#67683=EDGE_LOOP ( 'NONE', ( #72387, #29027, #51299, #43295 ) ) ;
#67685=AXIS2_PLACEMENT_3D ( 'NONE', #48347, #8505, #31049 ) ;
#67686=ORIENTED_EDGE ( 'NONE', *, *, #8257, .T. ) ;
#67690=CARTESIAN_POINT ( 'NONE',  ( 11.99999999999999822, -8.830959090341869100, -74.65491531819127147 ) ) ;
#67692=LINE ( 'NONE', #15434, #29810 ) ;
#67694=ORIENTED_EDGE ( 'NONE', *, *, #73643, .F. ) ;
#67695=CARTESIAN_POINT ( 'NONE',  ( 5.999999999999999112, 77.16300072079698680, -27.74655509720591340 ) ) ;
#67696=ORIENTED_EDGE ( 'NONE', *, *, #31848, .T. ) ;
#67697=EDGE_LOOP ( 'NONE', ( #7217, #64290, #67515, #24024 ) ) ;
#67716=DIRECTION ( 'NONE',  ( -1.000000000000000000, -0.000000000000000000, 0.000000000000000000 ) ) ;
#67720=AXIS2_PLACEMENT_3D ( 'NONE', #29043, #41438, #17398 ) ;
#67725=EDGE_LOOP ( 'NONE', ( #7136, #42807, #67696, #23407 ) ) ;
#67727=ORIENTED_EDGE ( 'NONE', *, *, #23013, .F. ) ;
#67741=DIRECTION ( 'NONE',  ( 0.000000000000000000, -0.9238795325112906243, 0.3826834323650805669 ) ) ;
#67746=CIRCLE ( 'NONE', #42519, 31.99999999999998934 ) ;
#67748=AXIS2_PLACEMENT_3D ( 'NONE', #72268, #30932, #60643 ) ;
#67749=CYLINDRICAL_SURFACE ( 'NONE', #52682, 31.99999999999998579 ) ;
#67755=CIRCLE ( 'NONE', #36500, 31.99999999999998579 ) ;
#67756=EDGE_CURVE ( 'NONE', #57151, #69865, #58358, .T. ) ;
#67761=ORIENTED_EDGE ( 'NONE', *, *, #24701, .F. ) ;
#67786=ORIENTED_EDGE ( 'NONE', *, *, #29082, .F. ) ;
#67793=FACE_OUTER_BOUND ( 'NONE', #43557, .T. ) ;
#67807=CARTESIAN_POINT ( 'NONE',  ( 11.99999999999999822, -3.894527615417340272, -81.90746397400391743 ) ) ;
#67808=DIRECTION ( 'NONE',  ( -1.000000000000000000, -0.000000000000000000, -0.000000000000000000 ) ) ;
#67810=CARTESIAN_POINT ( 'NONE',  ( 11.99999999999999822, 73.44644590900061587, 24.73286445877730699 ) ) ;
#67812=AXIS2_PLACEMENT_3D ( 'NONE', #71153, #54981, #26772 ) ;
#67813=CARTESIAN_POINT ( 'NONE',  ( 11.99999999999999822, 0.000000000000000000, 0.000000000000000000 ) ) ;
#67826=EDGE_CURVE ( 'NONE', #40774, #12733, #3165, .T. ) ;
#67831=EDGE_CURVE ( 'NONE', #36914, #45508, #31379, .T. ) ;
#67834=CARTESIAN_POINT ( 'NONE',  ( 11.99999999999999822, -49.70050353004846500, -59.46389618802017907 ) ) ;
#67853=VERTEX_POINT ( 'NONE', #26489 ) ;
#67863=ORIENTED_EDGE ( 'NONE', *, *, #46249, .T. ) ;
#67875=ORIENTED_EDGE ( 'NONE', *, *, #20097, .T. ) ;
#67878=DIRECTION ( 'NONE',  ( 0.000000000000000000, 0.000000000000000000, 1.000000000000000000 ) ) ;
#67889=ORIENTED_EDGE ( 'NONE', *, *, #39987, .T. ) ;
#67892=ORIENTED_EDGE ( 'NONE', *, *, #17384, .F. ) ;
#67917=ADVANCED_FACE ( 'NONE', ( #45282 ), #68203, .F. ) ;
#67921=DIRECTION ( 'NONE',  ( 0.000000000000000000, 0.000000000000000000, 1.000000000000000000 ) ) ;
#67922=AXIS2_PLACEMENT_3D ( 'NONE', #35144, #58081, #30239 ) ;
#67924=DIRECTION ( 'NONE',  ( -1.000000000000000000, 0.000000000000000000, 0.000000000000000000 ) ) ;
#67937=DIRECTION ( 'NONE',  ( -1.000000000000000000, 0.000000000000000000, -0.000000000000000000 ) ) ;
#67946=DIRECTION ( 'NONE',  ( -1.000000000000000000, 0.000000000000000000, -0.000000000000000000 ) ) ;
#67954=CARTESIAN_POINT ( 'NONE',  ( 15.00000000000000000, 23.49999999999999645, 1.499999999999995337 ) ) ;
#67956=PLANE ( 'NONE',  #32690 ) ;
#67965=CARTESIAN_POINT ( 'NONE',  ( 11.99999999999999822, 0.000000000000000000, 0.000000000000000000 ) ) ;
#67985=ADVANCED_FACE ( 'NONE', ( #17072 ), #5436, .F. ) ;
#67987=CARTESIAN_POINT ( 'NONE',  ( 11.99999999999999822, -77.32052557432845674, 5.256550761632577284 ) ) ;
#67992=VERTEX_POINT ( 'NONE', #23813 ) ;
#68001=ORIENTED_EDGE ( 'NONE', *, *, #16528, .F. ) ;
#68011=CYLINDRICAL_SURFACE ( 'NONE', #20787, 82.00000000000000000 ) ;
#68012=CARTESIAN_POINT ( 'NONE',  ( -10.00000000000000000, 0.000000000000000000, 0.000000000000000000 ) ) ;
#68018=FACE_OUTER_BOUND ( 'NONE', #21949, .T. ) ;
#68019=ADVANCED_FACE ( 'NONE', ( #22721 ), #52378, .F. ) ;
#68027=VECTOR ( 'NONE', #11613, 1000.000000000000000 ) ;
#68030=DIRECTION ( 'NONE',  ( -1.000000000000000000, -0.000000000000000000, -0.000000000000000000 ) ) ;
#68032=VECTOR ( 'NONE', #62776, 1000.000000000000114 ) ;
#68036=CARTESIAN_POINT ( 'NONE',  ( 11.99999999999999822, -77.19088730480528682, 6.903761155837505825 ) ) ;
#68043=CARTESIAN_POINT ( 'NONE',  ( 5.999999999999999112, 51.29473840253317007, -63.97538442413369353 ) ) ;
#68045=ORIENTED_EDGE ( 'NONE', *, *, #54074, .F. ) ;
#68049=FACE_OUTER_BOUND ( 'NONE', #3120, .T. ) ;
#68051=VERTEX_POINT ( 'NONE', #40744 ) ;
#68060=FACE_OUTER_BOUND ( 'NONE', #74148, .T. ) ;
#68061=ORIENTED_EDGE ( 'NONE', *, *, #34023, .F. ) ;
#68066=VERTEX_POINT ( 'NONE', #39637 ) ;
#68067=VERTEX_POINT ( 'NONE', #52006 ) ;
#68070=DIRECTION ( 'NONE',  ( -1.000000000000000000, 0.000000000000000000, -0.000000000000000000 ) ) ;
#68074=ORIENTED_EDGE ( 'NONE', *, *, #30134, .F. ) ;
#68077=DIRECTION ( 'NONE',  ( 0.000000000000000000, 0.9876883405951383255, -0.1564344650402277048 ) ) ;
#68079=ORIENTED_EDGE ( 'NONE', *, *, #55443, .T. ) ;
#68088=DIRECTION ( 'NONE',  ( -1.000000000000000000, -0.000000000000000000, -0.000000000000000000 ) ) ;
#68093=LINE ( 'NONE', #4212, #49449 ) ;
#68098=LINE ( 'NONE', #45558, #20744 ) ;
#68104=CARTESIAN_POINT ( 'NONE',  ( 11.99999999999999822, 0.000000000000000000, 0.000000000000000000 ) ) ;
#68106=VERTEX_POINT ( 'NONE', #3771 ) ;
#68110=DIRECTION ( 'NONE',  ( -1.000000000000000000, 0.000000000000000000, 0.000000000000000000 ) ) ;
#68111=DIRECTION ( 'NONE',  ( 0.000000000000000000, -0.3826834323650772363, -0.9238795325112919565 ) ) ;
#68118=DIRECTION ( 'NONE',  ( -1.000000000000000000, -0.000000000000000000, -0.000000000000000000 ) ) ;
#68125=LINE ( 'NONE', #16619, #70784 ) ;
#68133=EDGE_CURVE ( 'NONE', #7284, #42705, #40332, .T. ) ;
#68139=EDGE_CURVE ( 'NONE', #11963, #66021, #66541, .T. ) ;
#68158=VERTEX_POINT ( 'NONE', #48861 ) ;
#68160=CARTESIAN_POINT ( 'NONE',  ( 11.99999999999999822, 0.000000000000000000, 0.000000000000000000 ) ) ;
#68161=DIRECTION ( 'NONE',  ( -1.000000000000000000, 0.000000000000000000, 0.000000000000000000 ) ) ;
#68165=DIRECTION ( 'NONE',  ( 0.000000000000000000, 0.9238795325112851842, 0.3826834323650938341 ) ) ;
#68168=ORIENTED_EDGE ( 'NONE', *, *, #50263, .F. ) ;
#68175=CARTESIAN_POINT ( 'NONE',  ( 11.99999999999999822, 0.000000000000000000, 0.000000000000000000 ) ) ;
#68190=CIRCLE ( 'NONE', #5791, 31.99999999999998579 ) ;
#68192=DIRECTION ( 'NONE',  ( 0.000000000000000000, 0.000000000000000000, -1.000000000000000000 ) ) ;
#68203=PLANE ( 'NONE',  #37969 ) ;
#68211=( NAMED_UNIT ( * ) PLANE_ANGLE_UNIT ( ) SI_UNIT ( $, .RADIAN. ) );
#68213=CIRCLE ( 'NONE', #41790, 31.99999999999998579 ) ;
#68217=CARTESIAN_POINT ( 'NONE',  ( 12.00000000000000000, -20.55727247249748402, -16.78983467731284307 ) ) ;
#68233=CARTESIAN_POINT ( 'NONE',  ( 11.99999999999999822, -75.54627589209955829, 17.28742895386058009 ) ) ;
#68238=AXIS2_PLACEMENT_3D ( 'NONE', #26951, #25574, #67562 ) ;
#68240=EDGE_CURVE ( 'NONE', #20251, #18486, #24820, .T. ) ;
#68243=ORIENTED_EDGE ( 'NONE', *, *, #13917, .T. ) ;
#68245=DIRECTION ( 'NONE',  ( 0.000000000000000000, 0.000000000000000000, 1.000000000000000000 ) ) ;
#68253=CARTESIAN_POINT ( 'NONE',  ( 11.99999999999999822, 55.38113227695858143, -54.21277698773617715 ) ) ;
#68254=AXIS2_PLACEMENT_3D ( 'NONE', #3814, #60217, #26349 ) ;
#68266=DIRECTION ( 'NONE',  ( 0.000000000000000000, 0.000000000000000000, 1.000000000000000000 ) ) ;
#68275=CARTESIAN_POINT ( 'NONE',  ( 11.99999999999999822, 6.903761155837791819, 77.19088730480525840 ) ) ;
#68277=DIRECTION ( 'NONE',  ( 0.000000000000000000, 0.1045284632676558162, 0.9945218953682731788 ) ) ;
#68279=CARTESIAN_POINT ( 'NONE',  ( 0.000000000000000000, -66.50666863321973210, -39.78640506895674633 ) ) ;
#68280=DIRECTION ( 'NONE',  ( -1.000000000000000000, 0.000000000000000000, 0.000000000000000000 ) ) ;
#68281=EDGE_CURVE ( 'NONE', #50461, #15716, #22415, .T. ) ;
#68283=CARTESIAN_POINT ( 'NONE',  ( 11.99999999999999822, 0.000000000000000000, 0.000000000000000000 ) ) ;
#68298=DIRECTION ( 'NONE',  ( 0.000000000000000000, 0.000000000000000000, 1.000000000000000000 ) ) ;
#68301=FACE_OUTER_BOUND ( 'NONE', #25040, .T. ) ;
#68302=CARTESIAN_POINT ( 'NONE',  ( 11.99999999999999822, -0.8261519478425843888, -77.49459641780887864 ) ) ;
#68305=DIRECTION ( 'NONE',  ( -1.000000000000000000, -0.000000000000000000, -0.000000000000000000 ) ) ;
#68306=DIRECTION ( 'NONE',  ( 0.000000000000000000, 0.000000000000000000, 1.000000000000000000 ) ) ;
#68307=FACE_OUTER_BOUND ( 'NONE', #45673, .T. ) ;
#68312=AXIS2_PLACEMENT_3D ( 'NONE', #48965, #3145, #13147 ) ;
#68318=CARTESIAN_POINT ( 'NONE',  ( 11.99999999999999822, 0.000000000000000000, 0.000000000000000000 ) ) ;
#68322=CYLINDRICAL_SURFACE ( 'NONE', #7168, 31.99999999999999289 ) ;
#68324=DIRECTION ( 'NONE',  ( -1.000000000000000000, 0.000000000000000000, 0.000000000000000000 ) ) ;
#68327=VERTEX_POINT ( 'NONE', #22534 ) ;
#68336=ADVANCED_FACE ( 'NONE', ( #73640 ), #39082, .T. ) ;
#68341=VERTEX_POINT ( 'NONE', #10494 ) ;
#68343=CARTESIAN_POINT ( 'NONE',  ( 15.00000000000000000, 0.000000000000000000, 0.000000000000000000 ) ) ;
#68346=CARTESIAN_POINT ( 'NONE',  ( 6.000000000000000000, -22.90783923731575200, -78.73519480814978522 ) ) ;
#68358=EDGE_CURVE ( 'NONE', #36787, #28860, #45222, .T. ) ;
#68373=CIRCLE ( 'NONE', #40728, 77.49899999999999523 ) ;
#68374=EDGE_CURVE ( 'NONE', #6126, #21432, #5633, .T. ) ;
#68375=EDGE_CURVE ( 'NONE', #62821, #18312, #27409, .T. ) ;
#68376=AXIS2_PLACEMENT_3D ( 'NONE', #25819, #61159, #43514 ) ;
#68378=VERTEX_POINT ( 'NONE', #27793 ) ;
#68380=CARTESIAN_POINT ( 'NONE',  ( 11.99999999999999822, -22.90783923731575200, -78.73519480814978522 ) ) ;
#68381=VECTOR ( 'NONE', #19490, 1000.000000000000000 ) ;
#68382=AXIS2_PLACEMENT_3D ( 'NONE', #11256, #34186, #29273 ) ;
#68383=ORIENTED_EDGE ( 'NONE', *, *, #55237, .F. ) ;
#68386=VERTEX_POINT ( 'NONE', #15263 ) ;
#68392=CARTESIAN_POINT ( 'NONE',  ( 5.999999999999999112, 64.81221759200342092, 50.23322058963371006 ) ) ;
#68393=DIRECTION ( 'NONE',  ( -1.000000000000000000, 0.000000000000000000, 0.000000000000000000 ) ) ;
#68397=DIRECTION ( 'NONE',  ( -1.000000000000000000, 0.000000000000000000, 0.000000000000000000 ) ) ;
#68402=DIRECTION ( 'NONE',  ( 0.000000000000000000, 0.8090169943749445647, 0.5877852522924770229 ) ) ;
#68403=AXIS2_PLACEMENT_3D ( 'NONE', #33868, #6424, #56814 ) ;
#68405=EDGE_CURVE ( 'NONE', #73333, #32813, #13961, .T. ) ;
#68406=DIRECTION ( 'NONE',  ( 0.000000000000000000, -0.2334453638559126354, 0.9723699203976748917 ) ) ;
#68407=AXIS2_PLACEMENT_3D ( 'NONE', #44230, #67156, #33295 ) ;
#68438=ORIENTED_EDGE ( 'NONE', *, *, #7901, .T. ) ;
#68447=CYLINDRICAL_SURFACE ( 'NONE', #66071, 31.99999999999998579 ) ;
#68448=CIRCLE ( 'NONE', #21451, 82.00000000000000000 ) ;
#68450=VERTEX_POINT ( 'NONE', #66768 ) ;
#68466=CARTESIAN_POINT ( 'NONE',  ( 0.000000000000000000, -24.73286445877757345, 73.44644590900053061 ) ) ;
#68468=VERTEX_POINT ( 'NONE', #72026 ) ;
#68470=CARTESIAN_POINT ( 'NONE',  ( 0.000000000000000000, 14.67089635893713684, 73.72996012237443608 ) ) ;
#68471=CARTESIAN_POINT ( 'NONE',  ( 0.000000000000000000, 75.11764819372149304, -2.946379043146603482 ) ) ;
#68474=DIRECTION ( 'NONE',  ( -1.000000000000000000, 0.000000000000000000, 0.000000000000000000 ) ) ;
#68477=VECTOR ( 'NONE', #57996, 1000.000000000000000 ) ;
#68497=CARTESIAN_POINT ( 'NONE',  ( 11.99999999999999822, 62.20884554314020676, 46.21855187248652896 ) ) ;
#68498=ORIENTED_EDGE ( 'NONE', *, *, #62211, .T. ) ;
#68501=DIRECTION ( 'NONE',  ( -1.000000000000000000, -0.000000000000000000, -0.000000000000000000 ) ) ;
#68508=CARTESIAN_POINT ( 'NONE',  ( 0.000000000000000000, -68.26794271651286294, 31.47745569255117104 ) ) ;
#68511=DIRECTION ( 'NONE',  ( 0.000000000000000000, 0.000000000000000000, 1.000000000000000000 ) ) ;
#68512=EDGE_LOOP ( 'NONE', ( #41716, #28132, #27898, #34765 ) ) ;
#68517=CARTESIAN_POINT ( 'NONE',  ( 0.000000000000000000, 0.000000000000000000, 0.000000000000000000 ) ) ;
#68518=CIRCLE ( 'NONE', #16940, 82.00000000000000000 ) ;
#68528=CIRCLE ( 'NONE', #2510, 31.99999999999998934 ) ;
#68532=EDGE_CURVE ( 'NONE', #57658, #12172, #69211, .T. ) ;
#68534=EDGE_CURVE ( 'NONE', #55684, #31218, #25801, .T. ) ;
#68535=ORIENTED_EDGE ( 'NONE', *, *, #65038, .F. ) ;
#68548=DIRECTION ( 'NONE',  ( -1.000000000000000000, 0.000000000000000000, 0.000000000000000000 ) ) ;
#68550=FACE_OUTER_BOUND ( 'NONE', #5215, .T. ) ;
#68563=AXIS2_PLACEMENT_3D ( 'NONE', #46472, #1020, #1395 ) ;
#68578=DIRECTION ( 'NONE',  ( 0.000000000000000000, -0.8526401643540970632, 0.5224985647159410274 ) ) ;
#68601=CARTESIAN_POINT ( 'NONE',  ( 0.000000000000000000, 69.42325613327440692, 34.44570377933622041 ) ) ;
#68606=EDGE_CURVE ( 'NONE', #46926, #55521, #52396, .T. ) ;
#68607=VERTEX_POINT ( 'NONE', #63366 ) ;
#68611=CIRCLE ( 'NONE', #9773, 82.00000000000000000 ) ;
#68613=EDGE_CURVE ( 'NONE', #40077, #63927, #62024, .T. ) ;
#68616=VERTEX_POINT ( 'NONE', #73507 ) ;
#68619=CIRCLE ( 'NONE', #28994, 82.00000000000000000 ) ;
#68620=EDGE_CURVE ( 'NONE', #70501, #70390, #22390, .T. ) ;
#68627=ORIENTED_EDGE ( 'NONE', *, *, #20894, .T. ) ;
#68630=ORIENTED_EDGE ( 'NONE', *, *, #55330, .T. ) ;
#68637=VECTOR ( 'NONE', #69051, 1000.000000000000000 ) ;
#68639=CARTESIAN_POINT ( 'NONE',  ( 11.99999999999999822, 50.95692526931329525, 58.39081064771768581 ) ) ;
#68641=ORIENTED_EDGE ( 'NONE', *, *, #43714, .T. ) ;
#68654=EDGE_LOOP ( 'NONE', ( #19960, #61784, #23221, #50328 ) ) ;
#68661=DIRECTION ( 'NONE',  ( 0.000000000000000000, 0.8090169943749445647, 0.5877852522924770229 ) ) ;
#68678=CARTESIAN_POINT ( 'NONE',  ( 0.000000000000000000, 0.000000000000000000, 0.000000000000000000 ) ) ;
#68679=EDGE_CURVE ( 'NONE', #20162, #13138, #66889, .T. ) ;
#68680=DIRECTION ( 'NONE',  ( 0.000000000000000000, 0.2079116908177664758, 0.9781476007338042455 ) ) ;
#68683=AXIS2_PLACEMENT_3D ( 'NONE', #50956, #45333, #33277 ) ;
#68686=CARTESIAN_POINT ( 'NONE',  ( 5.999999999999999112, 79.10210256391368944, 21.60688246758614994 ) ) ;
#68696=DIRECTION ( 'NONE',  ( 0.000000000000000000, -0.9510565162951536422, -0.3090169943749471182 ) ) ;
#68698=FACE_OUTER_BOUND ( 'NONE', #9183, .T. ) ;
#68704=ORIENTED_EDGE ( 'NONE', *, *, #20632, .T. ) ;
#68708=EDGE_CURVE ( 'NONE', #66935, #54483, #3270, .T. ) ;
#68709=CARTESIAN_POINT ( 'NONE',  ( 11.99999999999999822, 0.000000000000000000, 0.000000000000000000 ) ) ;
#68717=ORIENTED_EDGE ( 'NONE', *, *, #55997, .F. ) ;
#68719=ORIENTED_EDGE ( 'NONE', *, *, #68240, .F. ) ;
#68729=ORIENTED_EDGE ( 'NONE', *, *, #66974, .F. ) ;
#68730=DIRECTION ( 'NONE',  ( 0.000000000000000000, 0.9969173337331281859, -0.07845909572784168229 ) ) ;
#68731=EDGE_LOOP ( 'NONE', ( #22801, #39197, #42100, #14481 ) ) ;
#68738=DIRECTION ( 'NONE',  ( -1.000000000000000000, 0.000000000000000000, 0.000000000000000000 ) ) ;
#68739=DIRECTION ( 'NONE',  ( -1.000000000000000000, -0.000000000000000000, 0.000000000000000000 ) ) ;
#68747=FACE_BOUND ( 'NONE', #20745, .T. ) ;
#68748=VERTEX_POINT ( 'NONE', #69359 ) ;
#68751=ORIENTED_EDGE ( 'NONE', *, *, #11148, .F. ) ;
#68753=ORIENTED_EDGE ( 'NONE', *, *, #50238, .T. ) ;
#68767=CARTESIAN_POINT ( 'NONE',  ( 12.00000000000000000, 5.835314593368470248, -22.81335362449854642 ) ) ;
#68770=DIRECTION ( 'NONE',  ( 0.000000000000000000, 0.000000000000000000, 1.000000000000000000 ) ) ;
#68779=CIRCLE ( 'NONE', #46978, 82.00000000000000000 ) ;
#68785=DIRECTION ( 'NONE',  ( 0.000000000000000000, -0.5877852522924797984, -0.8090169943749426773 ) ) ;
#68806=ORIENTED_EDGE ( 'NONE', *, *, #40850, .F. ) ;
#68814=VERTEX_POINT ( 'NONE', #59570 ) ;
#68824=VERTEX_POINT ( 'NONE', #41904 ) ;
#68831=DIRECTION ( 'NONE',  ( 0.000000000000000000, 0.9135454576426055295, 0.4067366430757899387 ) ) ;
#68837=VECTOR ( 'NONE', #46297, 1000.000000000000000 ) ;
#68839=CARTESIAN_POINT ( 'NONE',  ( 11.99999999999999822, 0.000000000000000000, 0.000000000000000000 ) ) ;
#68840=CARTESIAN_POINT ( 'NONE',  ( 0.000000000000000000, 16.65972982744933972, 80.28980883073764119 ) ) ;
#68843=VECTOR ( 'NONE', #37087, 1000.000000000000000 ) ;
#68846=CIRCLE ( 'NONE', #62854, 31.99999999999998579 ) ;
#68848=AXIS2_PLACEMENT_3D ( 'NONE', #4049, #37510, #14932 ) ;
#68857=EDGE_LOOP ( 'NONE', ( #51115, #61127, #11294, #18132 ) ) ;
#68859=CARTESIAN_POINT ( 'NONE',  ( 0.000000000000000000, 26.01480285779837232, 70.53064760720326376 ) ) ;
#68868=ORIENTED_EDGE ( 'NONE', *, *, #53695, .F. ) ;
#68870=CARTESIAN_POINT ( 'NONE',  ( 6.000000000000000000, 10.30890764327382136, 81.34940948281339956 ) ) ;
#68875=DIRECTION ( 'NONE',  ( 1.000000000000000000, 0.000000000000000000, 0.000000000000000000 ) ) ;
#68882=AXIS2_PLACEMENT_3D ( 'NONE', #297, #15025, #60902 ) ;
#68884=DIRECTION ( 'NONE',  ( -1.000000000000000000, -0.000000000000000000, 0.000000000000000000 ) ) ;
#68887=CARTESIAN_POINT ( 'NONE',  ( 0.000000000000000000, 50.23322058963442061, -64.81221759200289512 ) ) ;
#68893=ORIENTED_EDGE ( 'NONE', *, *, #12450, .T. ) ;
#68900=ORIENTED_EDGE ( 'NONE', *, *, #61306, .T. ) ;
#68901=AXIS2_PLACEMENT_3D ( 'NONE', #11020, #69995, #29767 ) ;
#68910=LINE ( 'NONE', #17399, #16399 ) ;
#68912=DIRECTION ( 'NONE',  ( -1.000000000000000000, 0.000000000000000000, 0.000000000000000000 ) ) ;
#68913=CARTESIAN_POINT ( 'NONE',  ( 11.99999999999999822, 2.946379043146343246, 75.11764819372150725 ) ) ;
#68922=DIRECTION ( 'NONE',  ( 0.000000000000000000, -0.9945218953682730678, 0.1045284632676570929 ) ) ;
#68923=DIRECTION ( 'NONE',  ( 1.000000000000000000, 0.000000000000000000, 0.000000000000000000 ) ) ;
#68931=FACE_OUTER_BOUND ( 'NONE', #26866, .T. ) ;
#68939=DIRECTION ( 'NONE',  ( 0.000000000000000000, 0.3090169943749480619, -0.9510565162951533091 ) ) ;
#68940=CARTESIAN_POINT ( 'NONE',  ( 11.99999999999999822, -39.78640506895651896, 66.50666863321988842 ) ) ;
#68945=EDGE_CURVE ( 'NONE', #54483, #5078, #7725, .T. ) ;
#68956=ADVANCED_FACE ( 'NONE', ( #30638 ), #30276, .T. ) ;
#68968=ORIENTED_EDGE ( 'NONE', *, *, #57212, .T. ) ;
#68970=DIRECTION ( 'NONE',  ( -1.000000000000000000, -0.000000000000000000, -0.000000000000000000 ) ) ;
#68976=ORIENTED_EDGE ( 'NONE', *, *, #61794, .T. ) ;
#68998=CYLINDRICAL_SURFACE ( 'NONE', #3093, 77.49899999999999523 ) ;
#69000=DIRECTION ( 'NONE',  ( -1.000000000000000000, 0.000000000000000000, 0.000000000000000000 ) ) ;
#69012=ORIENTED_EDGE ( 'NONE', *, *, #3954, .T. ) ;
#69015=DIRECTION ( 'NONE',  ( -1.000000000000000000, 0.000000000000000000, -0.000000000000000000 ) ) ;
#69019=EDGE_CURVE ( 'NONE', #35261, #50077, #2125, .T. ) ;
#69020=ORIENTED_EDGE ( 'NONE', *, *, #389, .F. ) ;
#69022=CARTESIAN_POINT ( 'NONE',  ( 0.000000000000000000, 2.543863470248399761, 81.96053171279903893 ) ) ;
#69034=CYLINDRICAL_SURFACE ( 'NONE', #11450, 31.99999999999998579 ) ;
#69035=EDGE_CURVE ( 'NONE', #54635, #31231, #59231, .T. ) ;
#69051=DIRECTION ( 'NONE',  ( 1.000000000000000000, -0.000000000000000000, -0.000000000000000000 ) ) ;
#69052=VERTEX_POINT ( 'NONE', #63776 ) ;
#69056=AXIS2_PLACEMENT_3D ( 'NONE', #45087, #9746, #55610 ) ;
#69061=DIRECTION ( 'NONE',  ( -1.000000000000000000, -0.000000000000000000, -0.000000000000000000 ) ) ;
#69073=CARTESIAN_POINT ( 'NONE',  ( 0.000000000000000000, 0.000000000000000000, 0.000000000000000000 ) ) ;
#69090=ORIENTED_EDGE ( 'NONE', *, *, #14868, .T. ) ;
#69093=DIRECTION ( 'NONE',  ( -1.000000000000000000, 0.000000000000000000, 0.000000000000000000 ) ) ;
#69100=AXIS2_PLACEMENT_3D ( 'NONE', #52080, #12226, #64854 ) ;
#69101=ORIENTED_EDGE ( 'NONE', *, *, #37594, .T. ) ;
#69106=DIRECTION ( 'NONE',  ( 0.000000000000000000, 0.7071067811865486830, -0.7071067811865464625 ) ) ;
#69108=LINE ( 'NONE', #64208, #29099 ) ;
#69112=ORIENTED_EDGE ( 'NONE', *, *, #28091, .F. ) ;
#69115=ORIENTED_EDGE ( 'NONE', *, *, #9141, .F. ) ;
#69117=AXIS2_PLACEMENT_3D ( 'NONE', #69293, #63670, #19260 ) ;
#69134=CYLINDRICAL_SURFACE ( 'NONE', #58044, 31.99999999999998579 ) ;
#69140=DIRECTION ( 'NONE',  ( 1.000000000000000000, 0.000000000000000000, 0.000000000000000000 ) ) ;
#69147=VERTEX_POINT ( 'NONE', #59988 ) ;
#69156=AXIS2_PLACEMENT_3D ( 'NONE', #55550, #20961, #49529 ) ;
#69157=ORIENTED_EDGE ( 'NONE', *, *, #8088, .F. ) ;
#69158=VERTEX_POINT ( 'NONE', #38520 ) ;
#69161=LINE ( 'NONE', #68043, #7760 ) ;
#69163=CARTESIAN_POINT ( 'NONE',  ( 6.000000000000000000, 16.65972982745045528, -80.28980883073738539 ) ) ;
#69166=VERTEX_POINT ( 'NONE', #67083 ) ;
#69173=CARTESIAN_POINT ( 'NONE',  ( 0.000000000000000000, -75.54627589209931671, -17.28742895386162814 ) ) ;
#69178=EDGE_CURVE ( 'NONE', #73599, #7335, #27267, .T. ) ;
#69183=ORIENTED_EDGE ( 'NONE', *, *, #66822, .F. ) ;
#69188=VERTEX_POINT ( 'NONE', #43444 ) ;
#69195=ORIENTED_EDGE ( 'NONE', *, *, #58805, .T. ) ;
#69197=VERTEX_POINT ( 'NONE', #2860 ) ;
#69205=LINE ( 'NONE', #94, #299 ) ;
#69207=ADVANCED_FACE ( 'NONE', ( #25754 ), #43060, .T. ) ;
#69211=CIRCLE ( 'NONE', #18796, 31.99999999999998224 ) ;
#69212=DIRECTION ( 'NONE',  ( -1.000000000000000000, 0.000000000000000000, 0.000000000000000000 ) ) ;
#69216=CARTESIAN_POINT ( 'NONE',  ( 11.99999999999999822, -72.35160999960831418, 20.41045688087797672 ) ) ;
#69226=CIRCLE ( 'NONE', #60844, 77.49900000000000944 ) ;
#69231=DIRECTION ( 'NONE',  ( 0.000000000000000000, -0.7071067811865536790, 0.7071067811865414665 ) ) ;
#69241=CARTESIAN_POINT ( 'NONE',  ( 11.99999999999999822, 18.89407956138257205, 75.16055320797038064 ) ) ;
#69243=ADVANCED_FACE ( 'NONE', ( #5070 ), #39268, .T. ) ;
#69244=DIRECTION ( 'NONE',  ( -1.000000000000000000, 0.000000000000000000, 0.000000000000000000 ) ) ;
#69248=ORIENTED_EDGE ( 'NONE', *, *, #3499, .F. ) ;
#69263=CARTESIAN_POINT ( 'NONE',  ( 0.000000000000000000, 73.73191006444572793, -14.66109333815486515 ) ) ;
#69280=AXIS2_PLACEMENT_3D ( 'NONE', #24854, #1968, #18472 ) ;
#69282=ADVANCED_FACE ( 'NONE', ( #11420 ), #21964, .T. ) ;
#69293=CARTESIAN_POINT ( 'NONE',  ( 11.99999999999999822, -8.840884882374576037, -74.65374052328658649 ) ) ;
#69296=EDGE_LOOP ( 'NONE', ( #21469, #67786, #60297, #53716 ) ) ;
#69300=CARTESIAN_POINT ( 'NONE',  ( 15.00000000000000000, -10.45096189432344502, -21.10159698893425784 ) ) ;
#69302=DIRECTION ( 'NONE',  ( -1.000000000000000000, 0.000000000000000000, -0.000000000000000000 ) ) ;
#69303=VECTOR ( 'NONE', #72867, 1000.000000000000114 ) ;
#69304=ORIENTED_EDGE ( 'NONE', *, *, #12889, .T. ) ;
#69307=CARTESIAN_POINT ( 'NONE',  ( 15.00000000000000000, 0.000000000000000000, 0.000000000000000000 ) ) ;
#69309=CARTESIAN_POINT ( 'NONE',  ( 0.000000000000000000, 0.000000000000000000, 0.000000000000000000 ) ) ;
#69314=AXIS2_PLACEMENT_3D ( 'NONE', #57296, #10684, #5807 ) ;
#69316=EDGE_CURVE ( 'NONE', #69892, #50077, #62120, .T. ) ;
#69323=EDGE_CURVE ( 'NONE', #35960, #73028, #45334, .T. ) ;
#69335=ORIENTED_EDGE ( 'NONE', *, *, #59107, .F. ) ;
#69343=VECTOR ( 'NONE', #64959, 1000.000000000000000 ) ;
#69352=CARTESIAN_POINT ( 'NONE',  ( 11.99999999999999822, -67.80270845531921964, 46.11716303203162681 ) ) ;
#69359=CARTESIAN_POINT ( 'NONE',  ( 12.00000000000000000, 16.61724383029390140, 20.69703378468902955 ) ) ;
#69365=EDGE_CURVE ( 'NONE', #1061, #25431, #38893, .T. ) ;
#69378=CYLINDRICAL_SURFACE ( 'NONE', #57632, 77.49899999999999523 ) ;
#69382=AXIS2_PLACEMENT_3D ( 'NONE', #31989, #10843, #37654 ) ;
#69383=AXIS2_PLACEMENT_3D ( 'NONE', #50931, #22367, #50175 ) ;
#69390=DIRECTION ( 'NONE',  ( 0.000000000000000000, 0.000000000000000000, 1.000000000000000000 ) ) ;
#69391=DIRECTION ( 'NONE',  ( 0.000000000000000000, -0.8910065241883626808, -0.4539904997395569075 ) ) ;
#69393=CARTESIAN_POINT ( 'NONE',  ( 0.000000000000000000, 70.53064760720278059, 26.01480285779964774 ) ) ;
#69394=CARTESIAN_POINT ( 'NONE',  ( -10.00000000000000000, 0.000000000000000000, 0.000000000000000000 ) ) ;
#69399=CIRCLE ( 'NONE', #5776, 77.49900000000000944 ) ;
#69401=AXIS2_PLACEMENT_3D ( 'NONE', #17074, #11419, #67457 ) ;
#69404=CARTESIAN_POINT ( 'NONE',  ( 11.99999999999999822, 0.000000000000000000, 0.000000000000000000 ) ) ;
#69410=EDGE_CURVE ( 'NONE', #72289, #25980, #11702, .T. ) ;
#69416=EDGE_CURVE ( 'NONE', #30664, #54778, #69680, .T. ) ;
#69423=VECTOR ( 'NONE', #73107, 1000.000000000000000 ) ;
#69437=EDGE_LOOP ( 'NONE', ( #66674, #52054, #36911, #58500 ) ) ;
#69461=FACE_OUTER_BOUND ( 'NONE', #26569, .T. ) ;
#69463=ORIENTED_EDGE ( 'NONE', *, *, #4864, .T. ) ;
#69464=DIRECTION ( 'NONE',  ( 0.000000000000000000, 0.5877852522924743583, -0.8090169943749465631 ) ) ;
#69468=ORIENTED_EDGE ( 'NONE', *, *, #44051, .T. ) ;
#69472=CARTESIAN_POINT ( 'NONE',  ( 11.99999999999999822, 0.000000000000000000, 0.000000000000000000 ) ) ;
#69473=CARTESIAN_POINT ( 'NONE',  ( 0.000000000000000000, 51.03279382321166224, -55.19960302592011914 ) ) ;
#69474=ORIENTED_EDGE ( 'NONE', *, *, #34539, .F. ) ;
#69478=DIRECTION ( 'NONE',  ( 0.000000000000000000, 0.000000000000000000, 1.000000000000000000 ) ) ;
#69479=ORIENTED_EDGE ( 'NONE', *, *, #42717, .T. ) ;
#69500=CYLINDRICAL_SURFACE ( 'NONE', #55070, 77.49899999999999523 ) ;
#69501=EDGE_CURVE ( 'NONE', #49856, #63817, #18177, .T. ) ;
#69504=FACE_OUTER_BOUND ( 'NONE', #61005, .T. ) ;
#69514=CIRCLE ( 'NONE', #70736, 31.99999999999998579 ) ;
#69515=ORIENTED_EDGE ( 'NONE', *, *, #48781, .F. ) ;
#69527=ORIENTED_EDGE ( 'NONE', *, *, #1576, .F. ) ;
#69531=ADVANCED_FACE ( 'NONE', ( #70036 ), #35467, .F. ) ;
#69534=AXIS2_PLACEMENT_3D ( 'NONE', #66084, #14553, #42032 ) ;
#69536=VECTOR ( 'NONE', #14596, 1000.000000000000000 ) ;
#69540=AXIS2_PLACEMENT_3D ( 'NONE', #64338, #30468, #58318 ) ;
#69544=ORIENTED_EDGE ( 'NONE', *, *, #36408, .F. ) ;
#69545=CARTESIAN_POINT ( 'NONE',  ( 11.99999999999999822, 0.000000000000000000, 0.000000000000000000 ) ) ;
#69546=ORIENTED_EDGE ( 'NONE', *, *, #48566, .T. ) ;
#69557=DIRECTION ( 'NONE',  ( 0.000000000000000000, 0.000000000000000000, 1.000000000000000000 ) ) ;
#69561=ORIENTED_EDGE ( 'NONE', *, *, #29930, .F. ) ;
#69564=EDGE_LOOP ( 'NONE', ( #40796, #61814, #6751, #52932 ) ) ;
#69573=DIRECTION ( 'NONE',  ( -1.000000000000000000, 0.000000000000000000, 0.000000000000000000 ) ) ;
#69583=LINE ( 'NONE', #63961, #35229 ) ;
#69588=CIRCLE ( 'NONE', #39595, 82.00000000000000000 ) ;
#69611=CARTESIAN_POINT ( 'NONE',  ( 11.99999999999999822, 44.88180994100466847, -63.18004540532978552 ) ) ;
#69614=DIRECTION ( 'NONE',  ( 0.000000000000000000, 0.000000000000000000, 1.000000000000000000 ) ) ;
#69626=FACE_OUTER_BOUND ( 'NONE', #3911, .T. ) ;
#69636=VECTOR ( 'NONE', #70577, 1000.000000000000000 ) ;
#69646=AXIS2_PLACEMENT_3D ( 'NONE', #44835, #61388, #27141 ) ;
#69655=DIRECTION ( 'NONE',  ( 0.000000000000000000, 0.000000000000000000, 1.000000000000000000 ) ) ;
#69676=EDGE_CURVE ( 'NONE', #47732, #65728, #63421, .T. ) ;
#69678=CARTESIAN_POINT ( 'NONE',  ( 11.99999999999999822, 75.11764819372149304, -2.946379043146603482 ) ) ;
#69680=LINE ( 'NONE', #6895, #35696 ) ;
#69684=EDGE_CURVE ( 'NONE', #38198, #45762, #68190, .T. ) ;
#69690=ORIENTED_EDGE ( 'NONE', *, *, #45708, .F. ) ;
#69691=CARTESIAN_POINT ( 'NONE',  ( 11.99999999999999822, -20.41045688087876897, 72.35160999960810102 ) ) ;
#69700=ORIENTED_EDGE ( 'NONE', *, *, #50607, .F. ) ;
#69701=ADVANCED_FACE ( 'NONE', ( #67364 ), #62492, .T. ) ;
#69705=FACE_OUTER_BOUND ( 'NONE', #49736, .T. ) ;
#69706=ADVANCED_FACE ( 'NONE', ( #16602 ), #44816, .T. ) ;
#69708=ORIENTED_EDGE ( 'NONE', *, *, #10864, .F. ) ;
#69709=ORIENTED_EDGE ( 'NONE', *, *, #71051, .F. ) ;
#69717=ORIENTED_EDGE ( 'NONE', *, *, #41079, .F. ) ;
#69726=DIRECTION ( 'NONE',  ( 0.000000000000000000, 0.5224985647159499091, -0.8526401643540916231 ) ) ;
#69729=CARTESIAN_POINT ( 'NONE',  ( 11.99999999999999822, -8.966570791700153364, -81.50828551894235829 ) ) ;
#69731=ORIENTED_EDGE ( 'NONE', *, *, #14839, .F. ) ;
#69732=DIRECTION ( 'NONE',  ( -1.000000000000000000, 0.000000000000000000, 0.000000000000000000 ) ) ;
#69733=VERTEX_POINT ( 'NONE', #38427 ) ;
#69736=VERTEX_POINT ( 'NONE', #62871 ) ;
#69739=CARTESIAN_POINT ( 'NONE',  ( 0.000000000000000000, -62.50329211542407393, -41.76937507738853839 ) ) ;
#69741=AXIS2_PLACEMENT_3D ( 'NONE', #53029, #24451, #70290 ) ;
#69742=DIRECTION ( 'NONE',  ( 0.000000000000000000, 0.1564344650402244019, 0.9876883405951387696 ) ) ;
#69746=DIRECTION ( 'NONE',  ( -1.000000000000000000, 0.000000000000000000, -0.000000000000000000 ) ) ;
#69760=CARTESIAN_POINT ( 'NONE',  ( 11.99999999999999822, 59.03342792756328095, -46.54456581323744757 ) ) ;
#69761=DIRECTION ( 'NONE',  ( 0.000000000000000000, 0.000000000000000000, -1.000000000000000000 ) ) ;
#69764=CYLINDRICAL_SURFACE ( 'NONE', #66528, 77.49899999999999523 ) ;
#69767=CYLINDRICAL_SURFACE ( 'NONE', #36399, 82.00000000000000000 ) ;
#69768=CARTESIAN_POINT ( 'NONE',  ( 0.000000000000000000, 0.000000000000000000, 0.000000000000000000 ) ) ;
#69770=EDGE_CURVE ( 'NONE', #8982, #68341, #39370, .T. ) ;
#69795=CARTESIAN_POINT ( 'NONE',  ( 0.000000000000000000, 68.67312586195046720, -35.91791733033404199 ) ) ;
#69796=DIRECTION ( 'NONE',  ( -1.000000000000000000, 0.000000000000000000, 0.000000000000000000 ) ) ;
#69800=ORIENTED_EDGE ( 'NONE', *, *, #47644, .T. ) ;
#69822=AXIS2_PLACEMENT_3D ( 'NONE', #72958, #67716, #73710 ) ;
#69828=CIRCLE ( 'NONE', #31403, 31.99999999999999289 ) ;
#69833=AXIS2_PLACEMENT_3D ( 'NONE', #29967, #42007, #7424 ) ;
#69848=FACE_OUTER_BOUND ( 'NONE', #30798, .T. ) ;
#69865=VERTEX_POINT ( 'NONE', #36114 ) ;
#69866=CARTESIAN_POINT ( 'NONE',  ( 0.000000000000000000, -74.18225833017913828, 34.94270380257611208 ) ) ;
#69870=AXIS2_PLACEMENT_3D ( 'NONE', #66523, #37582, #60518 ) ;
#69876=CARTESIAN_POINT ( 'NONE',  ( 11.99999999999999822, 46.53671651293948486, 59.03961581697416250 ) ) ;
#69880=CARTESIAN_POINT ( 'NONE',  ( 11.99999999999999822, 0.000000000000000000, 0.000000000000000000 ) ) ;
#69885=ORIENTED_EDGE ( 'NONE', *, *, #44168, .F. ) ;
#69891=CARTESIAN_POINT ( 'NONE',  ( 11.99999999999999822, -55.20638768913724448, -51.02545421589383068 ) ) ;
#69892=VERTEX_POINT ( 'NONE', #52296 ) ;
#69896=ORIENTED_EDGE ( 'NONE', *, *, #66878, .F. ) ;
#69902=DIRECTION ( 'NONE',  ( 0.000000000000000000, 0.000000000000000000, 1.000000000000000000 ) ) ;
#69920=VERTEX_POINT ( 'NONE', #470 ) ;
#69931=CARTESIAN_POINT ( 'NONE',  ( 11.99999999999999822, -68.26794271651286294, 31.47745569255117104 ) ) ;
#69935=VECTOR ( 'NONE', #54687, 1000.000000000000000 ) ;
#69940=CIRCLE ( 'NONE', #53103, 31.99999999999998224 ) ;
#69946=DIRECTION ( 'NONE',  ( -1.000000000000000000, 0.000000000000000000, 0.000000000000000000 ) ) ;
#69955=LINE ( 'NONE', #65452, #10721 ) ;
#69971=ORIENTED_EDGE ( 'NONE', *, *, #6451, .T. ) ;
#69975=ORIENTED_EDGE ( 'NONE', *, *, #49957, .T. ) ;
#69984=CARTESIAN_POINT ( 'NONE',  ( 11.99999999999999822, -50.95692526931372157, 58.39081064771733054 ) ) ;
#69987=EDGE_CURVE ( 'NONE', #34202, #34378, #47838, .T. ) ;
#69995=DIRECTION ( 'NONE',  ( -1.000000000000000000, 0.000000000000000000, 0.000000000000000000 ) ) ;
#69998=DIRECTION ( 'NONE',  ( 0.000000000000000000, 0.9238795325112877377, -0.3826834323650873948 ) ) ;
#70000=DIRECTION ( 'NONE',  ( -1.000000000000000000, 0.000000000000000000, 0.000000000000000000 ) ) ;
#70005=EDGE_CURVE ( 'NONE', #28647, #10445, #44250, .T. ) ;
#70019=CARTESIAN_POINT ( 'NONE',  ( 12.00000000000000000, -22.67460108101782978, -6.353146135317906840 ) ) ;
#70020=DIRECTION ( 'NONE',  ( 0.000000000000000000, 0.000000000000000000, 1.000000000000000000 ) ) ;
#70030=ORIENTED_EDGE ( 'NONE', *, *, #62508, .T. ) ;
#70032=ADVANCED_FACE ( 'NONE', ( #33324 ), #19556, .T. ) ;
#70036=FACE_OUTER_BOUND ( 'NONE', #60409, .T. ) ;
#70039=( NAMED_UNIT ( * ) PLANE_ANGLE_UNIT ( ) SI_UNIT ( $, .RADIAN. ) );
#70040=CARTESIAN_POINT ( 'NONE',  ( 15.00000000000000000, 14.60985201121729737, 18.46759930825687235 ) ) ;
#70042=CIRCLE ( 'NONE', #56812, 31.99999999999998224 ) ;
#70058=ORIENTED_EDGE ( 'NONE', *, *, #47709, .F. ) ;
#70059=DIRECTION ( 'NONE',  ( 1.000000000000000000, 0.000000000000000000, 0.000000000000000000 ) ) ;
#70064=ORIENTED_EDGE ( 'NONE', *, *, #69416, .T. ) ;
#70069=ORIENTED_EDGE ( 'NONE', *, *, #26567, .T. ) ;
#70075=AXIS2_PLACEMENT_3D ( 'NONE', #49689, #61739, #21123 ) ;
#70080=CIRCLE ( 'NONE', #67685, 21.00000000000000000 ) ;
#70082=EDGE_CURVE ( 'NONE', #65052, #33844, #36997, .T. ) ;
#70092=ORIENTED_EDGE ( 'NONE', *, *, #6547, .T. ) ;
#70096=ORIENTED_EDGE ( 'NONE', *, *, #36227, .T. ) ;
#70098=AXIS2_PLACEMENT_3D ( 'NONE', #56944, #5452, #40019 ) ;
#70100=DIRECTION ( 'NONE',  ( -1.000000000000000000, 0.000000000000000000, 0.000000000000000000 ) ) ;
#70101=CARTESIAN_POINT ( 'NONE',  ( -10.00000000000000000, 0.000000000000000000, 0.000000000000000000 ) ) ;
#70108=VERTEX_POINT ( 'NONE', #13548 ) ;
#70117=AXIS2_PLACEMENT_3D ( 'NONE', #38849, #51234, #55771 ) ;
#70121=LINE ( 'NONE', #47943, #45088 ) ;
#70122=CARTESIAN_POINT ( 'NONE',  ( 5.999999999999999112, 21.60688246758697062, -79.10210256391344785 ) ) ;
#70123=CARTESIAN_POINT ( 'NONE',  ( 11.99999999999999822, -73.44644590900077219, 24.73286445877677764 ) ) ;
#70143=VECTOR ( 'NONE', #58321, 1000.000000000000000 ) ;
#70149=ORIENTED_EDGE ( 'NONE', *, *, #71380, .T. ) ;
#70154=FACE_OUTER_BOUND ( 'NONE', #64158, .T. ) ;
#70155=CARTESIAN_POINT ( 'NONE',  ( 0.000000000000000000, -41.76937507738745836, -62.50329211542482710 ) ) ;
#70159=ORIENTED_EDGE ( 'NONE', *, *, #17879, .F. ) ;
#70160=VERTEX_POINT ( 'NONE', #39365 ) ;
#70162=EDGE_LOOP ( 'NONE', ( #31249, #14901, #39019, #2031 ) ) ;
#70171=VERTEX_POINT ( 'NONE', #28818 ) ;
#70173=ORIENTED_EDGE ( 'NONE', *, *, #27075, .T. ) ;
#70182=DIRECTION ( 'NONE',  ( -1.000000000000000000, 0.000000000000000000, -0.000000000000000000 ) ) ;
#70197=VERTEX_POINT ( 'NONE', #40464 ) ;
#70198=CIRCLE ( 'NONE', #61849, 82.00000000000000000 ) ;
#70200=CIRCLE ( 'NONE', #25934, 31.99999999999998579 ) ;
#70205=CARTESIAN_POINT ( 'NONE',  ( 0.000000000000000000, -18.89407956138204980, -75.16055320797050854 ) ) ;
#70216=FACE_OUTER_BOUND ( 'NONE', #18618, .T. ) ;
#70221=ORIENTED_EDGE ( 'NONE', *, *, #20605, .F. ) ;
#70222=DIRECTION ( 'NONE',  ( -1.000000000000000000, -0.000000000000000000, 0.000000000000000000 ) ) ;
#70223=DIRECTION ( 'NONE',  ( 1.000000000000000000, -0.000000000000000000, -0.000000000000000000 ) ) ;
#70224=DIRECTION ( 'NONE',  ( 0.000000000000000000, 0.000000000000000000, 1.000000000000000000 ) ) ;
#70226=LINE ( 'NONE', #64613, #15208 ) ;
#70232=EDGE_CURVE ( 'NONE', #21904, #66208, #19010, .T. ) ;
#70233=DIRECTION ( 'NONE',  ( -1.000000000000000000, 0.000000000000000000, 0.000000000000000000 ) ) ;
#70236=DIRECTION ( 'NONE',  ( -1.000000000000000000, 0.000000000000000000, 0.000000000000000000 ) ) ;
#70237=VECTOR ( 'NONE', #64166, 1000.000000000000000 ) ;
#70245=CIRCLE ( 'NONE', #34257, 31.99999999999999289 ) ;
#70246=ORIENTED_EDGE ( 'NONE', *, *, #73424, .T. ) ;
#70256=LINE ( 'NONE', #36797, #15282 ) ;
#70265=DIRECTION ( 'NONE',  ( 0.000000000000000000, 0.000000000000000000, 1.000000000000000000 ) ) ;
#70269=CIRCLE ( 'NONE', #47494, 82.00000000000000000 ) ;
#70275=ORIENTED_EDGE ( 'NONE', *, *, #73513, .T. ) ;
#70280=ORIENTED_EDGE ( 'NONE', *, *, #50123, .T. ) ;
#70288=FACE_OUTER_BOUND ( 'NONE', #27234, .T. ) ;
#70290=DIRECTION ( 'NONE',  ( 0.000000000000000000, 0.000000000000000000, 1.000000000000000000 ) ) ;
#70291=DIRECTION ( 'NONE',  ( -1.000000000000000000, -0.000000000000000000, -0.000000000000000000 ) ) ;
#70292=LINE ( 'NONE', #18797, #20741 ) ;
#70297=DIRECTION ( 'NONE',  ( 0.000000000000000000, 0.000000000000000000, 1.000000000000000000 ) ) ;
#70300=DIRECTION ( 'NONE',  ( 0.000000000000000000, -0.5224985647159381408, -0.8526401643540988395 ) ) ;
#70323=ADVANCED_FACE ( 'NONE', ( #48608 ), #48961, .T. ) ;
#70330=ADVANCED_FACE ( 'NONE', ( #42602 ), #71521, .T. ) ;
#70335=ORIENTED_EDGE ( 'NONE', *, *, #35573, .T. ) ;
#70339=DIRECTION ( 'NONE',  ( -1.000000000000000000, 0.000000000000000000, 0.000000000000000000 ) ) ;
#70342=EDGE_CURVE ( 'NONE', #42429, #63620, #15123, .T. ) ;
#70343=VERTEX_POINT ( 'NONE', #71892 ) ;
#70345=EDGE_CURVE ( 'NONE', #9142, #29501, #70620, .T. ) ;
#70359=DIRECTION ( 'NONE',  ( -1.000000000000000000, 0.000000000000000000, -0.000000000000000000 ) ) ;
#70366=AXIS2_PLACEMENT_3D ( 'NONE', #36552, #59504, #2402 ) ;
#70380=ORIENTED_EDGE ( 'NONE', *, *, #46631, .T. ) ;
#70390=VERTEX_POINT ( 'NONE', #65538 ) ;
#70402=DIRECTION ( 'NONE',  ( 0.000000000000000000, 0.000000000000000000, -1.000000000000000000 ) ) ;
#70404=FACE_OUTER_BOUND ( 'NONE', #35682, .T. ) ;
#70410=EDGE_CURVE ( 'NONE', #10633, #41779, #62112, .T. ) ;
#70415=CIRCLE ( 'NONE', #35603, 31.99999999999999645 ) ;
#70423=CIRCLE ( 'NONE', #58423, 31.99999999999998934 ) ;
#70425=ORIENTED_EDGE ( 'NONE', *, *, #70082, .F. ) ;
#70433=CARTESIAN_POINT ( 'NONE',  ( 0.000000000000000000, -21.60688246758530084, -79.10210256391388839 ) ) ;
#70438=ORIENTED_EDGE ( 'NONE', *, *, #33896, .F. ) ;
#70440=EDGE_CURVE ( 'NONE', #40781, #33089, #4985, .T. ) ;
#70451=LINE ( 'NONE', #70832, #33895 ) ;
#70457=VECTOR ( 'NONE', #28141, 1000.000000000000000 ) ;
#70459=CARTESIAN_POINT ( 'NONE',  ( 0.000000000000000000, -54.21277698773636899, -55.38113227695839669 ) ) ;
#70461=CARTESIAN_POINT ( 'NONE',  ( 15.00000000000000000, 23.49999999999999645, 1.499999999999995337 ) ) ;
#70465=VERTEX_POINT ( 'NONE', #27518 ) ;
#70469=VECTOR ( 'NONE', #63943, 1000.000000000000000 ) ;
#70472=FACE_OUTER_BOUND ( 'NONE', #47431, .T. ) ;
#70476=EDGE_LOOP ( 'NONE', ( #19954, #44006, #47571, #49258 ) ) ;
#70481=PLANE ( 'NONE',  #24449 ) ;
#70483=DIRECTION ( 'NONE',  ( 0.000000000000000000, 0.000000000000000000, 1.000000000000000000 ) ) ;
#70498=EDGE_CURVE ( 'NONE', #143, #34944, #31086, .T. ) ;
#70501=VERTEX_POINT ( 'NONE', #7559 ) ;
#70505=CIRCLE ( 'NONE', #38120, 82.00000000000000000 ) ;
#70507=CARTESIAN_POINT ( 'NONE',  ( 11.99999999999999822, 81.96053171279901051, 2.543863470248673764 ) ) ;
#70515=DIRECTION ( 'NONE',  ( -1.000000000000000000, -0.000000000000000000, 0.000000000000000000 ) ) ;
#70521=ORIENTED_EDGE ( 'NONE', *, *, #65059, .T. ) ;
#70543=EDGE_LOOP ( 'NONE', ( #21804, #32991, #62179, #60648 ) ) ;
#70547=CARTESIAN_POINT ( 'NONE',  ( 11.99999999999999822, -75.54627589209955829, 17.28742895386058009 ) ) ;
#70553=DIRECTION ( 'NONE',  ( -1.000000000000000000, -0.000000000000000000, -0.000000000000000000 ) ) ;
#70558=VECTOR ( 'NONE', #3352, 1000.000000000000000 ) ;
#70561=AXIS2_PLACEMENT_3D ( 'NONE', #45376, #5894, #68298 ) ;
#70569=AXIS2_PLACEMENT_3D ( 'NONE', #22623, #33898, #56839 ) ;
#70570=CARTESIAN_POINT ( 'NONE',  ( 11.99999999999999822, 0.000000000000000000, 0.000000000000000000 ) ) ;
#70577=DIRECTION ( 'NONE',  ( 0.000000000000000000, -0.8660254037844421493, -0.4999999999999939493 ) ) ;
#70586=AXIS2_PLACEMENT_3D ( 'NONE', #34137, #5961, #51800 ) ;
#70592=EDGE_CURVE ( 'NONE', #54635, #33655, #3479, .T. ) ;
#70602=CARTESIAN_POINT ( 'NONE',  ( 0.000000000000000000, -41.19522573413780009, 65.64334221924896440 ) ) ;
#70610=CIRCLE ( 'NONE', #21404, 31.99999999999998934 ) ;
#70613=ORIENTED_EDGE ( 'NONE', *, *, #63837, .F. ) ;
#70615=DIRECTION ( 'NONE',  ( 0.000000000000000000, -0.5224985647159559043, 0.8526401643540879594 ) ) ;
#70619=CARTESIAN_POINT ( 'NONE',  ( 0.000000000000000000, 26.02418014898407961, -70.52718814184231633 ) ) ;
#70620=CIRCLE ( 'NONE', #65819, 31.99999999999998224 ) ;
#70621=EDGE_LOOP ( 'NONE', ( #34561, #53917, #13940, #11500 ) ) ;
#70626=LINE ( 'NONE', #7499, #2333 ) ;
#70639=ORIENTED_EDGE ( 'NONE', *, *, #21709, .T. ) ;
#70642=CYLINDRICAL_SURFACE ( 'NONE', #36100, 82.00000000000000000 ) ;
#70643=VECTOR ( 'NONE', #38994, 1000.000000000000000 ) ;
#70647=DIRECTION ( 'NONE',  ( -1.000000000000000000, 0.000000000000000000, -0.000000000000000000 ) ) ;
#70653=DIRECTION ( 'NONE',  ( -1.000000000000000000, 0.000000000000000000, 0.000000000000000000 ) ) ;
#70654=CARTESIAN_POINT ( 'NONE',  ( 11.99999999999999822, 76.69515212746057387, -29.01471420065479379 ) ) ;
#70659=EDGE_CURVE ( 'NONE', #30548, #11576, #7921, .T. ) ;
#70660=CARTESIAN_POINT ( 'NONE',  ( 11.99999999999999822, 75.11764819372149304, -2.946379043146603482 ) ) ;
#70661=DIRECTION ( 'NONE',  ( -1.000000000000000000, -0.000000000000000000, -0.000000000000000000 ) ) ;
#70662=EDGE_CURVE ( 'NONE', #72362, #63075, #3783, .T. ) ;
#70664=VECTOR ( 'NONE', #2537, 1000.000000000000227 ) ;
#70669=AXIS2_PLACEMENT_3D ( 'NONE', #65948, #37378, #14427 ) ;
#70677=DIRECTION ( 'NONE',  ( -1.000000000000000000, 0.000000000000000000, 0.000000000000000000 ) ) ;
#70678=DIRECTION ( 'NONE',  ( -1.000000000000000000, -0.000000000000000000, -0.000000000000000000 ) ) ;
#70681=ORIENTED_EDGE ( 'NONE', *, *, #38875, .T. ) ;
#70685=CIRCLE ( 'NONE', #10711, 31.99999999999998579 ) ;
#70689=AXIS2_PLACEMENT_3D ( 'NONE', #54899, #43639, #66561 ) ;
#70696=LINE ( 'NONE', #59440, #14302 ) ;
#70706=ORIENTED_EDGE ( 'NONE', *, *, #6284, .F. ) ;
#70728=EDGE_LOOP ( 'NONE', ( #26338, #40212, #63939, #50933 ) ) ;
#70730=CARTESIAN_POINT ( 'NONE',  ( 11.99999999999999822, -70.53064760720297954, -26.01480285779911839 ) ) ;
#70734=DIRECTION ( 'NONE',  ( 0.000000000000000000, 0.9969173337331281859, -0.07845909572784182107 ) ) ;
#70736=AXIS2_PLACEMENT_3D ( 'NONE', #55634, #34187, #30 ) ;
#70737=DIRECTION ( 'NONE',  ( -1.000000000000000000, -0.000000000000000000, -0.000000000000000000 ) ) ;
#70742=EDGE_CURVE ( 'NONE', #9345, #60145, #23850, .T. ) ;
#70749=LINE ( 'NONE', #53841, #65660 ) ;
#70759=CARTESIAN_POINT ( 'NONE',  ( 0.000000000000000000, 46.53671651294032330, -59.03961581697353012 ) ) ;
#70775=LINE ( 'NONE', #65527, #38149 ) ;
#70781=AXIS2_PLACEMENT_3D ( 'NONE', #8636, #41724, #65418 ) ;
#70782=EDGE_CURVE ( 'NONE', #19667, #31764, #22680, .T. ) ;
#70783=LINE ( 'NONE', #60276, #7007 ) ;
#70784=VECTOR ( 'NONE', #67003, 1000.000000000000000 ) ;
#70786=CARTESIAN_POINT ( 'NONE',  ( 11.99999999999999822, 0.000000000000000000, 0.000000000000000000 ) ) ;
#70789=LINE ( 'NONE', #1683, #59889 ) ;
#70798=EDGE_CURVE ( 'NONE', #10460, #72940, #28171, .T. ) ;
#70799=CARTESIAN_POINT ( 'NONE',  ( 0.000000000000000000, 0.000000000000000000, 0.000000000000000000 ) ) ;
#70808=EDGE_LOOP ( 'NONE', ( #39144, #46964, #68641, #51300 ) ) ;
#70809=ORIENTED_EDGE ( 'NONE', *, *, #31632, .T. ) ;
#70810=VECTOR ( 'NONE', #14698, 1000.000000000000000 ) ;
#70811=EDGE_LOOP ( 'NONE', ( #60871, #484, #73709, #67505 ) ) ;
#70813=DIRECTION ( 'NONE',  ( 0.000000000000000000, -0.9510565162951543083, -0.3090169943749448977 ) ) ;
#70814=ORIENTED_EDGE ( 'NONE', *, *, #751, .F. ) ;
#70822=PLANE ( 'NONE',  #70669 ) ;
#70829=DIRECTION ( 'NONE',  ( 1.000000000000000000, 0.000000000000000000, 0.000000000000000000 ) ) ;
#70832=CARTESIAN_POINT ( 'NONE',  ( 15.00000000000000000, -19.89357724624986545, 12.59942793731086219 ) ) ;
#70833=EDGE_CURVE ( 'NONE', #64655, #42450, #73656, .T. ) ;
#70843=LINE ( 'NONE', #20467, #62685 ) ;
#70850=VERTEX_POINT ( 'NONE', #11257 ) ;
#70851=CIRCLE ( 'NONE', #36025, 82.00000000000000000 ) ;
#70853=FACE_OUTER_BOUND ( 'NONE', #73127, .T. ) ;
#70855=LINE ( 'NONE', #26481, #56762 ) ;
#70860=CIRCLE ( 'NONE', #10883, 31.99999999999997868 ) ;
#70862=DIRECTION ( 'NONE',  ( -1.000000000000000000, -0.000000000000000000, 0.000000000000000000 ) ) ;
#70865=DIRECTION ( 'NONE',  ( -1.000000000000000000, -0.000000000000000000, 0.000000000000000000 ) ) ;
#70868=DIRECTION ( 'NONE',  ( -1.000000000000000000, -0.000000000000000000, -0.000000000000000000 ) ) ;
#70878=DIRECTION ( 'NONE',  ( -1.000000000000000000, 0.000000000000000000, 0.000000000000000000 ) ) ;
#70880=DIRECTION ( 'NONE',  ( -1.000000000000000000, -0.000000000000000000, -0.000000000000000000 ) ) ;
#70885=EDGE_LOOP ( 'NONE', ( #48889, #6576, #54735, #17818 ) ) ;
#70888=ORIENTED_EDGE ( 'NONE', *, *, #12068, .F. ) ;
#70891=CIRCLE ( 'NONE', #56485, 77.49900000000000944 ) ;
#70904=VECTOR ( 'NONE', #11232, 1000.000000000000000 ) ;
#70906=ORIENTED_EDGE ( 'NONE', *, *, #14243, .T. ) ;
#70914=AXIS2_PLACEMENT_3D ( 'NONE', #23279, #46209, #68406 ) ;
#70919=ORIENTED_EDGE ( 'NONE', *, *, #57960, .F. ) ;
#70921=EDGE_LOOP ( 'NONE', ( #69463, #54844, #984, #73618 ) ) ;
#70924=CARTESIAN_POINT ( 'NONE',  ( 11.99999999999999822, -73.44644590900043113, -24.73286445877782924 ) ) ;
#70927=EDGE_CURVE ( 'NONE', #4461, #43683, #50290, .T. ) ;
#70936=EDGE_CURVE ( 'NONE', #59759, #39476, #69514, .T. ) ;
#70942=VERTEX_POINT ( 'NONE', #45862 ) ;
#70963=VERTEX_POINT ( 'NONE', #72898 ) ;
#70983=DIRECTION ( 'NONE',  ( -1.000000000000000000, 0.000000000000000000, -0.000000000000000000 ) ) ;
#70989=VERTEX_POINT ( 'NONE', #53329 ) ;
#70996=DIRECTION ( 'NONE',  ( -1.000000000000000000, -0.000000000000000000, 0.000000000000000000 ) ) ;
#71001=FACE_OUTER_BOUND ( 'NONE', #71834, .T. ) ;
#71008=ORIENTED_EDGE ( 'NONE', *, *, #29269, .F. ) ;
#71018=ORIENTED_EDGE ( 'NONE', *, *, #46944, .F. ) ;
#71019=DIRECTION ( 'NONE',  ( 0.000000000000000000, 1.000000000000000000, 1.445602896647339410E-16 ) ) ;
#71025=CARTESIAN_POINT ( 'NONE',  ( 12.00000000000000000, 16.83928648764922542, -16.46020748918050458 ) ) ;
#71028=CARTESIAN_POINT ( 'NONE',  ( 15.00000000000000000, 22.07842321921480888, -8.187992925817425771 ) ) ;
#71036=EDGE_CURVE ( 'NONE', #64851, #34378, #19117, .T. ) ;
#71041=DIRECTION ( 'NONE',  ( 0.000000000000000000, 0.8526401643540935105, -0.5224985647159468005 ) ) ;
#71051=EDGE_CURVE ( 'NONE', #32190, #6126, #59927, .T. ) ;
#71054=AXIS2_PLACEMENT_3D ( 'NONE', #42496, #19183, #70297 ) ;
#71055=CARTESIAN_POINT ( 'NONE',  ( 11.99999999999999822, -62.20884554313985149, -46.21855187248698371 ) ) ;
#71058=AXIS2_PLACEMENT_3D ( 'NONE', #44957, #38571, #55857 ) ;
#71064=AXIS2_PLACEMENT_3D ( 'NONE', #10952, #33877, #57189 ) ;
#71065=AXIS2_PLACEMENT_3D ( 'NONE', #32913, #63018, #257 ) ;
#71068=CARTESIAN_POINT ( 'NONE',  ( 11.99999999999999822, -36.72794159290197769, -65.59268652807249111 ) ) ;
#71072=ORIENTED_EDGE ( 'NONE', *, *, #22132, .T. ) ;
#71078=VERTEX_POINT ( 'NONE', #17638 ) ;
#71080=DIRECTION ( 'NONE',  ( -1.000000000000000000, 0.000000000000000000, 0.000000000000000000 ) ) ;
#71088=EDGE_CURVE ( 'NONE', #39517, #61033, #58228, .T. ) ;
#71093=ORIENTED_EDGE ( 'NONE', *, *, #73574, .T. ) ;
#71100=DIRECTION ( 'NONE',  ( -1.000000000000000000, 0.000000000000000000, -0.000000000000000000 ) ) ;
#71101=DIRECTION ( 'NONE',  ( 0.000000000000000000, 0.000000000000000000, 1.000000000000000000 ) ) ;
#71104=DIRECTION ( 'NONE',  ( -1.000000000000000000, 0.000000000000000000, -0.000000000000000000 ) ) ;
#71105=DIRECTION ( 'NONE',  ( 0.000000000000000000, 0.4539904997395413644, 0.8910065241883706744 ) ) ;
#71108=AXIS2_PLACEMENT_3D ( 'NONE', #15574, #44148, #15940 ) ;
#71109=ORIENTED_EDGE ( 'NONE', *, *, #34550, .F. ) ;
#71111=AXIS2_PLACEMENT_3D ( 'NONE', #714, #6683, #34142 ) ;
#71118=CARTESIAN_POINT ( 'NONE',  ( 0.000000000000000000, -39.47590169984795239, -71.87247863392457248 ) ) ;
#71126=ORIENTED_EDGE ( 'NONE', *, *, #12323, .F. ) ;
#71135=LINE ( 'NONE', #19637, #7270 ) ;
#71138=CARTESIAN_POINT ( 'NONE',  ( 11.99999999999999822, 55.16347631943131091, -60.67117009219074930 ) ) ;
#71139=DIRECTION ( 'NONE',  ( -1.000000000000000000, -0.000000000000000000, 0.000000000000000000 ) ) ;
#71149=ORIENTED_EDGE ( 'NONE', *, *, #31396, .T. ) ;
#71153=CARTESIAN_POINT ( 'NONE',  ( 11.99999999999999822, 0.000000000000000000, 0.000000000000000000 ) ) ;
#71164=FACE_OUTER_BOUND ( 'NONE', #58316, .T. ) ;
#71166=CIRCLE ( 'NONE', #24347, 31.99999999999998934 ) ;
#71168=EDGE_LOOP ( 'NONE', ( #63113, #22191, #52731, #70275 ) ) ;
#71185=ORIENTED_EDGE ( 'NONE', *, *, #70936, .T. ) ;
#71192=LINE ( 'NONE', #67046, #63509 ) ;
#71200=EDGE_CURVE ( 'NONE', #41863, #64009, #3533, .T. ) ;
#71201=DIRECTION ( 'NONE',  ( 0.000000000000000000, -0.9135454576426015327, 0.4067366430757989315 ) ) ;
#71207=VERTEX_POINT ( 'NONE', #32226 ) ;
#71208=CARTESIAN_POINT ( 'NONE',  ( 11.99999999999999822, 71.27951684758026829, 30.41916302227139113 ) ) ;
#71210=ORIENTED_EDGE ( 'NONE', *, *, #9071, .F. ) ;
#71212=ADVANCED_FACE ( 'NONE', ( #3701 ), #36769, .T. ) ;
#71213=CARTESIAN_POINT ( 'NONE',  ( 11.99999999999999822, -41.19522573413780009, 65.64334221924896440 ) ) ;
#71215=DIRECTION ( 'NONE',  ( -1.000000000000000000, -0.000000000000000000, 0.000000000000000000 ) ) ;
#71232=DIRECTION ( 'NONE',  ( 0.000000000000000000, 0.000000000000000000, 1.000000000000000000 ) ) ;
#71238=ORIENTED_EDGE ( 'NONE', *, *, #32503, .F. ) ;
#71247=ORIENTED_EDGE ( 'NONE', *, *, #45611, .F. ) ;
#71253=EDGE_CURVE ( 'NONE', #32106, #45883, #45557, .T. ) ;
#71255=CARTESIAN_POINT ( 'NONE',  ( 11.99999999999999822, -68.26794271651239399, -31.47745569255214093 ) ) ;
#71257=ADVANCED_FACE ( 'NONE', ( #32608 ), #68322, .T. ) ;
#71261=CARTESIAN_POINT ( 'NONE',  ( 0.000000000000000000, -23.16143007188479075, 73.95703589263966649 ) ) ;
#71271=ORIENTED_EDGE ( 'NONE', *, *, #46212, .T. ) ;
#71273=CIRCLE ( 'NONE', #501, 31.99999999999999289 ) ;
#71278=ORIENTED_EDGE ( 'NONE', *, *, #2266, .T. ) ;
#71288=EDGE_CURVE ( 'NONE', #48188, #39963, #44408, .T. ) ;
#71290=AXIS2_PLACEMENT_3D ( 'NONE', #62742, #22878, #45813 ) ;
#71298=ORIENTED_EDGE ( 'NONE', *, *, #45669, .F. ) ;
#71310=AXIS2_PLACEMENT_3D ( 'NONE', #18758, #52607, #46981 ) ;
#71312=DIRECTION ( 'NONE',  ( 0.000000000000000000, 0.000000000000000000, 1.000000000000000000 ) ) ;
#71315=DIRECTION ( 'NONE',  ( -1.000000000000000000, -0.000000000000000000, 0.000000000000000000 ) ) ;
#71317=DIRECTION ( 'NONE',  ( -1.000000000000000000, 0.000000000000000000, 0.000000000000000000 ) ) ;
#71319=CARTESIAN_POINT ( 'NONE',  ( 11.99999999999999822, -55.38113227695820484, 54.21277698773656084 ) ) ;
#71324=EDGE_LOOP ( 'NONE', ( #59745, #67597, #60300, #66929 ) ) ;
#71338=EDGE_CURVE ( 'NONE', #35131, #40037, #62705, .T. ) ;
#71340=ORIENTED_EDGE ( 'NONE', *, *, #8804, .F. ) ;
#71341=EDGE_CURVE ( 'NONE', #15633, #48915, #34098, .T. ) ;
#71345=AXIS2_PLACEMENT_3D ( 'NONE', #18252, #42311, #41193 ) ;
#71352=ADVANCED_FACE ( 'NONE', ( #10802 ), #66830, .T. ) ;
#71355=ORIENTED_EDGE ( 'NONE', *, *, #60303, .T. ) ;
#71367=ORIENTED_EDGE ( 'NONE', *, *, #64967, .F. ) ;
#71378=EDGE_LOOP ( 'NONE', ( #2803, #62082, #41682, #37361 ) ) ;
#71380=EDGE_CURVE ( 'NONE', #12604, #1097, #22802, .T. ) ;
#71384=VERTEX_POINT ( 'NONE', #46129 ) ;
#71386=DIRECTION ( 'NONE',  ( -1.000000000000000000, 0.000000000000000000, -0.000000000000000000 ) ) ;
#71387=CARTESIAN_POINT ( 'NONE',  ( 0.000000000000000000, 2.956366410620650420, 75.11725578898469280 ) ) ;
#71393=ORIENTED_EDGE ( 'NONE', *, *, #49957, .F. ) ;
#71399=CYLINDRICAL_SURFACE ( 'NONE', #66881, 31.99999999999998579 ) ;
#71402=AXIS2_PLACEMENT_3D ( 'NONE', #71841, #66234, #53825 ) ;
#71407=FACE_OUTER_BOUND ( 'NONE', #64940, .T. ) ;
#71408=CARTESIAN_POINT ( 'NONE',  ( 11.99999999999999822, 8.840884882375075193, 74.65374052328651544 ) ) ;
#71411=CYLINDRICAL_SURFACE ( 'NONE', #71054, 82.00000000000000000 ) ;
#71414=DIRECTION ( 'NONE',  ( 0.000000000000000000, -0.2079116908177641998, -0.9781476007338046896 ) ) ;
#71416=LINE ( 'NONE', #73554, #46628 ) ;
#71422=VERTEX_POINT ( 'NONE', #13657 ) ;
#71425=CIRCLE ( 'NONE', #18631, 31.99999999999999289 ) ;
#71434=VERTEX_POINT ( 'NONE', #57778 ) ;
#71435=ADVANCED_FACE ( 'NONE', ( #30942, #24943 ), #11529, .F. ) ;
#71443=CIRCLE ( 'NONE', #39067, 31.99999999999998934 ) ;
#71445=ORIENTED_EDGE ( 'NONE', *, *, #52611, .T. ) ;
#71447=EDGE_LOOP ( 'NONE', ( #13735, #25468, #11848, #26643 ) ) ;
#71451=ORIENTED_EDGE ( 'NONE', *, *, #6288, .F. ) ;
#71463=ORIENTED_EDGE ( 'NONE', *, *, #57212, .F. ) ;
#71467=ADVANCED_FACE ( 'NONE', ( #68698 ), #11901, .T. ) ;
#71472=VERTEX_POINT ( 'NONE', #63069 ) ;
#71473=CARTESIAN_POINT ( 'NONE',  ( 0.000000000000000000, 0.000000000000000000, 0.000000000000000000 ) ) ;
#71502=DIRECTION ( 'NONE',  ( 0.000000000000000000, 0.000000000000000000, 1.000000000000000000 ) ) ;
#71521=CYLINDRICAL_SURFACE ( 'NONE', #1035, 77.49899999999999523 ) ;
#71526=LINE ( 'NONE', #2790, #22190 ) ;
#71535=ADVANCED_FACE ( 'NONE', ( #15939 ), #9927, .T. ) ;
#71541=ORIENTED_EDGE ( 'NONE', *, *, #23621, .T. ) ;
#71542=AXIS2_PLACEMENT_3D ( 'NONE', #40293, #11703, #41403 ) ;
#71543=ORIENTED_EDGE ( 'NONE', *, *, #59842, .F. ) ;
#71547=DIRECTION ( 'NONE',  ( -1.000000000000000000, -0.000000000000000000, -0.000000000000000000 ) ) ;
#71556=DIRECTION ( 'NONE',  ( -1.000000000000000000, -0.000000000000000000, -0.000000000000000000 ) ) ;
#71561=DIRECTION ( 'NONE',  ( -1.000000000000000000, -0.000000000000000000, -0.000000000000000000 ) ) ;
#71565=CYLINDRICAL_SURFACE ( 'NONE', #28291, 31.99999999999998579 ) ;
#71567=DIRECTION ( 'NONE',  ( -1.000000000000000000, 0.000000000000000000, -0.000000000000000000 ) ) ;
#71594=CIRCLE ( 'NONE', #45212, 77.49899999999999523 ) ;
#71595=ORIENTED_EDGE ( 'NONE', *, *, #38875, .F. ) ;
#71597=CARTESIAN_POINT ( 'NONE',  ( 11.99999999999999822, -68.26794271651286294, 31.47745569255117104 ) ) ;
#71600=VECTOR ( 'NONE', #31263, 1000.000000000000000 ) ;
#71602=CARTESIAN_POINT ( 'NONE',  ( 11.99999999999999822, 2.956366410621684260, -75.11725578898465017 ) ) ;
#71606=AXIS2_PLACEMENT_3D ( 'NONE', #73882, #46068, #34402 ) ;
#71611=VECTOR ( 'NONE', #13623, 1000.000000000000000 ) ;
#71621=AXIS2_PLACEMENT_3D ( 'NONE', #69876, #64619, #63895 ) ;
#71623=ORIENTED_EDGE ( 'NONE', *, *, #23193, .T. ) ;
#71625=ORIENTED_EDGE ( 'NONE', *, *, #37034, .F. ) ;
#71639=EDGE_CURVE ( 'NONE', #59562, #72371, #27541, .T. ) ;
#71643=CIRCLE ( 'NONE', #6826, 31.99999999999998934 ) ;
#71646=ORIENTED_EDGE ( 'NONE', *, *, #23193, .F. ) ;
#71647=ORIENTED_EDGE ( 'NONE', *, *, #5559, .T. ) ;
#71656=EDGE_LOOP ( 'NONE', ( #64461, #425, #47178, #69304 ) ) ;
#71669=DIRECTION ( 'NONE',  ( 1.000000000000000000, -0.000000000000000000, -0.000000000000000000 ) ) ;
#71674=CIRCLE ( 'NONE', #26054, 82.00000000000000000 ) ;
#71677=AXIS2_PLACEMENT_3D ( 'NONE', #28640, #17009, #33540 ) ;
#71679=DIRECTION ( 'NONE',  ( -1.000000000000000000, -0.000000000000000000, 0.000000000000000000 ) ) ;
#71691=EDGE_CURVE ( 'NONE', #45341, #42450, #67447, .T. ) ;
#71695=ADVANCED_FACE ( 'NONE', ( #8264 ), #18435, .T. ) ;
#71705=AXIS2_PLACEMENT_3D ( 'NONE', #62585, #24200, #2037 ) ;
#71706=CARTESIAN_POINT ( 'NONE',  ( 11.99999999999999822, 8.840884882375075193, 74.65374052328651544 ) ) ;
#71714=ORIENTED_EDGE ( 'NONE', *, *, #68613, .T. ) ;
#71720=CARTESIAN_POINT ( 'NONE',  ( 11.99999999999999822, 0.000000000000000000, 0.000000000000000000 ) ) ;
#71721=EDGE_LOOP ( 'NONE', ( #15723, #74086, #40133, #70173 ) ) ;
#71730=DIRECTION ( 'NONE',  ( 0.000000000000000000, -0.8090169943749401238, -0.5877852522924831291 ) ) ;
#71735=ORIENTED_EDGE ( 'NONE', *, *, #18426, .T. ) ;
#71741=CIRCLE ( 'NONE', #2203, 77.49899999999999523 ) ;
#71748=ORIENTED_EDGE ( 'NONE', *, *, #49748, .T. ) ;
#71749=ORIENTED_EDGE ( 'NONE', *, *, #60751, .T. ) ;
#71758=EDGE_CURVE ( 'NONE', #70108, #27488, #53030, .T. ) ;
#71767=CYLINDRICAL_SURFACE ( 'NONE', #27870, 31.99999999999998579 ) ;
#71770=EDGE_CURVE ( 'NONE', #55213, #25600, #26417, .T. ) ;
#71773=AXIS2_PLACEMENT_3D ( 'NONE', #58932, #18321, #41264 ) ;
#71776=CARTESIAN_POINT ( 'NONE',  ( 15.00000000000000000, -22.67460108101782978, -6.353146135317906840 ) ) ;
#71777=AXIS2_PLACEMENT_3D ( 'NONE', #13996, #41119, #8376 ) ;
#71778=CARTESIAN_POINT ( 'NONE',  ( 12.00000000000000000, 22.07842321921480533, -8.187992925817425771 ) ) ;
#71791=CARTESIAN_POINT ( 'NONE',  ( 0.000000000000000000, 18.89407956138362010, -75.16055320797013906 ) ) ;
#71799=DIRECTION ( 'NONE',  ( 0.000000000000000000, 0.000000000000000000, 1.000000000000000000 ) ) ;
#71800=EDGE_CURVE ( 'NONE', #8982, #9094, #30447, .T. ) ;
#71802=AXIS2_PLACEMENT_3D ( 'NONE', #53772, #73189, #56286 ) ;
#71808=ORIENTED_EDGE ( 'NONE', *, *, #13178, .F. ) ;
#71814=AXIS2_PLACEMENT_3D ( 'NONE', #38904, #27980, #21977 ) ;
#71820=ORIENTED_EDGE ( 'NONE', *, *, #20686, .T. ) ;
#71822=AXIS2_PLACEMENT_3D ( 'NONE', #22402, #61516, #34048 ) ;
#71823=CARTESIAN_POINT ( 'NONE',  ( 11.99999999999999822, 71.21200624218795383, 40.65526001592638039 ) ) ;
#71827=ORIENTED_EDGE ( 'NONE', *, *, #59597, .F. ) ;
#71828=DIRECTION ( 'NONE',  ( -1.000000000000000000, 0.000000000000000000, -0.000000000000000000 ) ) ;
#71829=VERTEX_POINT ( 'NONE', #41378 ) ;
#71834=EDGE_LOOP ( 'NONE', ( #37885, #34666, #36147, #5175 ) ) ;
#71841=CARTESIAN_POINT ( 'NONE',  ( 11.99999999999999822, 72.35160999960844208, -20.41045688087747223 ) ) ;
#71853=CARTESIAN_POINT ( 'NONE',  ( 11.99999999999999822, -54.21277698773636899, -55.38113227695839669 ) ) ;
#71854=DIRECTION ( 'NONE',  ( -1.000000000000000000, -0.000000000000000000, -0.000000000000000000 ) ) ;
#71856=CIRCLE ( 'NONE', #67091, 77.49899999999999523 ) ;
#71858=EDGE_CURVE ( 'NONE', #38945, #68066, #58851, .T. ) ;
#71864=EDGE_CURVE ( 'NONE', #29201, #42911, #70851, .T. ) ;
#71869=CYLINDRICAL_SURFACE ( 'NONE', #37551, 77.49899999999999523 ) ;
#71875=ORIENTED_EDGE ( 'NONE', *, *, #10899, .F. ) ;
#71890=( GEOMETRIC_REPRESENTATION_CONTEXT ( 3 ) GLOBAL_UNCERTAINTY_ASSIGNED_CONTEXT ( ( #60175 ) ) GLOBAL_UNIT_ASSIGNED_CONTEXT ( ( #57499, #31032, #49072 ) ) REPRESENTATION_CONTEXT ( 'NONE', 'WORKASPACE' ) );
#71891=CARTESIAN_POINT ( 'NONE',  ( -10.00000000000000000, 0.000000000000000000, 0.000000000000000000 ) ) ;
#71892=CARTESIAN_POINT ( 'NONE',  ( 15.00000000000000000, 22.07842321921480888, -8.187992925817425771 ) ) ;
#71894=VERTEX_POINT ( 'NONE', #60501 ) ;
#71897=LINE ( 'NONE', #32415, #16172 ) ;
#71911=CARTESIAN_POINT ( 'NONE',  ( 11.99999999999999822, -11.30684508768393748, 76.66974797899833050 ) ) ;
#71922=DIRECTION ( 'NONE',  ( -1.000000000000000000, 0.000000000000000000, -0.000000000000000000 ) ) ;
#71924=VECTOR ( 'NONE', #50421, 1000.000000000000000 ) ;
#71930=ORIENTED_EDGE ( 'NONE', *, *, #56192, .F. ) ;
#71948=ORIENTED_EDGE ( 'NONE', *, *, #55798, .F. ) ;
#71950=CARTESIAN_POINT ( 'NONE',  ( 0.000000000000000000, -46.11716303203136391, -67.80270845531939017 ) ) ;
#71962=CARTESIAN_POINT ( 'NONE',  ( 11.99999999999999822, 0.000000000000000000, 0.000000000000000000 ) ) ;
#71966=CARTESIAN_POINT ( 'NONE',  ( 11.99999999999999822, 63.97538442413427617, 51.29473840253247374 ) ) ;
#71980=CARTESIAN_POINT ( 'NONE',  ( 11.99999999999999822, -59.46389618801999433, 49.70050353004867816 ) ) ;
#71983=ADVANCED_FACE ( 'NONE', ( #3736 ), #14987, .T. ) ;
#72002=ORIENTED_EDGE ( 'NONE', *, *, #28248, .F. ) ;
#72006=ORIENTED_EDGE ( 'NONE', *, *, #42953, .F. ) ;
#72009=CARTESIAN_POINT ( 'NONE',  ( 0.000000000000000000, 0.000000000000000000, 0.000000000000000000 ) ) ;
#72014=CIRCLE ( 'NONE', #15581, 82.00000000000000000 ) ;
#72024=CARTESIAN_POINT ( 'NONE',  ( 11.99999999999999822, -34.44570377933647620, 69.42325613327427902 ) ) ;
#72026=CARTESIAN_POINT ( 'NONE',  ( 11.99999999999999822, 66.50666863322055633, -39.78640506895536078 ) ) ;
#72035=ORIENTED_EDGE ( 'NONE', *, *, #33710, .F. ) ;
#72038=LINE ( 'NONE', #55502, #12622 ) ;
#72046=CIRCLE ( 'NONE', #8410, 77.49899999999999523 ) ;
#72049=VERTEX_POINT ( 'NONE', #73985 ) ;
#72053=AXIS2_PLACEMENT_3D ( 'NONE', #39125, #21825, #44772 ) ;
#72061=FACE_OUTER_BOUND ( 'NONE', #74233, .T. ) ;
#72065=DIRECTION ( 'NONE',  ( -1.000000000000000000, -0.000000000000000000, -0.000000000000000000 ) ) ;
#72068=CARTESIAN_POINT ( 'NONE',  ( 0.000000000000000000, -6.903761155837269570, -77.19088730480530103 ) ) ;
#72070=CARTESIAN_POINT ( 'NONE',  ( 11.99999999999999822, 0.000000000000000000, 0.000000000000000000 ) ) ;
#72075=EDGE_CURVE ( 'NONE', #44373, #13681, #73611, .T. ) ;
#72078=ORIENTED_EDGE ( 'NONE', *, *, #14063, .T. ) ;
#72079=AXIS2_PLACEMENT_3D ( 'NONE', #741, #33407, #10874 ) ;
#72081=AXIS2_PLACEMENT_3D ( 'NONE', #15297, #43890, #20192 ) ;
#72095=AXIS2_PLACEMENT_3D ( 'NONE', #18918, #1688, #20416 ) ;
#72100=PLANE ( 'NONE',  #1610 ) ;
#72105=VERTEX_POINT ( 'NONE', #16482 ) ;
#72110=EDGE_CURVE ( 'NONE', #70989, #9267, #44312, .T. ) ;
#72124=EDGE_CURVE ( 'NONE', #62825, #47275, #64906, .T. ) ;
#72126=CIRCLE ( 'NONE', #8495, 82.00000000000000000 ) ;
#72138=DIRECTION ( 'NONE',  ( -1.000000000000000000, -0.000000000000000000, 0.000000000000000000 ) ) ;
#72140=CARTESIAN_POINT ( 'NONE',  ( 0.000000000000000000, 12.93880638057426502, -76.41127070299258150 ) ) ;
#72142=ORIENTED_EDGE ( 'NONE', *, *, #917, .T. ) ;
#72145=DIRECTION ( 'NONE',  ( 0.000000000000000000, -0.8660254037844374864, 0.5000000000000019984 ) ) ;
#72154=AXIS2_PLACEMENT_3D ( 'NONE', #7457, #7084, #1491 ) ;
#72160=CARTESIAN_POINT ( 'NONE',  ( 11.99999999999999822, 55.19960302592141232, -51.03279382321027668 ) ) ;
#72163=DIRECTION ( 'NONE',  ( 0.000000000000000000, -6.938893903907231533E-15, 1.000000000000000000 ) ) ;
#72174=CARTESIAN_POINT ( 'NONE',  ( -10.00000000000000000, 0.000000000000000000, 0.000000000000000000 ) ) ;
#72175=AXIS2_PLACEMENT_3D ( 'NONE', #64395, #51623, #69655 ) ;
#72178=ORIENTED_EDGE ( 'NONE', *, *, #32044, .T. ) ;
#72179=ORIENTED_EDGE ( 'NONE', *, *, #51999, .T. ) ;
#72180=DIRECTION ( 'NONE',  ( 0.000000000000000000, -0.4539904997395350916, -0.8910065241883738940 ) ) ;
#72183=ORIENTED_EDGE ( 'NONE', *, *, #15867, .T. ) ;
#72219=CARTESIAN_POINT ( 'NONE',  ( 0.000000000000000000, 0.000000000000000000, 0.000000000000000000 ) ) ;
#72221=EDGE_LOOP ( 'NONE', ( #12523, #38372, #49248, #32704 ) ) ;
#72222=EDGE_CURVE ( 'NONE', #29677, #42164, #1308, .T. ) ;
#72224=ORIENTED_EDGE ( 'NONE', *, *, #59842, .T. ) ;
#72233=CIRCLE ( 'NONE', #61472, 31.99999999999999289 ) ;
#72234=DIRECTION ( 'NONE',  ( -1.000000000000000000, 0.000000000000000000, -0.000000000000000000 ) ) ;
#72235=CARTESIAN_POINT ( 'NONE',  ( 11.99999999999999822, 0.000000000000000000, 0.000000000000000000 ) ) ;
#72238=ORIENTED_EDGE ( 'NONE', *, *, #66278, .F. ) ;
#72240=VERTEX_POINT ( 'NONE', #35252 ) ;
#72242=DIRECTION ( 'NONE',  ( 0.000000000000000000, 0.000000000000000000, 1.000000000000000000 ) ) ;
#72253=CARTESIAN_POINT ( 'NONE',  ( 11.99999999999999822, -74.65491531819111515, 23.16904090965678265 ) ) ;
#72261=AXIS2_PLACEMENT_3D ( 'NONE', #7645, #47501, #70402 ) ;
#72268=CARTESIAN_POINT ( 'NONE',  ( 11.99999999999999822, 65.58780272294129077, -36.73666225445822420 ) ) ;
#72269=CARTESIAN_POINT ( 'NONE',  ( 11.99999999999999822, -26.02418014898359289, 70.52718814184250107 ) ) ;
#72286=DIRECTION ( 'NONE',  ( -1.000000000000000000, 0.000000000000000000, -0.000000000000000000 ) ) ;
#72288=AXIS2_PLACEMENT_3D ( 'NONE', #11240, #52199, #68770 ) ;
#72289=VERTEX_POINT ( 'NONE', #52918 ) ;
#72291=EDGE_CURVE ( 'NONE', #41798, #20819, #19111, .T. ) ;
#72293=EDGE_LOOP ( 'NONE', ( #71445, #73388, #65322, #5858 ) ) ;
#72297=VECTOR ( 'NONE', #61524, 1000.000000000000000 ) ;
#72308=VERTEX_POINT ( 'NONE', #70547 ) ;
#72317=DIRECTION ( 'NONE',  ( 0.000000000000000000, 0.000000000000000000, 1.000000000000000000 ) ) ;
#72320=ORIENTED_EDGE ( 'NONE', *, *, #40014, .F. ) ;
#72324=CARTESIAN_POINT ( 'NONE',  ( 11.99999999999999822, 58.39081064771751528, 50.95692526931350841 ) ) ;
#72326=EDGE_CURVE ( 'NONE', #1061, #366, #35912, .T. ) ;
#72328=CARTESIAN_POINT ( 'NONE',  ( 11.99999999999999822, 70.52718814184294160, -26.02418014898236720 ) ) ;
#72330=DIRECTION ( 'NONE',  ( -1.000000000000000000, 0.000000000000000000, 0.000000000000000000 ) ) ;
#72333=EDGE_CURVE ( 'NONE', #8374, #36975, #23243, .T. ) ;
#72341=CARTESIAN_POINT ( 'NONE',  ( 11.99999999999999822, 68.27212725128275395, 31.46837873495001503 ) ) ;
#72350=CIRCLE ( 'NONE', #2791, 31.99999999999998579 ) ;
#72356=FACE_OUTER_BOUND ( 'NONE', #43430, .T. ) ;
#72357=CIRCLE ( 'NONE', #7377, 77.49899999999999523 ) ;
#72358=AXIS2_PLACEMENT_3D ( 'NONE', #11537, #73207, #16827 ) ;
#72362=VERTEX_POINT ( 'NONE', #65317 ) ;
#72371=VERTEX_POINT ( 'NONE', #48746 ) ;
#72375=EDGE_CURVE ( 'NONE', #71384, #60009, #66061, .T. ) ;
#72378=DIRECTION ( 'NONE',  ( 0.000000000000000000, 0.000000000000000000, 1.000000000000000000 ) ) ;
#72384=ORIENTED_EDGE ( 'NONE', *, *, #53659, .T. ) ;
#72386=EDGE_LOOP ( 'NONE', ( #68900, #2394, #56223, #62208 ) ) ;
#72387=ORIENTED_EDGE ( 'NONE', *, *, #18518, .T. ) ;
#72389=DIRECTION ( 'NONE',  ( -1.000000000000000000, -0.000000000000000000, 0.000000000000000000 ) ) ;
#72392=DIRECTION ( 'NONE',  ( -1.000000000000000000, 0.000000000000000000, 0.000000000000000000 ) ) ;
#72397=CARTESIAN_POINT ( 'NONE',  ( 6.000000000000000000, -80.55351364060578589, -15.33399622253569383 ) ) ;
#72398=ORIENTED_EDGE ( 'NONE', *, *, #65059, .F. ) ;
#72401=EDGE_CURVE ( 'NONE', #19971, #8287, #20554, .T. ) ;
#72418=EDGE_CURVE ( 'NONE', #5982, #45341, #9266, .T. ) ;
#72423=CARTESIAN_POINT ( 'NONE',  ( 12.00000000000000000, 24.81905959214260804, -9.408202855044827118 ) ) ;
#72426=ORIENTED_EDGE ( 'NONE', *, *, #27512, .T. ) ;
#72444=EDGE_LOOP ( 'NONE', ( #62888, #28130, #45949, #58199 ) ) ;
#72446=CYLINDRICAL_SURFACE ( 'NONE', #49165, 82.00000000000000000 ) ;
#72450=ORIENTED_EDGE ( 'NONE', *, *, #66488, .F. ) ;
#72451=AXIS2_PLACEMENT_3D ( 'NONE', #9419, #33085, #4177 ) ;
#72463=FACE_OUTER_BOUND ( 'NONE', #46980, .T. ) ;
#72465=CARTESIAN_POINT ( 'NONE',  ( 0.000000000000000000, -36.72794159290288718, 65.59268652807197952 ) ) ;
#72470=AXIS2_PLACEMENT_3D ( 'NONE', #13956, #42191, #59110 ) ;
#72474=ORIENTED_EDGE ( 'NONE', *, *, #751, .T. ) ;
#72475=CARTESIAN_POINT ( 'NONE',  ( 11.99999999999999822, 75.16055320797057959, -18.89407956138179046 ) ) ;
#72477=DIRECTION ( 'NONE',  ( -1.000000000000000000, -0.000000000000000000, 0.000000000000000000 ) ) ;
#72493=EDGE_LOOP ( 'NONE', ( #16737, #71748, #73990, #5657 ) ) ;
#72496=DIRECTION ( 'NONE',  ( 1.000000000000000000, 0.000000000000000000, 0.000000000000000000 ) ) ;
#72509=CIRCLE ( 'NONE', #34096, 31.99999999999998934 ) ;
#72518=DIRECTION ( 'NONE',  ( -1.000000000000000000, 0.000000000000000000, 0.000000000000000000 ) ) ;
#72523=DIRECTION ( 'NONE',  ( 0.000000000000000000, -0.7431448254773938000, -0.6691306063588585706 ) ) ;
#72531=EDGE_CURVE ( 'NONE', #39794, #36331, #48378, .T. ) ;
#72534=VECTOR ( 'NONE', #32193, 1000.000000000000000 ) ;
#72536=CARTESIAN_POINT ( 'NONE',  ( 0.000000000000000000, 0.000000000000000000, 0.000000000000000000 ) ) ;
#72560=AXIS2_PLACEMENT_3D ( 'NONE', #66627, #15110, #38049 ) ;
#72564=ADVANCED_FACE ( 'NONE', ( #27673 ), #27285, .T. ) ;
#72565=ORIENTED_EDGE ( 'NONE', *, *, #55237, .T. ) ;
#72570=LINE ( 'NONE', #67695, #49243 ) ;
#72571=EDGE_CURVE ( 'NONE', #29346, #10762, #39571, .T. ) ;
#72573=AXIS2_PLACEMENT_3D ( 'NONE', #59668, #59294, #52530 ) ;
#72575=ORIENTED_EDGE ( 'NONE', *, *, #21049, .T. ) ;
#72579=ORIENTED_EDGE ( 'NONE', *, *, #73829, .F. ) ;
#72592=CARTESIAN_POINT ( 'NONE',  ( 0.000000000000000000, -81.50828551894220197, -8.966570791701586884 ) ) ;
#72602=CARTESIAN_POINT ( 'NONE',  ( 15.00000000000000000, 14.60985201121703980, -18.46759930825707841 ) ) ;
#72603=DIRECTION ( 'NONE',  ( 0.000000000000000000, 0.000000000000000000, 1.000000000000000000 ) ) ;
#72607=CARTESIAN_POINT ( 'NONE',  ( 11.99999999999999822, -50.95692526931287603, -58.39081064771804819 ) ) ;
#72609=CIRCLE ( 'NONE', #45016, 31.99999999999998579 ) ;
#72618=PLANE ( 'NONE',  #48461 ) ;
#72621=AXIS2_PLACEMENT_3D ( 'NONE', #8537, #66427, #15274 ) ;
#72622=CARTESIAN_POINT ( 'NONE',  ( 11.99999999999999822, 0.000000000000000000, 0.000000000000000000 ) ) ;
#72624=EDGE_CURVE ( 'NONE', #26970, #32269, #32357, .T. ) ;
#72626=FACE_OUTER_BOUND ( 'NONE', #3117, .T. ) ;
#72627=CARTESIAN_POINT ( 'NONE',  ( 11.99999999999999822, -17.28742895386031719, -75.54627589209962935 ) ) ;
#72638=ORIENTED_EDGE ( 'NONE', *, *, #61794, .F. ) ;
#72652=VECTOR ( 'NONE', #49858, 1000.000000000000000 ) ;
#72655=LINE ( 'NONE', #32807, #59721 ) ;
#72666=CARTESIAN_POINT ( 'NONE',  ( 15.00000000000000000, 23.49999999999999645, 1.499999999999995337 ) ) ;
#72675=ORIENTED_EDGE ( 'NONE', *, *, #10033, .T. ) ;
#72677=DIRECTION ( 'NONE',  ( -1.000000000000000000, -0.000000000000000000, 0.000000000000000000 ) ) ;
#72688=CARTESIAN_POINT ( 'NONE',  ( 11.99999999999999822, -26.01480285779785362, -70.53064760720343429 ) ) ;
#72694=CARTESIAN_POINT ( 'NONE',  ( 11.99999999999999822, -79.10210256391381733, 21.60688246758557796 ) ) ;
#72697=ADVANCED_FACE ( 'NONE', ( #55508 ), #73524, .F. ) ;
#72703=DIRECTION ( 'NONE',  ( 0.000000000000000000, 0.4539904997395413089, 0.8910065241883705633 ) ) ;
#72719=AXIS2_PLACEMENT_3D ( 'NONE', #69307, #51650, #11772 ) ;
#72722=EDGE_LOOP ( 'NONE', ( #11440, #23576, #62370, #51889 ) ) ;
#72723=LINE ( 'NONE', #38912, #67077 ) ;
#72730=EDGE_LOOP ( 'NONE', ( #42261, #22282, #2998, #62617 ) ) ;
#72732=ADVANCED_FACE ( 'NONE', ( #53106 ), #1643, .F. ) ;
#72736=FACE_OUTER_BOUND ( 'NONE', #9634, .T. ) ;
#72742=CARTESIAN_POINT ( 'NONE',  ( 11.99999999999999822, 40.65526001592713357, -71.21200624218752750 ) ) ;
#72747=VERTEX_POINT ( 'NONE', #64394 ) ;
#72755=ORIENTED_EDGE ( 'NONE', *, *, #34196, .F. ) ;
#72758=CARTESIAN_POINT ( 'NONE',  ( 15.00000000000000000, -14.54903810567676636, -22.19967320028755964 ) ) ;
#72763=VECTOR ( 'NONE', #53840, 1000.000000000000000 ) ;
#72769=ORIENTED_EDGE ( 'NONE', *, *, #14493, .T. ) ;
#72771=CARTESIAN_POINT ( 'NONE',  ( 11.99999999999999822, -77.19088730480528682, 6.903761155837505825 ) ) ;
#72792=LINE ( 'NONE', #55532, #41028 ) ;
#72804=CYLINDRICAL_SURFACE ( 'NONE', #4765, 82.00000000000000000 ) ;
#72816=EDGE_CURVE ( 'NONE', #69166, #32269, #24898, .T. ) ;
#72818=ORIENTED_EDGE ( 'NONE', *, *, #44168, .T. ) ;
#72819=AXIS2_PLACEMENT_3D ( 'NONE', #29901, #41203, #13722 ) ;
#72832=ORIENTED_EDGE ( 'NONE', *, *, #47052, .F. ) ;
#72854=DIRECTION ( 'NONE',  ( 0.000000000000000000, 0.000000000000000000, -1.000000000000000000 ) ) ;
#72857=ORIENTED_EDGE ( 'NONE', *, *, #8450, .F. ) ;
#72862=ORIENTED_EDGE ( 'NONE', *, *, #63347, .F. ) ;
#72866=CIRCLE ( 'NONE', #58455, 82.00000000000000000 ) ;
#72867=DIRECTION ( 'NONE',  ( 0.000000000000000000, -0.4999999999999930611, 0.8660254037844425934 ) ) ;
#72871=VECTOR ( 'NONE', #60503, 1000.000000000000000 ) ;
#72873=CARTESIAN_POINT ( 'NONE',  ( 15.00000000000000000, 8.688484142253932063, -21.88630264137371029 ) ) ;
#72875=EDGE_CURVE ( 'NONE', #21153, #5291, #66245, .T. ) ;
#72883=EDGE_CURVE ( 'NONE', #7244, #73443, #14356, .T. ) ;
#72889=CARTESIAN_POINT ( 'NONE',  ( 6.000000000000000000, 80.55351364060589958, 15.33399622253512540 ) ) ;
#72896=EDGE_CURVE ( 'NONE', #12388, #43826, #2365, .T. ) ;
#72897=DIRECTION ( 'NONE',  ( -1.000000000000000000, -0.000000000000000000, -0.000000000000000000 ) ) ;
#72898=CARTESIAN_POINT ( 'NONE',  ( 11.99999999999999822, -62.20884554314051229, 46.21855187248609553 ) ) ;
#72905=ORIENTED_EDGE ( 'NONE', *, *, #62515, .F. ) ;
#72916=ORIENTED_EDGE ( 'NONE', *, *, #20806, .F. ) ;
#72917=DIRECTION ( 'NONE',  ( 0.000000000000000000, 0.9876883405951383255, -0.1564344650402277048 ) ) ;
#72919=CARTESIAN_POINT ( 'NONE',  ( 12.00000000000000000, -11.95096189432312350, 23.69967320028773017 ) ) ;
#72921=ORIENTED_EDGE ( 'NONE', *, *, #54685, .F. ) ;
#72922=DIRECTION ( 'NONE',  ( -1.000000000000000000, 0.000000000000000000, 0.000000000000000000 ) ) ;
#72925=CYLINDRICAL_SURFACE ( 'NONE', #60555, 82.00000000000000000 ) ;
#72928=DIRECTION ( 'NONE',  ( 1.000000000000000000, -0.000000000000000000, -0.000000000000000000 ) ) ;
#72930=CYLINDRICAL_SURFACE ( 'NONE', #72053, 77.49899999999999523 ) ;
#72932=ADVANCED_FACE ( 'NONE', ( #37781 ), #8084, .T. ) ;
#72933=ORIENTED_EDGE ( 'NONE', *, *, #66073, .F. ) ;
#72937=CARTESIAN_POINT ( 'NONE',  ( 11.99999999999999822, -72.35432306680498016, 20.40083707022857951 ) ) ;
#72940=VERTEX_POINT ( 'NONE', #13715 ) ;
#72941=CIRCLE ( 'NONE', #50148, 77.49899999999998101 ) ;
#72942=ORIENTED_EDGE ( 'NONE', *, *, #19242, .T. ) ;
#72946=VECTOR ( 'NONE', #14491, 1000.000000000000000 ) ;
#72950=ORIENTED_EDGE ( 'NONE', *, *, #9855, .F. ) ;
#72955=CARTESIAN_POINT ( 'NONE',  ( 12.00000000000000000, -13.04903810567675393, -19.60159698893424718 ) ) ;
#72958=CARTESIAN_POINT ( 'NONE',  ( 0.000000000000000000, 0.000000000000000000, 0.000000000000000000 ) ) ;
#72967=EDGE_CURVE ( 'NONE', #19971, #43677, #67155, .T. ) ;
#72968=VERTEX_POINT ( 'NONE', #71966 ) ;
#72973=LINE ( 'NONE', #72602, #16659 ) ;
#72977=ORIENTED_EDGE ( 'NONE', *, *, #7654, .T. ) ;
#72982=LINE ( 'NONE', #15865, #5750 ) ;
#72987=EDGE_CURVE ( 'NONE', #42112, #37729, #8329, .T. ) ;
#72989=EDGE_CURVE ( 'NONE', #50748, #9521, #62448, .T. ) ;
#72991=VERTEX_POINT ( 'NONE', #9931 ) ;
#72992=CARTESIAN_POINT ( 'NONE',  ( 5.999999999999999112, -71.21200624218768382, -40.65526001592688488 ) ) ;
#73003=AXIS2_PLACEMENT_3D ( 'NONE', #23364, #57582, #27879 ) ;
#73006=ORIENTED_EDGE ( 'NONE', *, *, #743, .F. ) ;
#73007=VECTOR ( 'NONE', #11993, 1000.000000000000000 ) ;
#73008=CARTESIAN_POINT ( 'NONE',  ( 6.000000000000000000, -34.94270380257585629, -74.18225833017926618 ) ) ;
#73010=ORIENTED_EDGE ( 'NONE', *, *, #24352, .F. ) ;
#73013=CYLINDRICAL_SURFACE ( 'NONE', #38193, 31.99999999999998579 ) ;
#73023=CARTESIAN_POINT ( 'NONE',  ( 15.00000000000000000, -20.55727247249726020, 16.78983467731313084 ) ) ;
#73028=VERTEX_POINT ( 'NONE', #38883 ) ;
#73029=ORIENTED_EDGE ( 'NONE', *, *, #44292, .T. ) ;
#73040=EDGE_CURVE ( 'NONE', #70465, #59562, #57669, .T. ) ;
#73042=CYLINDRICAL_SURFACE ( 'NONE', #16706, 31.99999999999998579 ) ;
#73050=DIRECTION ( 'NONE',  ( -1.000000000000000000, -0.000000000000000000, -0.000000000000000000 ) ) ;
#73053=CARTESIAN_POINT ( 'NONE',  ( 15.00000000000000000, -0.9646360437375368635, -23.52805723605589705 ) ) ;
#73069=CARTESIAN_POINT ( 'NONE',  ( 11.99999999999999822, 74.65491531819105830, 8.830959090343693418 ) ) ;
#73084=AXIS2_PLACEMENT_3D ( 'NONE', #68913, #40334, #68165 ) ;
#73097=VECTOR ( 'NONE', #31564, 1000.000000000000000 ) ;
#73098=VECTOR ( 'NONE', #73371, 1000.000000000000000 ) ;
#73101=ORIENTED_EDGE ( 'NONE', *, *, #54074, .T. ) ;
#73105=ORIENTED_EDGE ( 'NONE', *, *, #39888, .T. ) ;
#73107=DIRECTION ( 'NONE',  ( -1.000000000000000000, 0.000000000000000000, 0.000000000000000000 ) ) ;
#73113=VERTEX_POINT ( 'NONE', #10308 ) ;
#73114=AXIS2_PLACEMENT_3D ( 'NONE', #72536, #37247, #66908 ) ;
#73117=CARTESIAN_POINT ( 'NONE',  ( 11.99999999999999822, -54.21277698773713638, 55.38113227695764351 ) ) ;
#73127=EDGE_LOOP ( 'NONE', ( #23422, #55909, #296, #6280 ) ) ;
#73132=CARTESIAN_POINT ( 'NONE',  ( 11.99999999999999822, 8.830959090342393125, 74.65491531819122883 ) ) ;
#73134=CARTESIAN_POINT ( 'NONE',  ( 0.000000000000000000, 33.71516098798741012, 74.74816331893441657 ) ) ;
#73136=ORIENTED_EDGE ( 'NONE', *, *, #11953, .F. ) ;
#73138=EDGE_LOOP ( 'NONE', ( #23854, #2047, #27261, #51331 ) ) ;
#73150=DIRECTION ( 'NONE',  ( 0.000000000000000000, 0.000000000000000000, 1.000000000000000000 ) ) ;
#73153=AXIS2_PLACEMENT_3D ( 'NONE', #73154, #5134, #68277 ) ;
#73154=CARTESIAN_POINT ( 'NONE',  ( 15.00000000000000000, -3.948201729842355068, -23.21447184625292692 ) ) ;
#73157=CARTESIAN_POINT ( 'NONE',  ( 11.99999999999999822, 0.000000000000000000, 0.000000000000000000 ) ) ;
#73158=DIRECTION ( 'NONE',  ( 0.000000000000000000, 0.000000000000000000, 1.000000000000000000 ) ) ;
#73160=VERTEX_POINT ( 'NONE', #72694 ) ;
#73170=ORIENTED_EDGE ( 'NONE', *, *, #7564, .T. ) ;
#73171=CIRCLE ( 'NONE', #35930, 31.99999999999998934 ) ;
#73173=ADVANCED_FACE ( 'NONE', ( #63306 ), #18531, .T. ) ;
#73180=CARTESIAN_POINT ( 'NONE',  ( 6.000000000000000000, -81.34940948281344220, 10.30890764327355846 ) ) ;
#73182=DIRECTION ( 'NONE',  ( -1.000000000000000000, 0.000000000000000000, 0.000000000000000000 ) ) ;
#73185=CARTESIAN_POINT ( 'NONE',  ( 11.99999999999999822, -21.60688246758531150, -79.10210256391390260 ) ) ;
#73189=DIRECTION ( 'NONE',  ( -1.000000000000000000, -0.000000000000000000, -0.000000000000000000 ) ) ;
#73197=DIRECTION ( 'NONE',  ( 0.000000000000000000, 0.000000000000000000, 1.000000000000000000 ) ) ;
#73206=CYLINDRICAL_SURFACE ( 'NONE', #41676, 77.49899999999999523 ) ;
#73207=DIRECTION ( 'NONE',  ( -1.000000000000000000, -0.000000000000000000, -0.000000000000000000 ) ) ;
#73208=LINE ( 'NONE', #61208, #5049 ) ;
#73215=EDGE_LOOP ( 'NONE', ( #36892, #61064, #58344, #15815 ) ) ;
#73220=EDGE_CURVE ( 'NONE', #64618, #41319, #19213, .T. ) ;
#73233=DIRECTION ( 'NONE',  ( 0.000000000000000000, -0.7431448254773954654, -0.6691306063588569053 ) ) ;
#73238=DIRECTION ( 'NONE',  ( -1.000000000000000000, 0.000000000000000000, 0.000000000000000000 ) ) ;
#73239=CYLINDRICAL_SURFACE ( 'NONE', #29276, 31.99999999999998579 ) ;
#73253=ORIENTED_EDGE ( 'NONE', *, *, #63837, .T. ) ;
#73258=CIRCLE ( 'NONE', #50452, 77.49899999999999523 ) ;
#73263=DIRECTION ( 'NONE',  ( -1.000000000000000000, 0.000000000000000000, 0.000000000000000000 ) ) ;
#73268=LINE ( 'NONE', #43344, #52877 ) ;
#73271=CARTESIAN_POINT ( 'NONE',  ( 15.00000000000000000, 0.000000000000000000, 0.000000000000000000 ) ) ;
#73274=DIRECTION ( 'NONE',  ( -1.000000000000000000, -0.000000000000000000, -0.000000000000000000 ) ) ;
#73278=DIRECTION ( 'NONE',  ( -0.000000000000000000, 0.8090169943749491166, 0.5877852522924709167 ) ) ;
#73296=AXIS2_PLACEMENT_3D ( 'NONE', #72070, #38615, #37137 ) ;
#73300=VERTEX_POINT ( 'NONE', #47485 ) ;
#73313=CARTESIAN_POINT ( 'NONE',  ( 0.000000000000000000, 31.47745569255140552, 68.26794271651274926 ) ) ;
#73315=ORIENTED_EDGE ( 'NONE', *, *, #66046, .T. ) ;
#73318=ORIENTED_EDGE ( 'NONE', *, *, #59661, .T. ) ;
#73319=ORIENTED_EDGE ( 'NONE', *, *, #56951, .T. ) ;
#73324=AXIS2_PLACEMENT_3D ( 'NONE', #16951, #56435, #68077 ) ;
#73328=VECTOR ( 'NONE', #5260, 1000.000000000000000 ) ;
#73333=VERTEX_POINT ( 'NONE', #24915 ) ;
#73340=CARTESIAN_POINT ( 'NONE',  ( 11.99999999999999822, -14.66109333815410487, -73.73191006444587003 ) ) ;
#73346=ORIENTED_EDGE ( 'NONE', *, *, #28259, .T. ) ;
#73351=DIRECTION ( 'NONE',  ( -1.000000000000000000, 0.000000000000000000, 0.000000000000000000 ) ) ;
#73355=LINE ( 'NONE', #9468, #14554 ) ;
#73371=DIRECTION ( 'NONE',  ( -1.000000000000000000, 0.000000000000000000, 0.000000000000000000 ) ) ;
#73373=ORIENTED_EDGE ( 'NONE', *, *, #53370, .F. ) ;
#73382=CARTESIAN_POINT ( 'NONE',  ( 0.000000000000000000, -77.16300072079641836, -27.74655509720752278 ) ) ;
#73383=CARTESIAN_POINT ( 'NONE',  ( 0.000000000000000000, -28.89263327155795480, 71.91182617369177876 ) ) ;
#73384=VERTEX_POINT ( 'NONE', #47845 ) ;
#73388=ORIENTED_EDGE ( 'NONE', *, *, #4442, .T. ) ;
#73389=EDGE_CURVE ( 'NONE', #18663, #68106, #37323, .T. ) ;
#73391=VERTEX_POINT ( 'NONE', #59510 ) ;
#73396=EDGE_CURVE ( 'NONE', #51872, #27944, #71135, .T. ) ;
#73397=ORIENTED_EDGE ( 'NONE', *, *, #56882, .F. ) ;
#73418=DIRECTION ( 'NONE',  ( 0.000000000000000000, 0.000000000000000000, 1.000000000000000000 ) ) ;
#73419=PLANE ( 'NONE',  #70117 ) ;
#73424=EDGE_CURVE ( 'NONE', #8256, #63525, #73268, .T. ) ;
#73431=VERTEX_POINT ( 'NONE', #8373 ) ;
#73432=FACE_OUTER_BOUND ( 'NONE', #66916, .T. ) ;
#73439=DIRECTION ( 'NONE',  ( -1.000000000000000000, -0.000000000000000000, -0.000000000000000000 ) ) ;
#73442=AXIS2_PLACEMENT_3D ( 'NONE', #34495, #69093, #10837 ) ;
#73443=VERTEX_POINT ( 'NONE', #54243 ) ;
#73453=ORIENTED_EDGE ( 'NONE', *, *, #41370, .F. ) ;
#73466=EDGE_LOOP ( 'NONE', ( #530, #54038, #68806, #55594 ) ) ;
#73468=CIRCLE ( 'NONE', #18256, 31.99999999999998579 ) ;
#73477=VECTOR ( 'NONE', #14446, 1000.000000000000000 ) ;
#73484=VECTOR ( 'NONE', #69796, 1000.000000000000000 ) ;
#73485=CYLINDRICAL_SURFACE ( 'NONE', #8138, 82.00000000000000000 ) ;
#73486=VECTOR ( 'NONE', #47839, 1000.000000000000114 ) ;
#73507=CARTESIAN_POINT ( 'NONE',  ( 0.000000000000000000, 71.27951684758026829, 30.41916302227139113 ) ) ;
#73508=VERTEX_POINT ( 'NONE', #11972 ) ;
#73513=EDGE_CURVE ( 'NONE', #72289, #30548, #49264, .T. ) ;
#73514=ORIENTED_EDGE ( 'NONE', *, *, #60095, .F. ) ;
#73518=EDGE_CURVE ( 'NONE', #10549, #70108, #54064, .T. ) ;
#73522=DIRECTION ( 'NONE',  ( 0.000000000000000000, 0.000000000000000000, 1.000000000000000000 ) ) ;
#73524=PLANE ( 'NONE',  #73153 ) ;
#73525=ORIENTED_EDGE ( 'NONE', *, *, #37117, .T. ) ;
#73527=DIRECTION ( 'NONE',  ( 0.000000000000000000, -0.9945218953682740670, -0.1045284632676459352 ) ) ;
#73529=ORIENTED_EDGE ( 'NONE', *, *, #47750, .F. ) ;
#73530=AXIS2_PLACEMENT_3D ( 'NONE', #29488, #35514, #22771 ) ;
#73533=CARTESIAN_POINT ( 'NONE',  ( 11.99999999999999822, -8.830959090342926032, 74.65491531819115778 ) ) ;
#73534=DIRECTION ( 'NONE',  ( 0.000000000000000000, 0.000000000000000000, 1.000000000000000000 ) ) ;
#73536=VECTOR ( 'NONE', #17962, 1000.000000000000000 ) ;
#73541=DIRECTION ( 'NONE',  ( -1.000000000000000000, -0.000000000000000000, -0.000000000000000000 ) ) ;
#73545=DIRECTION ( 'NONE',  ( 0.000000000000000000, 0.4539904997395413644, 0.8910065241883706744 ) ) ;
#73547=DIRECTION ( 'NONE',  ( -1.000000000000000000, 0.000000000000000000, -0.000000000000000000 ) ) ;
#73548=DIRECTION ( 'NONE',  ( -1.000000000000000000, 0.000000000000000000, 0.000000000000000000 ) ) ;
#73549=DIRECTION ( 'NONE',  ( -1.000000000000000000, 0.000000000000000000, 0.000000000000000000 ) ) ;
#73554=CARTESIAN_POINT ( 'NONE',  ( 15.00000000000000000, 22.07842321921492612, 8.187992925817123790 ) ) ;
#73555=DIRECTION ( 'NONE',  ( -1.000000000000000000, 0.000000000000000000, 0.000000000000000000 ) ) ;
#73557=EDGE_CURVE ( 'NONE', #23395, #35486, #119, .T. ) ;
#73558=CARTESIAN_POINT ( 'NONE',  ( 0.000000000000000000, -59.75363087400114637, 56.15606465354937171 ) ) ;
#73562=ADVANCED_FACE ( 'NONE', ( #51453 ), #6353, .F. ) ;
#73565=FACE_OUTER_BOUND ( 'NONE', #35615, .T. ) ;
#73568=CARTESIAN_POINT ( 'NONE',  ( 11.99999999999999822, -71.21200624218823805, 40.65526001592589722 ) ) ;
#73573=CARTESIAN_POINT ( 'NONE',  ( 11.99999999999999822, 0.000000000000000000, 0.000000000000000000 ) ) ;
#73574=EDGE_CURVE ( 'NONE', #62322, #8415, #16880, .T. ) ;
#73575=DIRECTION ( 'NONE',  ( 0.000000000000000000, -0.3090169943749350168, -0.9510565162951576390 ) ) ;
#73578=CARTESIAN_POINT ( 'NONE',  ( 11.99999999999999822, -76.66974797899844418, 11.30684508768314522 ) ) ;
#73580=EDGE_CURVE ( 'NONE', #19963, #14426, #64902, .T. ) ;
#73590=CIRCLE ( 'NONE', #41199, 31.99999999999998579 ) ;
#73594=FACE_OUTER_BOUND ( 'NONE', #20241, .T. ) ;
#73599=VERTEX_POINT ( 'NONE', #16506 ) ;
#73602=EDGE_CURVE ( 'NONE', #55862, #70850, #70891, .T. ) ;
#73603=ORIENTED_EDGE ( 'NONE', *, *, #68534, .F. ) ;
#73608=FACE_OUTER_BOUND ( 'NONE', #28290, .T. ) ;
#73611=LINE ( 'NONE', #38674, #46836 ) ;
#73616=ORIENTED_EDGE ( 'NONE', *, *, #71036, .T. ) ;
#73618=ORIENTED_EDGE ( 'NONE', *, *, #66650, .T. ) ;
#73627=CARTESIAN_POINT ( 'NONE',  ( 15.00000000000000000, 22.07842321921480888, -8.187992925817425771 ) ) ;
#73630=DIRECTION ( 'NONE',  ( 0.000000000000000000, 0.3090169943749450088, -0.9510565162951543083 ) ) ;
#73635=CARTESIAN_POINT ( 'NONE',  ( 15.00000000000000000, -14.54903810567644484, 22.19967320028775504 ) ) ;
#73637=LINE ( 'NONE', #3767, #65670 ) ;
#73639=CIRCLE ( 'NONE', #37644, 31.99999999999998934 ) ;
#73640=FACE_OUTER_BOUND ( 'NONE', #47615, .T. ) ;
#73643=EDGE_CURVE ( 'NONE', #855, #2154, #67305, .T. ) ;
#73644=CARTESIAN_POINT ( 'NONE',  ( 11.99999999999999822, -20.40083707022829174, -72.35432306680507963 ) ) ;
#73647=VECTOR ( 'NONE', #66542, 1000.000000000000000 ) ;
#73656=LINE ( 'NONE', #16157, #4659 ) ;
#73665=LINE ( 'NONE', #62041, #34176 ) ;
#73671=EDGE_CURVE ( 'NONE', #18572, #31821, #68611, .T. ) ;
#73674=ORIENTED_EDGE ( 'NONE', *, *, #72987, .T. ) ;
#73676=EDGE_CURVE ( 'NONE', #14426, #8127, #2531, .T. ) ;
#73686=EDGE_CURVE ( 'NONE', #72991, #30232, #29615, .T. ) ;
#73690=ORIENTED_EDGE ( 'NONE', *, *, #27846, .T. ) ;
#73694=ORIENTED_EDGE ( 'NONE', *, *, #73040, .F. ) ;
#73699=ORIENTED_EDGE ( 'NONE', *, *, #60012, .F. ) ;
#73707=VERTEX_POINT ( 'NONE', #24007 ) ;
#73709=ORIENTED_EDGE ( 'NONE', *, *, #1426, .T. ) ;
#73710=DIRECTION ( 'NONE',  ( 0.000000000000000000, -0.9510565162951499785, -0.3090169943749582204 ) ) ;
#73712=DIRECTION ( 'NONE',  ( -1.000000000000000000, 0.000000000000000000, -0.000000000000000000 ) ) ;
#73716=CARTESIAN_POINT ( 'NONE',  ( 11.99999999999999822, 62.50884508063427347, 41.76106447765511831 ) ) ;
#73717=DIRECTION ( 'NONE',  ( 0.000000000000000000, 0.9510565162951544194, -0.3090169943749446757 ) ) ;
#73725=ORIENTED_EDGE ( 'NONE', *, *, #46094, .F. ) ;
#73736=EDGE_CURVE ( 'NONE', #16641, #5078, #73258, .T. ) ;
#73739=AXIS2_PLACEMENT_3D ( 'NONE', #24775, #59735, #25155 ) ;
#73747=DIRECTION ( 'NONE',  ( -1.000000000000000000, -0.000000000000000000, 0.000000000000000000 ) ) ;
#73750=CIRCLE ( 'NONE', #63012, 31.99999999999998579 ) ;
#73751=CARTESIAN_POINT ( 'NONE',  ( 11.99999999999999822, 77.49459641780886443, -0.8261519478433960728 ) ) ;
#73752=ADVANCED_FACE ( 'NONE', ( #17987 ), #41649, .T. ) ;
#73759=FACE_OUTER_BOUND ( 'NONE', #71721, .T. ) ;
#73762=DIRECTION ( 'NONE',  ( -1.000000000000000000, 0.000000000000000000, -0.000000000000000000 ) ) ;
#73772=DIRECTION ( 'NONE',  ( -1.000000000000000000, -0.000000000000000000, 0.000000000000000000 ) ) ;
#73778=ORIENTED_EDGE ( 'NONE', *, *, #813, .F. ) ;
#73786=CARTESIAN_POINT ( 'NONE',  ( 0.000000000000000000, 0.000000000000000000, 0.000000000000000000 ) ) ;
#73801=AXIS2_PLACEMENT_3D ( 'NONE', #11736, #34681, #35426 ) ;
#73806=CARTESIAN_POINT ( 'NONE',  ( 0.000000000000000000, 40.65526001592713357, -71.21200624218752750 ) ) ;
#73813=CARTESIAN_POINT ( 'NONE',  ( 0.000000000000000000, 31.46837873495072913, -68.27212725128242710 ) ) ;
#73815=DIRECTION ( 'NONE',  ( 0.000000000000000000, 0.9135454576426010886, -0.4067366430757998752 ) ) ;
#73829=EDGE_CURVE ( 'NONE', #45831, #33770, #33654, .T. ) ;
#73830=DIRECTION ( 'NONE',  ( -1.000000000000000000, 0.000000000000000000, -0.000000000000000000 ) ) ;
#73831=CARTESIAN_POINT ( 'NONE',  ( 11.99999999999999822, 2.946379043147425492, -75.11764819372145041 ) ) ;
#73841=DIRECTION ( 'NONE',  ( 0.000000000000000000, -0.8526401643540860720, -0.5224985647159589019 ) ) ;
#73852=VECTOR ( 'NONE', #56248, 1000.000000000000000 ) ;
#73859=ORIENTED_EDGE ( 'NONE', *, *, #9748, .T. ) ;
#73865=DIRECTION ( 'NONE',  ( -1.000000000000000000, -0.000000000000000000, 0.000000000000000000 ) ) ;
#73877=DIRECTION ( 'NONE',  ( -1.000000000000000000, -0.000000000000000000, -0.000000000000000000 ) ) ;
#73882=CARTESIAN_POINT ( 'NONE',  ( 11.99999999999999822, 0.000000000000000000, 0.000000000000000000 ) ) ;
#73883=ORIENTED_EDGE ( 'NONE', *, *, #47444, .F. ) ;
#73885=ORIENTED_EDGE ( 'NONE', *, *, #36188, .F. ) ;
#73896=CARTESIAN_POINT ( 'NONE',  ( 11.99999999999999822, 75.54627589209944460, 17.28742895386110945 ) ) ;
#73902=AXIS2_PLACEMENT_3D ( 'NONE', #29490, #64467, #52425 ) ;
#73907=EDGE_CURVE ( 'NONE', #33472, #23343, #26204, .T. ) ;
#73915=EDGE_CURVE ( 'NONE', #72049, #59443, #19319, .T. ) ;
#73920=DIRECTION ( 'NONE',  ( 0.000000000000000000, 0.7431448254773862505, -0.6691306063588671194 ) ) ;
#73922=CIRCLE ( 'NONE', #51114, 77.49899999999999523 ) ;
#73927=AXIS2_PLACEMENT_3D ( 'NONE', #67070, #44145, #17063 ) ;
#73930=DIRECTION ( 'NONE',  ( 0.000000000000000000, 0.000000000000000000, 1.000000000000000000 ) ) ;
#73953=FACE_OUTER_BOUND ( 'NONE', #16192, .T. ) ;
#73970=ORIENTED_EDGE ( 'NONE', *, *, #37130, .F. ) ;
#73983=EDGE_CURVE ( 'NONE', #73431, #16620, #57385, .T. ) ;
#73985=CARTESIAN_POINT ( 'NONE',  ( 11.99999999999999822, -34.44570377933549565, -69.42325613327476219 ) ) ;
#73986=EDGE_LOOP ( 'NONE', ( #6037, #10023, #22760, #1507 ) ) ;
#73990=ORIENTED_EDGE ( 'NONE', *, *, #72375, .F. ) ;
#73996=CARTESIAN_POINT ( 'NONE',  ( 0.000000000000000000, -39.78640506895559525, -66.50666863322042843 ) ) ;
#74000=DIRECTION ( 'NONE',  ( -1.000000000000000000, 0.000000000000000000, 0.000000000000000000 ) ) ;
#74004=EDGE_CURVE ( 'NONE', #43826, #28647, #23182, .T. ) ;
#74010=DIRECTION ( 'NONE',  ( -1.000000000000000000, -0.000000000000000000, -0.000000000000000000 ) ) ;
#74012=DIRECTION ( 'NONE',  ( -1.000000000000000000, 0.000000000000000000, -0.000000000000000000 ) ) ;
#74021=LINE ( 'NONE', #40198, #73328 ) ;
#74030=CIRCLE ( 'NONE', #46459, 77.49899999999999523 ) ;
#74034=DIRECTION ( 'NONE',  ( 0.000000000000000000, -0.8090169943749530024, 0.5877852522924653655 ) ) ;
#74038=CIRCLE ( 'NONE', #65634, 77.49900000000000944 ) ;
#74041=DIRECTION ( 'NONE',  ( -1.000000000000000000, -0.000000000000000000, 0.000000000000000000 ) ) ;
#74042=VERTEX_POINT ( 'NONE', #17163 ) ;
#74045=ORIENTED_EDGE ( 'NONE', *, *, #71253, .T. ) ;
#74052=AXIS2_PLACEMENT_3D ( 'NONE', #37926, #21346, #35244 ) ;
#74063=ORIENTED_EDGE ( 'NONE', *, *, #34023, .T. ) ;
#74067=ORIENTED_EDGE ( 'NONE', *, *, #36475, .F. ) ;
#74070=ORIENTED_EDGE ( 'NONE', *, *, #71800, .T. ) ;
#74077=EDGE_CURVE ( 'NONE', #12380, #73300, #27698, .T. ) ;
#74086=ORIENTED_EDGE ( 'NONE', *, *, #22413, .T. ) ;
#74098=AXIS2_PLACEMENT_3D ( 'NONE', #68517, #11712, #69614 ) ;
#74105=EDGE_LOOP ( 'NONE', ( #61016, #17383, #34221, #22202 ) ) ;
#74106=EDGE_CURVE ( 'NONE', #48711, #42829, #54116, .T. ) ;
#74110=CARTESIAN_POINT ( 'NONE',  ( 0.000000000000000000, 81.90746397400387480, 3.894527615418180044 ) ) ;
#74111=DIRECTION ( 'NONE',  ( -1.000000000000000000, 0.000000000000000000, 0.000000000000000000 ) ) ;
#74116=EDGE_CURVE ( 'NONE', #74042, #30840, #72126, .T. ) ;
#74123=ADVANCED_FACE ( 'NONE', ( #58870 ), #65255, .T. ) ;
#74131=FACE_OUTER_BOUND ( 'NONE', #72493, .T. ) ;
#74148=EDGE_LOOP ( 'NONE', ( #30996, #27524, #22753, #18326 ) ) ;
#74152=LINE ( 'NONE', #61407, #22541 ) ;
#74155=ADVANCED_FACE ( 'NONE', ( #12617 ), #53225, .F. ) ;
#74165=FACE_OUTER_BOUND ( 'NONE', #4543, .T. ) ;
#74175=ORIENTED_EDGE ( 'NONE', *, *, #43327, .T. ) ;
#74180=CARTESIAN_POINT ( 'NONE',  ( 5.999999999999999112, -77.16300072079641836, -27.74655509720751922 ) ) ;
#74181=LINE ( 'NONE', #9554, #57878 ) ;
#74189=VECTOR ( 'NONE', #52842, 1000.000000000000000 ) ;
#74195=DIRECTION ( 'NONE',  ( -1.000000000000000000, -0.000000000000000000, 0.000000000000000000 ) ) ;
#74204=EDGE_CURVE ( 'NONE', #9966, #44223, #14490, .T. ) ;
#74205=EDGE_CURVE ( 'NONE', #59562, #71472, #24288, .T. ) ;
#74207=FACE_OUTER_BOUND ( 'NONE', #50286, .T. ) ;
#74210=LINE ( 'NONE', #10686, #43035 ) ;
#74211=VECTOR ( 'NONE', #72286, 1000.000000000000000 ) ;
#74228=AXIS2_PLACEMENT_3D ( 'NONE', #35185, #1016, #69761 ) ;
#74233=EDGE_LOOP ( 'NONE', ( #52617, #33239, #38835, #31695 ) ) ;
#74256=AXIS2_PLACEMENT_3D ( 'NONE', #60203, #54185, #19945 ) ;
#74258=VECTOR ( 'NONE', #13545, 999.9999999999998863 ) ;
#74264=ORIENTED_EDGE ( 'NONE', *, *, #73676, .F. ) ;
#74273=DIRECTION ( 'NONE',  ( -1.000000000000000000, 0.000000000000000000, 0.000000000000000000 ) ) ;
#74274=DIRECTION ( 'NONE',  ( 0.000000000000000000, 0.000000000000000000, 1.000000000000000000 ) ) ;
#74276=VERTEX_POINT ( 'NONE', #46852 ) ;
#74291=ORIENTED_EDGE ( 'NONE', *, *, #25229, .F. ) ;
#74307=CIRCLE ( 'NONE', #62301, 31.99999999999998579 ) ;
#74309=DIRECTION ( 'NONE',  ( -1.000000000000000000, 0.000000000000000000, -0.000000000000000000 ) ) ;
#74310=AXIS2_PLACEMENT_3D ( 'NONE', #3878, #54262, #19656 ) ;
#74328=AXIS2_PLACEMENT_3D ( 'NONE', #72219, #54574, #48562 ) ;
#74334=DIRECTION ( 'NONE',  ( 0.000000000000000000, 0.000000000000000000, -1.000000000000000000 ) ) ;
#74340=DIRECTION ( 'NONE',  ( -1.000000000000000000, -0.000000000000000000, -0.000000000000000000 ) ) ;
ENDSEC;
END-ISO-10303-21;
